ISO-10303-21;
HEADER;
/* Generated by software containing ST-Developer
 * from STEP Tools, Inc. (www.steptools.com) 
 */

FILE_DESCRIPTION(
/* description */ (''),
/* implementation_level */ '2;1');

FILE_NAME(
/* name */ '17_ISO_4762_M8x45-12.9_Socket_Head_Screw.step',
/* time_stamp */ '2026-10-23T00:52:27+05:00',
/* author */ (''),
/* organization */ (''),
/* preprocessor_version */ 'ST-DEVELOPER v20.2',
/* originating_system */ 'Autodesk Translation Framework v15.15.0.0',
/* authorisation */ '');

FILE_SCHEMA (('AUTOMOTIVE_DESIGN { 1 0 10303 214 3 1 1 }'));
ENDSEC;

DATA;
#10=MECHANICAL_DESIGN_GEOMETRIC_PRESENTATION_REPRESENTATION('',(#1573),#59204);
#313=TOROIDAL_SURFACE('',#24719,0.4333,0.04);
#559=B_SPLINE_SURFACE_WITH_KNOTS('',3,3,((#50367,#50368,#50369,#50370,#50371,
#50372,#50373,#50374,#50375,#50376,#50377,#50378,#50379,#50380,#50381,#50382,
#50383,#50384,#50385,#50386,#50387,#50388,#50389,#50390,#50391,#50392,#50393,
#50394,#50395,#50396,#50397,#50398,#50399,#50400,#50401,#50402,#50403,#50404,
#50405,#50406,#50407,#50408,#50409,#50410,#50411,#50412,#50413,#50414,#50415,
#50416,#50417,#50418,#50419,#50420,#50421,#50422,#50423,#50424,#50425,#50426,
#50427,#50428,#50429,#50430,#50431,#50432,#50433,#50434,#50435,#50436,#50437,
#50438,#50439,#50440,#50441,#50442,#50443,#50444,#50445,#50446,#50447,#50448,
#50449,#50450,#50451,#50452,#50453,#50454,#50455,#50456,#50457,#50458,#50459,
#50460,#50461,#50462,#50463,#50464,#50465,#50466,#50467,#50468,#50469,#50470,
#50471,#50472,#50473,#50474,#50475,#50476,#50477,#50478,#50479,#50480,#50481,
#50482,#50483,#50484,#50485,#50486,#50487,#50488,#50489,#50490,#50491,#50492,
#50493,#50494,#50495,#50496,#50497,#50498,#50499,#50500,#50501,#50502,#50503,
#50504,#50505,#50506,#50507,#50508,#50509,#50510,#50511,#50512),(#50513,
#50514,#50515,#50516,#50517,#50518,#50519,#50520,#50521,#50522,#50523,#50524,
#50525,#50526,#50527,#50528,#50529,#50530,#50531,#50532,#50533,#50534,#50535,
#50536,#50537,#50538,#50539,#50540,#50541,#50542,#50543,#50544,#50545,#50546,
#50547,#50548,#50549,#50550,#50551,#50552,#50553,#50554,#50555,#50556,#50557,
#50558,#50559,#50560,#50561,#50562,#50563,#50564,#50565,#50566,#50567,#50568,
#50569,#50570,#50571,#50572,#50573,#50574,#50575,#50576,#50577,#50578,#50579,
#50580,#50581,#50582,#50583,#50584,#50585,#50586,#50587,#50588,#50589,#50590,
#50591,#50592,#50593,#50594,#50595,#50596,#50597,#50598,#50599,#50600,#50601,
#50602,#50603,#50604,#50605,#50606,#50607,#50608,#50609,#50610,#50611,#50612,
#50613,#50614,#50615,#50616,#50617,#50618,#50619,#50620,#50621,#50622,#50623,
#50624,#50625,#50626,#50627,#50628,#50629,#50630,#50631,#50632,#50633,#50634,
#50635,#50636,#50637,#50638,#50639,#50640,#50641,#50642,#50643,#50644,#50645,
#50646,#50647,#50648,#50649,#50650,#50651,#50652,#50653,#50654,#50655,#50656,
#50657,#50658),(#50659,#50660,#50661,#50662,#50663,#50664,#50665,#50666,
#50667,#50668,#50669,#50670,#50671,#50672,#50673,#50674,#50675,#50676,#50677,
#50678,#50679,#50680,#50681,#50682,#50683,#50684,#50685,#50686,#50687,#50688,
#50689,#50690,#50691,#50692,#50693,#50694,#50695,#50696,#50697,#50698,#50699,
#50700,#50701,#50702,#50703,#50704,#50705,#50706,#50707,#50708,#50709,#50710,
#50711,#50712,#50713,#50714,#50715,#50716,#50717,#50718,#50719,#50720,#50721,
#50722,#50723,#50724,#50725,#50726,#50727,#50728,#50729,#50730,#50731,#50732,
#50733,#50734,#50735,#50736,#50737,#50738,#50739,#50740,#50741,#50742,#50743,
#50744,#50745,#50746,#50747,#50748,#50749,#50750,#50751,#50752,#50753,#50754,
#50755,#50756,#50757,#50758,#50759,#50760,#50761,#50762,#50763,#50764,#50765,
#50766,#50767,#50768,#50769,#50770,#50771,#50772,#50773,#50774,#50775,#50776,
#50777,#50778,#50779,#50780,#50781,#50782,#50783,#50784,#50785,#50786,#50787,
#50788,#50789,#50790,#50791,#50792,#50793,#50794,#50795,#50796,#50797,#50798,
#50799,#50800,#50801,#50802,#50803,#50804),(#50805,#50806,#50807,#50808,
#50809,#50810,#50811,#50812,#50813,#50814,#50815,#50816,#50817,#50818,#50819,
#50820,#50821,#50822,#50823,#50824,#50825,#50826,#50827,#50828,#50829,#50830,
#50831,#50832,#50833,#50834,#50835,#50836,#50837,#50838,#50839,#50840,#50841,
#50842,#50843,#50844,#50845,#50846,#50847,#50848,#50849,#50850,#50851,#50852,
#50853,#50854,#50855,#50856,#50857,#50858,#50859,#50860,#50861,#50862,#50863,
#50864,#50865,#50866,#50867,#50868,#50869,#50870,#50871,#50872,#50873,#50874,
#50875,#50876,#50877,#50878,#50879,#50880,#50881,#50882,#50883,#50884,#50885,
#50886,#50887,#50888,#50889,#50890,#50891,#50892,#50893,#50894,#50895,#50896,
#50897,#50898,#50899,#50900,#50901,#50902,#50903,#50904,#50905,#50906,#50907,
#50908,#50909,#50910,#50911,#50912,#50913,#50914,#50915,#50916,#50917,#50918,
#50919,#50920,#50921,#50922,#50923,#50924,#50925,#50926,#50927,#50928,#50929,
#50930,#50931,#50932,#50933,#50934,#50935,#50936,#50937,#50938,#50939,#50940,
#50941,#50942,#50943,#50944,#50945,#50946,#50947,#50948,#50949,#50950)),
 .UNSPECIFIED.,.F.,.F.,.F.,(4,4),(4,1,1,1,1,1,1,1,1,1,1,1,1,1,1,1,1,1,1,
1,1,1,1,1,1,1,1,1,1,1,1,1,1,1,1,1,1,1,1,1,1,1,1,1,1,1,1,1,1,1,1,1,1,1,1,
1,1,1,1,1,1,1,1,1,1,1,1,1,1,1,1,1,1,1,1,1,1,1,1,1,1,1,1,1,1,1,1,1,1,1,1,
1,1,1,1,1,1,1,1,1,1,1,1,1,1,1,1,1,1,1,1,1,1,1,1,1,1,1,1,1,1,1,1,1,1,1,1,
1,1,1,1,1,1,1,1,1,1,1,1,1,1,1,1,4),(0.,0.0820126057383863),(13.6780597280665,
14.6766929621808,15.675326196295,16.6739594304093,17.6725926645235,18.6712258986378,
19.6698591327521,20.6684923668663,21.6671256009806,22.6657588350948,23.6643920692091,
24.6630253033233,25.6616585374376,26.6602917715518,27.6589250056661,28.6575582397804,
29.6561914738946,30.6548247080089,31.6534579421231,32.6520911762374,33.6507244103516,
34.6493576444659,35.6479908785801,36.6466241126944,37.6452573468086,38.6438905809229,
39.6425238150372,40.6411570491514,41.6397902832657,42.6384235173799,43.6370567514942,
44.6356899856084,45.6343232197227,46.6329564538369,47.6315896879512,48.6302229220655,
49.6288561561797,50.627489390294,51.6261226244082,52.6247558585225,53.6233890926367,
54.622022326751,55.6206555608652,56.6192887949795,57.6179220290938,58.616555263208,
59.6151884973223,60.6138217314365,61.6124549655508,62.611088199665,63.6097214337793,
64.6083546678935,65.6069879020078,66.6056211361221,67.6042543702363,68.6028876043506,
69.6015208384648,70.6001540725791,71.5987873066933,72.5974205408076,73.5960537749218,
74.5946870090361,75.5933202431503,76.5919534772646,77.5905867113789,78.5892199454931,
79.5878531796074,80.5864864137216,81.5851196478359,82.5837528819501,83.5823861160644,
84.5810193501787,85.5796525842929,86.5782858184072,87.5769190525214,88.5755522866357,
89.5741855207499,90.5728187548642,91.5714519889784,92.5700852230927,93.568718457207,
94.5673516913212,95.5659849254355,96.5646181595497,97.563251393664,98.5618846277782,
99.5605178618925,100.559151096007,101.557784330121,102.556417564235,103.555050798349,
104.553684032464,105.552317266578,106.550950500692,107.549583734807,108.548216968921,
109.546850203035,110.545483437149,111.544116671264,112.542749905378,113.541383139492,
114.540016373606,115.538649607721,116.537282841835,117.535916075949,118.534549310063,
119.533182544178,120.531815778292,121.530449012406,122.52908224652,123.527715480635,
124.526348714749,125.524981948863,126.523615182977,127.522248417092,128.520881651206,
129.51951488532,130.518148119434,131.516781353549,132.515414587663,133.514047821777,
134.512681055891,135.511314290006,136.50994752412,137.508580758234,138.507213992348,
139.505847226463,140.504480460577,141.503113694691,142.501746928805,143.50038016292,
144.499013397034,145.497646631148,146.496279865262,147.494913099377,148.493546333491,
149.492179567605,150.490812801719,151.489446035834,152.488079269948,153.486712504062,
154.485345738177,155.483978972291,156.482612206405),.UNSPECIFIED.);
#560=B_SPLINE_SURFACE_WITH_KNOTS('',3,3,((#51107,#51108,#51109,#51110,#51111,
#51112,#51113,#51114,#51115,#51116,#51117,#51118,#51119,#51120,#51121,#51122,
#51123,#51124,#51125,#51126,#51127,#51128,#51129,#51130,#51131,#51132,#51133,
#51134,#51135,#51136,#51137,#51138,#51139,#51140,#51141,#51142,#51143,#51144,
#51145,#51146,#51147,#51148,#51149,#51150,#51151,#51152,#51153,#51154,#51155,
#51156,#51157,#51158,#51159,#51160,#51161,#51162,#51163,#51164,#51165,#51166,
#51167,#51168,#51169,#51170,#51171,#51172,#51173,#51174,#51175,#51176,#51177,
#51178,#51179,#51180,#51181,#51182,#51183,#51184,#51185,#51186,#51187,#51188,
#51189,#51190,#51191,#51192,#51193,#51194,#51195,#51196,#51197,#51198,#51199,
#51200,#51201,#51202,#51203,#51204,#51205,#51206,#51207,#51208,#51209,#51210,
#51211,#51212,#51213,#51214,#51215,#51216,#51217,#51218,#51219,#51220,#51221,
#51222,#51223,#51224,#51225,#51226,#51227,#51228,#51229,#51230,#51231,#51232,
#51233,#51234,#51235,#51236,#51237,#51238,#51239,#51240,#51241,#51242,#51243,
#51244,#51245,#51246,#51247,#51248,#51249,#51250,#51251,#51252),(#51253,
#51254,#51255,#51256,#51257,#51258,#51259,#51260,#51261,#51262,#51263,#51264,
#51265,#51266,#51267,#51268,#51269,#51270,#51271,#51272,#51273,#51274,#51275,
#51276,#51277,#51278,#51279,#51280,#51281,#51282,#51283,#51284,#51285,#51286,
#51287,#51288,#51289,#51290,#51291,#51292,#51293,#51294,#51295,#51296,#51297,
#51298,#51299,#51300,#51301,#51302,#51303,#51304,#51305,#51306,#51307,#51308,
#51309,#51310,#51311,#51312,#51313,#51314,#51315,#51316,#51317,#51318,#51319,
#51320,#51321,#51322,#51323,#51324,#51325,#51326,#51327,#51328,#51329,#51330,
#51331,#51332,#51333,#51334,#51335,#51336,#51337,#51338,#51339,#51340,#51341,
#51342,#51343,#51344,#51345,#51346,#51347,#51348,#51349,#51350,#51351,#51352,
#51353,#51354,#51355,#51356,#51357,#51358,#51359,#51360,#51361,#51362,#51363,
#51364,#51365,#51366,#51367,#51368,#51369,#51370,#51371,#51372,#51373,#51374,
#51375,#51376,#51377,#51378,#51379,#51380,#51381,#51382,#51383,#51384,#51385,
#51386,#51387,#51388,#51389,#51390,#51391,#51392,#51393,#51394,#51395,#51396,
#51397,#51398),(#51399,#51400,#51401,#51402,#51403,#51404,#51405,#51406,
#51407,#51408,#51409,#51410,#51411,#51412,#51413,#51414,#51415,#51416,#51417,
#51418,#51419,#51420,#51421,#51422,#51423,#51424,#51425,#51426,#51427,#51428,
#51429,#51430,#51431,#51432,#51433,#51434,#51435,#51436,#51437,#51438,#51439,
#51440,#51441,#51442,#51443,#51444,#51445,#51446,#51447,#51448,#51449,#51450,
#51451,#51452,#51453,#51454,#51455,#51456,#51457,#51458,#51459,#51460,#51461,
#51462,#51463,#51464,#51465,#51466,#51467,#51468,#51469,#51470,#51471,#51472,
#51473,#51474,#51475,#51476,#51477,#51478,#51479,#51480,#51481,#51482,#51483,
#51484,#51485,#51486,#51487,#51488,#51489,#51490,#51491,#51492,#51493,#51494,
#51495,#51496,#51497,#51498,#51499,#51500,#51501,#51502,#51503,#51504,#51505,
#51506,#51507,#51508,#51509,#51510,#51511,#51512,#51513,#51514,#51515,#51516,
#51517,#51518,#51519,#51520,#51521,#51522,#51523,#51524,#51525,#51526,#51527,
#51528,#51529,#51530,#51531,#51532,#51533,#51534,#51535,#51536,#51537,#51538,
#51539,#51540,#51541,#51542,#51543,#51544),(#51545,#51546,#51547,#51548,
#51549,#51550,#51551,#51552,#51553,#51554,#51555,#51556,#51557,#51558,#51559,
#51560,#51561,#51562,#51563,#51564,#51565,#51566,#51567,#51568,#51569,#51570,
#51571,#51572,#51573,#51574,#51575,#51576,#51577,#51578,#51579,#51580,#51581,
#51582,#51583,#51584,#51585,#51586,#51587,#51588,#51589,#51590,#51591,#51592,
#51593,#51594,#51595,#51596,#51597,#51598,#51599,#51600,#51601,#51602,#51603,
#51604,#51605,#51606,#51607,#51608,#51609,#51610,#51611,#51612,#51613,#51614,
#51615,#51616,#51617,#51618,#51619,#51620,#51621,#51622,#51623,#51624,#51625,
#51626,#51627,#51628,#51629,#51630,#51631,#51632,#51633,#51634,#51635,#51636,
#51637,#51638,#51639,#51640,#51641,#51642,#51643,#51644,#51645,#51646,#51647,
#51648,#51649,#51650,#51651,#51652,#51653,#51654,#51655,#51656,#51657,#51658,
#51659,#51660,#51661,#51662,#51663,#51664,#51665,#51666,#51667,#51668,#51669,
#51670,#51671,#51672,#51673,#51674,#51675,#51676,#51677,#51678,#51679,#51680,
#51681,#51682,#51683,#51684,#51685,#51686,#51687,#51688,#51689,#51690)),
 .UNSPECIFIED.,.F.,.F.,.F.,(4,4),(4,1,1,1,1,1,1,1,1,1,1,1,1,1,1,1,1,1,1,
1,1,1,1,1,1,1,1,1,1,1,1,1,1,1,1,1,1,1,1,1,1,1,1,1,1,1,1,1,1,1,1,1,1,1,1,
1,1,1,1,1,1,1,1,1,1,1,1,1,1,1,1,1,1,1,1,1,1,1,1,1,1,1,1,1,1,1,1,1,1,1,1,
1,1,1,1,1,1,1,1,1,1,1,1,1,1,1,1,1,1,1,1,1,1,1,1,1,1,1,1,1,1,1,1,1,1,1,1,
1,1,1,1,1,1,1,1,1,1,1,1,1,1,1,1,4),(0.,0.0820126057383863),(16.9785412059632,
17.9771744400775,18.9758076741917,19.974440908306,20.9730741424202,21.9717073765345,
22.9703406106487,23.968973844763,24.9676070788772,25.9662403129915,26.9648735471058,
27.96350678122,28.9621400153343,29.9607732494485,30.9594064835628,31.958039717677,
32.9566729517913,33.9553061859055,34.9539394200198,35.9525726541341,36.9512058882483,
37.9498391223626,38.9484723564768,39.9471055905911,40.9457388247053,41.9443720588196,
42.9430052929338,43.9416385270481,44.9402717611624,45.9389049952766,46.9375382293909,
47.9361714635051,48.9348046976194,49.9334379317336,50.9320711658479,51.9307043999621,
52.9293376340764,53.9279708681906,54.9266041023049,55.9252373364192,56.9238705705334,
57.9225038046477,58.9211370387619,59.9197702728762,60.9184035069904,61.9170367411047,
62.9156699752189,63.9143032093332,64.9129364434474,65.9115696775617,66.910202911676,
67.9088361457902,68.9074693799045,69.9061026140187,70.904735848133,71.9033690822472,
72.9020023163615,73.9006355504758,74.89926878459,75.8979020187043,76.8965352528185,
77.8951684869328,78.893801721047,79.8924349551613,80.8910681892755,81.8897014233898,
82.888334657504,83.8869678916183,84.8856011257326,85.8842343598468,86.8828675939611,
87.8815008280753,88.8801340621896,89.8787672963038,90.8774005304181,91.8760337645324,
92.8746669986466,93.8733002327609,94.8719334668751,95.8705667009894,96.8691999351036,
97.8678331692179,98.8664664033321,99.8650996374464,100.863732871561,101.862366105675,
102.860999339789,103.859632573903,104.858265808018,105.856899042132,106.855532276246,
107.85416551036,108.852798744475,109.851431978589,110.850065212703,111.848698446817,
112.847331680932,113.845964915046,114.84459814916,115.843231383274,116.841864617389,
117.840497851503,118.839131085617,119.837764319731,120.836397553846,121.83503078796,
122.833664022074,123.832297256189,124.830930490303,125.829563724417,126.828196958531,
127.826830192646,128.82546342676,129.824096660874,130.822729894988,131.821363129103,
132.819996363217,133.818629597331,134.817262831445,135.81589606556,136.814529299674,
137.813162533788,138.811795767902,139.810429002017,140.809062236131,141.807695470245,
142.806328704359,143.804961938474,144.803595172588,145.802228406702,146.800861640816,
147.799494874931,148.798128109045,149.796761343159,150.795394577273,151.794027811388,
152.792661045502,153.791294279616,154.78992751373,155.788560747845,156.787193981959,
157.785827216073,158.784460450187,159.783093684302),.UNSPECIFIED.);
#1277=B_SPLINE_CURVE_WITH_KNOTS('',3,(#48579,#48580,#48581,#48582,#48583,
#48584,#48585,#48586,#48587,#48588,#48589,#48590,#48591),.UNSPECIFIED.,
 .F.,.F.,(4,3,3,3,4),(-5.01260736916534,-4.99316617057127,-3.99453293645702,
-2.99589970234276,-2.06120159751579),.UNSPECIFIED.);
#1278=B_SPLINE_CURVE_WITH_KNOTS('',3,(#48599,#48600,#48601,#48602,#48603,
#48604,#48605,#48606,#48607,#48608),.UNSPECIFIED.,.F.,.F.,(4,3,3,4),(0.,
0.998633234114252,1.99726646822851,2.02990353988235),.UNSPECIFIED.);
#1279=B_SPLINE_CURVE_WITH_KNOTS('',3,(#48613,#48614,#48615,#48616,#48617,
#48618,#48619,#48620,#48621,#48622,#48623,#48624,#48625,#48626,#48627,#48628,
#48629,#48630,#48631,#48632,#48633,#48634),.UNSPECIFIED.,.F.,.F.,(4,3,3,
3,3,3,3,4),(-11.2957926763449,-10.9849655752568,-9.98633234114256,-8.9876991070283,
-7.98906587291404,-6.99043263879979,-5.99179940468553,-5.01260736916534),
 .UNSPECIFIED.);
#1280=B_SPLINE_CURVE_WITH_KNOTS('',3,(#48635,#48636,#48637,#48638,#48639,
#48640,#48641,#48642,#48643,#48644,#48645,#48646,#48647,#48648,#48649,#48650,
#48651,#48652,#48653,#48654,#48655,#48656),.UNSPECIFIED.,.F.,.F.,(4,3,3,
3,3,3,3,4),(2.02990353988235,2.99589970234276,3.99453293645702,4.99316617057127,
5.99179940468553,6.99043263879979,7.98906587291404,8.31308884706194),
 .UNSPECIFIED.);
#1281=B_SPLINE_CURVE_WITH_KNOTS('',3,(#48661,#48662,#48663,#48664,#48665,
#48666,#48667,#48668,#48669,#48670,#48671,#48672,#48673,#48674,#48675,#48676,
#48677,#48678,#48679,#48680,#48681,#48682),.UNSPECIFIED.,.F.,.F.,(4,3,3,
3,3,3,3,4),(-17.5789779835245,-16.9767649799423,-15.9781317458281,-14.9794985117138,
-13.9808652775996,-12.9822320434853,-11.9835988093711,-11.2957926763449),
 .UNSPECIFIED.);
#1282=B_SPLINE_CURVE_WITH_KNOTS('',3,(#48683,#48684,#48685,#48686,#48687,
#48688,#48689,#48690,#48691,#48692,#48693,#48694,#48695,#48696,#48697,#48698,
#48699,#48700,#48701,#48702,#48703,#48704),.UNSPECIFIED.,.F.,.F.,(4,3,3,
3,3,3,3,4),(8.31308884706194,8.9876991070283,9.98633234114255,10.9849655752568,
11.9835988093711,12.9822320434853,13.9808652775996,14.5962741542415),
 .UNSPECIFIED.);
#1283=B_SPLINE_CURVE_WITH_KNOTS('',3,(#48709,#48710,#48711,#48712,#48713,
#48714,#48715,#48716,#48717,#48718,#48719,#48720,#48721,#48722,#48723,#48724,
#48725,#48726,#48727,#48728,#48729,#48730),.UNSPECIFIED.,.F.,.F.,(4,3,3,
3,3,3,3,4),(-23.8621632907041,-22.9685643846279,-21.9699311505136,-20.9712979163994,
-19.9726646822851,-18.9740314481709,-17.9753982140566,-17.5789779835245),
 .UNSPECIFIED.);
#1284=B_SPLINE_CURVE_WITH_KNOTS('',3,(#48731,#48732,#48733,#48734,#48735,
#48736,#48737,#48738,#48739,#48740,#48741,#48742,#48743,#48744,#48745,#48746,
#48747,#48748,#48749,#48750,#48751,#48752),.UNSPECIFIED.,.F.,.F.,(4,3,3,
3,3,3,3,4),(14.5962741542415,14.9794985117138,15.9781317458281,16.9767649799423,
17.9753982140566,18.9740314481709,19.9726646822851,20.8794594614211),
 .UNSPECIFIED.);
#1285=B_SPLINE_CURVE_WITH_KNOTS('',3,(#48757,#48758,#48759,#48760,#48761,
#48762,#48763,#48764,#48765,#48766,#48767,#48768,#48769,#48770,#48771,#48772,
#48773,#48774,#48775,#48776,#48777,#48778,#48779,#48780,#48781),
 .UNSPECIFIED.,.F.,.F.,(4,3,3,3,3,3,3,3,4),(-30.1453485978837,-29.9589970234277,
-28.9603637893134,-27.9617305551992,-26.9630973210849,-25.9644640869706,
-24.9658308528564,-23.9671976187421,-23.8621632907041),.UNSPECIFIED.);
#1286=B_SPLINE_CURVE_WITH_KNOTS('',3,(#48782,#48783,#48784,#48785,#48786,
#48787,#48788,#48789,#48790,#48791,#48792,#48793,#48794,#48795,#48796,#48797,
#48798,#48799,#48800,#48801,#48802,#48803,#48804,#48805,#48806),
 .UNSPECIFIED.,.F.,.F.,(4,3,3,3,3,3,3,3,4),(20.8794594614211,20.9712979163994,
21.9699311505136,22.9685643846279,23.9671976187421,24.9658308528564,25.9644640869706,
26.9630973210849,27.1626447686007),.UNSPECIFIED.);
#1287=B_SPLINE_CURVE_WITH_KNOTS('',3,(#48811,#48812,#48813,#48814,#48815,
#48816,#48817,#48818,#48819,#48820,#48821,#48822,#48823,#48824,#48825,#48826,
#48827,#48828,#48829,#48830,#48831,#48832),.UNSPECIFIED.,.F.,.F.,(4,3,3,
3,3,3,3,4),(-36.4285339050633,-35.9507964281132,-34.9521631939989,-33.9535299598847,
-32.9548967257704,-31.9562634916562,-30.9576302575419,-30.1453485978837),
 .UNSPECIFIED.);
#1288=B_SPLINE_CURVE_WITH_KNOTS('',3,(#48833,#48834,#48835,#48836,#48837,
#48838,#48839,#48840,#48841,#48842,#48843,#48844,#48845,#48846,#48847,#48848,
#48849,#48850,#48851,#48852,#48853,#48854),.UNSPECIFIED.,.F.,.F.,(4,3,3,
3,3,3,3,4),(27.1626447686007,27.9617305551991,28.9603637893134,29.9589970234277,
30.9576302575419,31.9562634916562,32.9548967257704,33.4458300757803),
 .UNSPECIFIED.);
#1289=B_SPLINE_CURVE_WITH_KNOTS('',3,(#48859,#48860,#48861,#48862,#48863,
#48864,#48865,#48866,#48867,#48868,#48869,#48870,#48871,#48872,#48873,#48874,
#48875,#48876,#48877,#48878,#48879,#48880),.UNSPECIFIED.,.F.,.F.,(4,3,3,
3,3,3,3,4),(-42.7117192122429,-41.9425958327987,-40.9439625986845,-39.9453293645702,
-38.946696130456,-37.9480628963417,-36.9494296622274,-36.4285339050633),
 .UNSPECIFIED.);
#1290=B_SPLINE_CURVE_WITH_KNOTS('',3,(#48881,#48882,#48883,#48884,#48885,
#48886,#48887,#48888,#48889,#48890,#48891,#48892,#48893,#48894,#48895,#48896,
#48897,#48898,#48899,#48900,#48901,#48902),.UNSPECIFIED.,.F.,.F.,(4,3,3,
3,3,3,3,4),(33.4458300757803,33.9535299598847,34.9521631939989,35.9507964281132,
36.9494296622274,37.9480628963417,38.946696130456,39.7290153829599),
 .UNSPECIFIED.);
#1291=B_SPLINE_CURVE_WITH_KNOTS('',3,(#48907,#48908,#48909,#48910,#48911,
#48912,#48913,#48914,#48915,#48916,#48917,#48918,#48919,#48920,#48921,#48922,
#48923,#48924,#48925,#48926,#48927,#48928,#48929,#48930,#48931),
 .UNSPECIFIED.,.F.,.F.,(4,3,3,3,3,3,3,3,4),(-48.9949045194225,-48.9330284715985,
-47.9343952374843,-46.93576200337,-45.9371287692558,-44.9384955351415,-43.9398623010272,
-42.941229066913,-42.7117192122429),.UNSPECIFIED.);
#1292=B_SPLINE_CURVE_WITH_KNOTS('',3,(#48932,#48933,#48934,#48935,#48936,
#48937,#48938,#48939,#48940,#48941,#48942,#48943,#48944,#48945,#48946,#48947,
#48948,#48949,#48950,#48951,#48952,#48953,#48954,#48955,#48956),
 .UNSPECIFIED.,.F.,.F.,(4,3,3,3,3,3,3,3,4),(39.7290153829599,39.9453293645702,
40.9439625986845,41.9425958327987,42.941229066913,43.9398623010272,44.9384955351415,
45.9371287692557,46.0122006901395),.UNSPECIFIED.);
#1293=B_SPLINE_CURVE_WITH_KNOTS('',3,(#48961,#48962,#48963,#48964,#48965,
#48966,#48967,#48968,#48969,#48970,#48971,#48972,#48973,#48974,#48975,#48976,
#48977,#48978,#48979,#48980,#48981,#48982),.UNSPECIFIED.,.F.,.F.,(4,3,3,
3,3,3,3,4),(-55.278089826602,-54.924827876284,-53.9261946421698,-52.9275614080555,
-51.9289281739413,-50.930294939827,-49.9316617057128,-48.9949045194225),
 .UNSPECIFIED.);
#1294=B_SPLINE_CURVE_WITH_KNOTS('',3,(#48983,#48984,#48985,#48986,#48987,
#48988,#48989,#48990,#48991,#48992,#48993,#48994,#48995,#48996,#48997,#48998,
#48999,#49000,#49001,#49002,#49003,#49004),.UNSPECIFIED.,.F.,.F.,(4,3,3,
3,3,3,3,4),(46.0122006901395,46.93576200337,47.9343952374843,48.9330284715985,
49.9316617057128,50.930294939827,51.9289281739413,52.2953859973191),
 .UNSPECIFIED.);
#1295=B_SPLINE_CURVE_WITH_KNOTS('',3,(#49009,#49010,#49011,#49012,#49013,
#49014,#49015,#49016,#49017,#49018,#49019,#49020,#49021,#49022,#49023,#49024,
#49025,#49026,#49027,#49028,#49029,#49030),.UNSPECIFIED.,.F.,.F.,(4,3,3,
3,3,3,3,4),(-61.5612751337816,-60.9166272809696,-59.9179940468553,-58.9193608127411,
-57.9207275786268,-56.9220943445126,-55.9234611103983,-55.278089826602),
 .UNSPECIFIED.);
#1296=B_SPLINE_CURVE_WITH_KNOTS('',3,(#49031,#49032,#49033,#49034,#49035,
#49036,#49037,#49038,#49039,#49040,#49041,#49042,#49043,#49044,#49045,#49046,
#49047,#49048,#49049,#49050,#49051,#49052),.UNSPECIFIED.,.F.,.F.,(4,3,3,
3,3,3,3,4),(52.2953859973191,52.9275614080555,53.9261946421698,54.9248278762841,
55.9234611103983,56.9220943445126,57.9207275786268,58.5785713044986),
 .UNSPECIFIED.);
#1297=B_SPLINE_CURVE_WITH_KNOTS('',3,(#49057,#49058,#49059,#49060,#49061,
#49062,#49063,#49064,#49065,#49066,#49067,#49068,#49069,#49070,#49071,#49072,
#49073,#49074,#49075,#49076,#49077,#49078),.UNSPECIFIED.,.F.,.F.,(4,3,3,
3,3,3,3,4),(-67.8444604409612,-66.9084266856551,-65.9097934515409,-64.9111602174266,
-63.9125269833123,-62.9138937491981,-61.9152605150838,-61.5612751337816),
 .UNSPECIFIED.);
#1298=B_SPLINE_CURVE_WITH_KNOTS('',3,(#49079,#49080,#49081,#49082,#49083,
#49084,#49085,#49086,#49087,#49088,#49089,#49090,#49091,#49092,#49093,#49094,
#49095,#49096,#49097,#49098,#49099,#49100),.UNSPECIFIED.,.F.,.F.,(4,3,3,
3,3,3,3,4),(58.5785713044986,58.9193608127411,59.9179940468553,60.9166272809696,
61.9152605150838,62.9138937491981,63.9125269833123,64.8617566116782),
 .UNSPECIFIED.);
#1299=B_SPLINE_CURVE_WITH_KNOTS('',3,(#49105,#49106,#49107,#49108,#49109,
#49110,#49111,#49112,#49113,#49114,#49115,#49116,#49117,#49118,#49119,#49120,
#49121,#49122,#49123,#49124,#49125,#49126,#49127,#49128,#49129),
 .UNSPECIFIED.,.F.,.F.,(4,3,3,3,3,3,3,3,4),(-74.1276457481408,-73.8988593244549,
-72.9002260903406,-71.9015928562264,-70.9029596221121,-69.9043263879979,
-68.9056931538836,-67.9070599197694,-67.8444604409612),.UNSPECIFIED.);
#1300=B_SPLINE_CURVE_WITH_KNOTS('',3,(#49130,#49131,#49132,#49133,#49134,
#49135,#49136,#49137,#49138,#49139,#49140,#49141,#49142,#49143,#49144,#49145,
#49146,#49147,#49148,#49149,#49150,#49151,#49152,#49153,#49154),
 .UNSPECIFIED.,.F.,.F.,(4,3,3,3,3,3,3,3,4),(64.8617566116782,64.9111602174266,
65.9097934515408,66.9084266856551,67.9070599197694,68.9056931538836,69.9043263879979,
70.9029596221121,71.1449419188578),.UNSPECIFIED.);
#1301=B_SPLINE_CURVE_WITH_KNOTS('',3,(#49159,#49160,#49161,#49162,#49163,
#49164,#49165,#49166,#49167,#49168,#49169,#49170,#49171,#49172,#49173,#49174,
#49175,#49176,#49177,#49178,#49179,#49180),.UNSPECIFIED.,.F.,.F.,(4,3,3,
3,3,3,3,4),(-80.4108310553204,-79.8906587291404,-78.8920254950262,-77.8933922609119,
-76.8947590267977,-75.8961257926834,-74.8974925585692,-74.1276457481408),
 .UNSPECIFIED.);
#1302=B_SPLINE_CURVE_WITH_KNOTS('',3,(#49181,#49182,#49183,#49184,#49185,
#49186,#49187,#49188,#49189,#49190,#49191,#49192,#49193,#49194,#49195,#49196,
#49197,#49198,#49199,#49200,#49201,#49202),.UNSPECIFIED.,.F.,.F.,(4,3,3,
3,3,3,3,4),(71.1449419188578,71.9015928562264,72.9002260903406,73.8988593244549,
74.8974925585692,75.8961257926834,76.8947590267977,77.4281272260374),
 .UNSPECIFIED.);
#1303=B_SPLINE_CURVE_WITH_KNOTS('',3,(#49207,#49208,#49209,#49210,#49211,
#49212,#49213,#49214,#49215,#49216,#49217,#49218,#49219,#49220,#49221,#49222,
#49223,#49224,#49225,#49226,#49227,#49228),.UNSPECIFIED.,.F.,.F.,(4,3,3,
3,3,3,3,4),(-86.6940163625,-85.882458133826,-84.8838248997117,-83.8851916655974,
-82.8865584314832,-81.8879251973689,-80.8892919632547,-80.4108310553204),
 .UNSPECIFIED.);
#1304=B_SPLINE_CURVE_WITH_KNOTS('',3,(#49229,#49230,#49231,#49232,#49233,
#49234,#49235,#49236,#49237,#49238,#49239,#49240,#49241,#49242,#49243,#49244,
#49245,#49246,#49247,#49248,#49249,#49250),.UNSPECIFIED.,.F.,.F.,(4,3,3,
3,3,3,3,4),(77.4281272260374,77.8933922609119,78.8920254950262,79.8906587291404,
80.8892919632547,81.887925197369,82.8865584314832,83.711312533217),
 .UNSPECIFIED.);
#1305=B_SPLINE_CURVE_WITH_KNOTS('',3,(#49255,#49256,#49257,#49258,#49259,
#49260,#49261,#49262,#49263,#49264,#49265,#49266,#49267,#49268,#49269,#49270,
#49271,#49272,#49273,#49274,#49275,#49276,#49277,#49278,#49279),
 .UNSPECIFIED.,.F.,.F.,(4,3,3,3,3,3,3,3,4),(-92.9772016696796,-92.8728907726257,
-91.8742575385115,-90.8756243043972,-89.876991070283,-88.8783578361687,
-87.8797246020545,-86.8810913679402,-86.6940163625),.UNSPECIFIED.);
#1306=B_SPLINE_CURVE_WITH_KNOTS('',3,(#49280,#49281,#49282,#49283,#49284,
#49285,#49286,#49287,#49288,#49289,#49290,#49291,#49292,#49293,#49294,#49295,
#49296,#49297,#49298,#49299,#49300,#49301,#49302,#49303,#49304),
 .UNSPECIFIED.,.F.,.F.,(4,3,3,3,3,3,3,3,4),(83.711312533217,83.8851916655975,
84.8838248997117,85.882458133826,86.8810913679402,87.8797246020545,88.8783578361687,
89.876991070283,89.9944978403966),.UNSPECIFIED.);
#1307=B_SPLINE_CURVE_WITH_KNOTS('',3,(#49309,#49310,#49311,#49312,#49313,
#49314,#49315,#49316,#49317,#49318,#49319,#49320,#49321,#49322,#49323,#49324,
#49325,#49326,#49327,#49328,#49329,#49330),.UNSPECIFIED.,.F.,.F.,(4,3,3,
3,3,3,3,4),(-99.2603869768592,-98.8646901773113,-97.866056943197,-96.8674237090828,
-95.8687904749685,-94.8701572408543,-93.87152400674,-92.9772016696796),
 .UNSPECIFIED.);
#1308=B_SPLINE_CURVE_WITH_KNOTS('',3,(#49331,#49332,#49333,#49334,#49335,
#49336,#49337,#49338,#49339,#49340,#49341,#49342,#49343,#49344,#49345,#49346,
#49347,#49348,#49349,#49350,#49351,#49352),.UNSPECIFIED.,.F.,.F.,(4,3,3,
3,3,3,3,4),(89.9944978403966,90.8756243043972,91.8742575385115,92.8728907726258,
93.87152400674,94.8701572408542,95.8687904749685,96.2776831475762),
 .UNSPECIFIED.);
#1309=B_SPLINE_CURVE_WITH_KNOTS('',3,(#49357,#49358,#49359,#49360,#49361,
#49362,#49363,#49364,#49365,#49366,#49367,#49368,#49369,#49370,#49371,#49372,
#49373,#49374,#49375,#49376,#49377,#49378),.UNSPECIFIED.,.F.,.F.,(4,3,3,
3,3,3,3,4),(-105.543572284039,-104.856489581997,-103.857856347883,-102.859223113768,
-101.860589879654,-100.86195664554,-99.8633234114255,-99.2603869768592),
 .UNSPECIFIED.);
#1310=B_SPLINE_CURVE_WITH_KNOTS('',3,(#49379,#49380,#49381,#49382,#49383,
#49384,#49385,#49386,#49387,#49388,#49389,#49390,#49391,#49392,#49393,#49394,
#49395,#49396,#49397,#49398,#49399,#49400),.UNSPECIFIED.,.F.,.F.,(4,3,3,
3,3,3,3,4),(96.2776831475762,96.8674237090828,97.866056943197,98.8646901773113,
99.8633234114255,100.86195664554,101.860589879654,102.560868454756),
 .UNSPECIFIED.);
#1311=B_SPLINE_CURVE_WITH_KNOTS('',3,(#49405,#49406,#49407,#49408,#49409,
#49410,#49411,#49412,#49413,#49414,#49415,#49416,#49417,#49418,#49419,#49420,
#49421,#49422,#49423,#49424,#49425,#49426),.UNSPECIFIED.,.F.,.F.,(4,3,3,
3,3,3,3,4),(-111.826757591218,-110.848288986682,-109.849655752568,-108.851022518454,
-107.85238928434,-106.853756050225,-105.855122816111,-105.543572284039),
 .UNSPECIFIED.);
#1312=B_SPLINE_CURVE_WITH_KNOTS('',3,(#49427,#49428,#49429,#49430,#49431,
#49432,#49433,#49434,#49435,#49436,#49437,#49438,#49439,#49440,#49441,#49442,
#49443,#49444,#49445,#49446,#49447,#49448),.UNSPECIFIED.,.F.,.F.,(4,3,3,
3,3,3,3,4),(102.560868454756,102.859223113768,103.857856347883,104.856489581997,
105.855122816111,106.853756050225,107.85238928434,108.844053761935),
 .UNSPECIFIED.);
#1313=B_SPLINE_CURVE_WITH_KNOTS('',3,(#49453,#49454,#49455,#49456,#49457,
#49458,#49459,#49460,#49461,#49462,#49463,#49464,#49465,#49466,#49467,#49468,
#49469,#49470,#49471,#49472,#49473,#49474,#49475,#49476,#49477),
 .UNSPECIFIED.,.F.,.F.,(4,3,3,3,3,3,3,3,4),(-118.109942898398,-117.838721625482,
-116.840088391368,-115.841455157254,-114.842821923139,-113.844188689025,
-112.845555454911,-111.846922220797,-111.826757591218),.UNSPECIFIED.);
#1314=B_SPLINE_CURVE_WITH_KNOTS('',3,(#49478,#49479,#49480,#49481,#49482,
#49483,#49484,#49485,#49486,#49487,#49488,#49489,#49490,#49491,#49492,#49493,
#49494,#49495,#49496,#49497,#49498,#49499,#49500,#49501,#49502),
 .UNSPECIFIED.,.F.,.F.,(4,3,3,3,3,3,3,3,4),(108.844053761935,108.851022518454,
109.849655752568,110.848288986682,111.846922220797,112.845555454911,113.844188689025,
114.842821923139,115.127239069115),.UNSPECIFIED.);
#1315=B_SPLINE_CURVE_WITH_KNOTS('',3,(#49507,#49508,#49509,#49510,#49511,
#49512,#49513,#49514,#49515,#49516,#49517,#49518,#49519,#49520,#49521,#49522,
#49523,#49524,#49525,#49526,#49527,#49528),.UNSPECIFIED.,.F.,.F.,(4,3,3,
3,3,3,3,4),(-124.393128205578,-123.830521030168,-122.831887796053,-121.833254561939,
-120.834621327825,-119.835988093711,-118.837354859596,-118.109942898398),
 .UNSPECIFIED.);
#1316=B_SPLINE_CURVE_WITH_KNOTS('',3,(#49529,#49530,#49531,#49532,#49533,
#49534,#49535,#49536,#49537,#49538,#49539,#49540,#49541,#49542,#49543,#49544,
#49545,#49546,#49547,#49548,#49549,#49550),.UNSPECIFIED.,.F.,.F.,(4,3,3,
3,3,3,3,4),(115.127239069115,115.841455157254,116.840088391368,117.838721625482,
118.837354859596,119.835988093711,120.834621327825,121.410424376295),
 .UNSPECIFIED.);
#1317=B_SPLINE_CURVE_WITH_KNOTS('',3,(#49555,#49556,#49557,#49558,#49559,
#49560,#49561,#49562,#49563,#49564,#49565,#49566,#49567,#49568,#49569,#49570,
#49571,#49572,#49573,#49574,#49575,#49576),.UNSPECIFIED.,.F.,.F.,(4,3,3,
3,3,3,3,4),(-130.676313512757,-129.822320434853,-128.823687200739,-127.825053966625,
-126.82642073251,-125.827787498396,-124.829154264282,-124.393128205578),
 .UNSPECIFIED.);
#1318=B_SPLINE_CURVE_WITH_KNOTS('',3,(#49577,#49578,#49579,#49580,#49581,
#49582,#49583,#49584,#49585,#49586,#49587,#49588,#49589,#49590,#49591,#49592,
#49593,#49594,#49595,#49596,#49597,#49598),.UNSPECIFIED.,.F.,.F.,(4,3,3,
3,3,3,3,4),(121.410424376295,121.833254561939,122.831887796053,123.830521030168,
124.829154264282,125.827787498396,126.82642073251,127.693609683474),
 .UNSPECIFIED.);
#1319=B_SPLINE_CURVE_WITH_KNOTS('',3,(#49603,#49604,#49605,#49606,#49607,
#49608,#49609,#49610,#49611,#49612,#49613,#49614,#49615,#49616,#49617,#49618,
#49619,#49620,#49621,#49622,#49623,#49624,#49625,#49626,#49627),
 .UNSPECIFIED.,.F.,.F.,(4,3,3,3,3,3,3,3,4),(-136.959498819937,-136.812753073653,
-135.814119839539,-134.815486605424,-133.81685337131,-132.818220137196,
-131.819586903082,-130.820953668967,-130.676313512757),.UNSPECIFIED.);
#1320=B_SPLINE_CURVE_WITH_KNOTS('',3,(#49628,#49629,#49630,#49631,#49632,
#49633,#49634,#49635,#49636,#49637,#49638,#49639,#49640,#49641,#49642,#49643,
#49644,#49645,#49646,#49647,#49648,#49649,#49650,#49651,#49652),
 .UNSPECIFIED.,.F.,.F.,(4,3,3,3,3,3,3,3,4),(127.693609683474,127.825053966625,
128.823687200739,129.822320434853,130.820953668967,131.819586903082,132.818220137196,
133.81685337131,133.976794990654),.UNSPECIFIED.);
#1321=B_SPLINE_CURVE_WITH_KNOTS('',3,(#49659,#49660,#49661,#49662,#49663,
#49664,#49665,#49666,#49667,#49668,#49669,#49670,#49671,#49672,#49673,#49674,
#49675,#49676,#49677),.UNSPECIFIED.,.F.,.F.,(4,3,3,3,3,3,4),(-142.804552478339,
-141.805919244224,-140.80728601011,-139.808652775996,-138.810019541882,
-137.811386307767,-136.959498819937),.UNSPECIFIED.);
#1322=B_SPLINE_CURVE_WITH_KNOTS('',3,(#49678,#49679,#49680,#49681,#49682,
#49683,#49684,#49685,#49686,#49687,#49688,#49689,#49690,#49691,#49692,#49693,
#49694,#49695,#49696,#49697,#49698,#49699),.UNSPECIFIED.,.F.,.F.,(4,3,3,
3,3,3,3,4),(133.976794990654,134.815486605425,135.814119839539,136.812753073653,
137.811386307767,138.810019541882,139.808652775996,140.259980297833),
 .UNSPECIFIED.);
#1323=B_SPLINE_CURVE_WITH_KNOTS('',3,(#49705,#49706,#49707,#49708,#49709,
#49710,#49711),.UNSPECIFIED.,.F.,.F.,(4,1,1,1,4),(153.9380400259,154.78992751373,
155.788560747845,156.787193981959,157.721892086786),.UNSPECIFIED.);
#1324=B_SPLINE_CURVE_WITH_KNOTS('',3,(#49714,#49715,#49716,#49717,#49718,
#49719),.UNSPECIFIED.,.F.,.F.,(4,1,1,4),(153.9380400259,154.485345738177,
155.483978972291,156.482612206405),.UNSPECIFIED.);
#1325=B_SPLINE_CURVE_WITH_KNOTS('',3,(#49724,#49725,#49726,#49727,#49728,
#49729,#49730,#49731,#49732,#49733,#49734),.UNSPECIFIED.,.F.,.F.,(4,1,1,
1,1,1,1,1,4),(147.65485471872,147.799494874931,148.798128109045,149.796761343159,
150.795394577273,151.794027811388,152.792661045502,153.791294279616,153.9380400259),
 .UNSPECIFIED.);
#1326=B_SPLINE_CURVE_WITH_KNOTS('',3,(#49735,#49736,#49737,#49738,#49739,
#49740,#49741,#49742,#49743,#49744),.UNSPECIFIED.,.F.,.F.,(4,1,1,1,1,1,
1,4),(147.65485471872,148.493546333491,149.492179567605,150.490812801719,
151.489446035834,152.488079269948,153.486712504062,153.9380400259),
 .UNSPECIFIED.);
#1327=B_SPLINE_CURVE_WITH_KNOTS('',3,(#49749,#49750,#49751,#49752,#49753,
#49754,#49755,#49756,#49757,#49758),.UNSPECIFIED.,.F.,.F.,(4,1,1,1,1,1,
1,4),(141.371669411541,141.807695470245,142.806328704359,143.804961938474,
144.803595172588,145.802228406702,146.800861640816,147.65485471872),
 .UNSPECIFIED.);
#1328=B_SPLINE_CURVE_WITH_KNOTS('',3,(#49759,#49760,#49761,#49762,#49763,
#49764,#49765,#49766,#49767,#49768,#49769),.UNSPECIFIED.,.F.,.F.,(4,1,1,
1,1,1,1,1,4),(141.371669411541,141.503113694691,142.501746928805,143.50038016292,
144.499013397034,145.497646631148,146.496279865262,147.494913099377,147.65485471872),
 .UNSPECIFIED.);
#1329=B_SPLINE_CURVE_WITH_KNOTS('',3,(#49774,#49775,#49776,#49777,#49778,
#49779,#49780,#49781,#49782,#49783),.UNSPECIFIED.,.F.,.F.,(4,1,1,1,1,1,
1,4),(135.088484104361,135.81589606556,136.814529299674,137.813162533788,
138.811795767902,139.810429002017,140.809062236131,141.371669411541),
 .UNSPECIFIED.);
#1330=B_SPLINE_CURVE_WITH_KNOTS('',3,(#49784,#49785,#49786,#49787,#49788,
#49789,#49790,#49791,#49792,#49793),.UNSPECIFIED.,.F.,.F.,(4,1,1,1,1,1,
1,4),(135.088484104361,135.511314290006,136.50994752412,137.508580758234,
138.507213992348,139.505847226463,140.504480460577,141.371669411541),
 .UNSPECIFIED.);
#1331=B_SPLINE_CURVE_WITH_KNOTS('',3,(#49798,#49799,#49800,#49801,#49802,
#49803,#49804,#49805,#49806,#49807,#49808),.UNSPECIFIED.,.F.,.F.,(4,1,1,
1,1,1,1,1,4),(128.805298797182,128.82546342676,129.824096660874,130.822729894988,
131.821363129103,132.819996363217,133.818629597331,134.817262831445,135.088484104361),
 .UNSPECIFIED.);
#1332=B_SPLINE_CURVE_WITH_KNOTS('',3,(#49809,#49810,#49811,#49812,#49813,
#49814,#49815,#49816,#49817,#49818),.UNSPECIFIED.,.F.,.F.,(4,1,1,1,1,1,
1,4),(128.805298797182,129.51951488532,130.518148119434,131.516781353549,
132.515414587663,133.514047821777,134.512681055891,135.088484104361),
 .UNSPECIFIED.);
#1333=B_SPLINE_CURVE_WITH_KNOTS('',3,(#49823,#49824,#49825,#49826,#49827,
#49828,#49829,#49830,#49831,#49832),.UNSPECIFIED.,.F.,.F.,(4,1,1,1,1,1,
1,4),(122.522113490002,122.833664022074,123.832297256189,124.830930490303,
125.829563724417,126.828196958531,127.826830192646,128.805298797182),
 .UNSPECIFIED.);
#1334=B_SPLINE_CURVE_WITH_KNOTS('',3,(#49833,#49834,#49835,#49836,#49837,
#49838,#49839,#49840,#49841,#49842,#49843),.UNSPECIFIED.,.F.,.F.,(4,1,1,
1,1,1,1,1,4),(122.522113490002,122.52908224652,123.527715480635,124.526348714749,
125.524981948863,126.523615182977,127.522248417092,128.520881651206,128.805298797182),
 .UNSPECIFIED.);
#1335=B_SPLINE_CURVE_WITH_KNOTS('',3,(#49848,#49849,#49850,#49851,#49852,
#49853,#49854,#49855,#49856,#49857),.UNSPECIFIED.,.F.,.F.,(4,1,1,1,1,1,
1,4),(116.238928182822,116.841864617389,117.840497851503,118.839131085617,
119.837764319731,120.836397553846,121.83503078796,122.522113490002),
 .UNSPECIFIED.);
#1336=B_SPLINE_CURVE_WITH_KNOTS('',3,(#49858,#49859,#49860,#49861,#49862,
#49863,#49864,#49865,#49866,#49867),.UNSPECIFIED.,.F.,.F.,(4,1,1,1,1,1,
1,4),(116.238928182822,116.537282841835,117.535916075949,118.534549310063,
119.533182544178,120.531815778292,121.530449012406,122.522113490002),
 .UNSPECIFIED.);
#1337=B_SPLINE_CURVE_WITH_KNOTS('',3,(#49872,#49873,#49874,#49875,#49876,
#49877,#49878,#49879,#49880,#49881),.UNSPECIFIED.,.F.,.F.,(4,1,1,1,1,1,
1,4),(109.955742875643,110.850065212703,111.848698446817,112.847331680932,
113.845964915046,114.84459814916,115.843231383274,116.238928182822),
 .UNSPECIFIED.);
#1338=B_SPLINE_CURVE_WITH_KNOTS('',3,(#49882,#49883,#49884,#49885,#49886,
#49887,#49888,#49889,#49890,#49891),.UNSPECIFIED.,.F.,.F.,(4,1,1,1,1,1,
1,4),(109.955742875643,110.545483437149,111.544116671264,112.542749905378,
113.541383139492,114.540016373606,115.538649607721,116.238928182822),
 .UNSPECIFIED.);
#1339=B_SPLINE_CURVE_WITH_KNOTS('',3,(#49896,#49897,#49898,#49899,#49900,
#49901,#49902,#49903,#49904,#49905,#49906),.UNSPECIFIED.,.F.,.F.,(4,1,1,
1,1,1,1,1,4),(103.672557568463,103.859632573903,104.858265808018,105.856899042132,
106.855532276246,107.85416551036,108.852798744475,109.851431978589,109.955742875643),
 .UNSPECIFIED.);
#1340=B_SPLINE_CURVE_WITH_KNOTS('',3,(#49907,#49908,#49909,#49910,#49911,
#49912,#49913,#49914,#49915,#49916),.UNSPECIFIED.,.F.,.F.,(4,1,1,1,1,1,
1,4),(103.672557568463,104.553684032464,105.552317266578,106.550950500692,
107.549583734807,108.548216968921,109.546850203035,109.955742875643),
 .UNSPECIFIED.);
#1341=B_SPLINE_CURVE_WITH_KNOTS('',3,(#49921,#49922,#49923,#49924,#49925,
#49926,#49927,#49928,#49929,#49930),.UNSPECIFIED.,.F.,.F.,(4,1,1,1,1,1,
1,4),(97.3893722612837,97.8678331692179,98.8664664033321,99.8650996374464,
100.863732871561,101.862366105675,102.860999339789,103.672557568463),
 .UNSPECIFIED.);
#1342=B_SPLINE_CURVE_WITH_KNOTS('',3,(#49931,#49932,#49933,#49934,#49935,
#49936,#49937,#49938,#49939,#49940,#49941),.UNSPECIFIED.,.F.,.F.,(4,1,1,
1,1,1,1,1,4),(97.3893722612836,97.563251393664,98.5618846277782,99.5605178618925,
100.559151096007,101.557784330121,102.556417564235,103.555050798349,103.672557568463),
 .UNSPECIFIED.);
#1343=B_SPLINE_CURVE_WITH_KNOTS('',3,(#49946,#49947,#49948,#49949,#49950,
#49951,#49952,#49953,#49954,#49955),.UNSPECIFIED.,.F.,.F.,(4,1,1,1,1,1,
1,4),(91.1061869541041,91.8760337645324,92.8746669986466,93.8733002327609,
94.8719334668751,95.8705667009894,96.8691999351036,97.3893722612837),
 .UNSPECIFIED.);
#1344=B_SPLINE_CURVE_WITH_KNOTS('',3,(#49956,#49957,#49958,#49959,#49960,
#49961,#49962,#49963,#49964,#49965),.UNSPECIFIED.,.F.,.F.,(4,1,1,1,1,1,
1,4),(91.106186954104,91.5714519889784,92.5700852230927,93.568718457207,
94.5673516913212,95.5659849254355,96.5646181595497,97.3893722612836),
 .UNSPECIFIED.);
#1345=B_SPLINE_CURVE_WITH_KNOTS('',3,(#49970,#49971,#49972,#49973,#49974,
#49975,#49976,#49977,#49978,#49979,#49980),.UNSPECIFIED.,.F.,.F.,(4,1,1,
1,1,1,1,1,4),(84.8230016469245,84.8856011257326,85.8842343598468,86.8828675939611,
87.8815008280753,88.8801340621896,89.8787672963038,90.8774005304181,91.1061869541041),
 .UNSPECIFIED.);
#1346=B_SPLINE_CURVE_WITH_KNOTS('',3,(#49981,#49982,#49983,#49984,#49985,
#49986,#49987,#49988,#49989,#49990),.UNSPECIFIED.,.F.,.F.,(4,1,1,1,1,1,
1,4),(84.8230016469244,85.5796525842929,86.5782858184072,87.5769190525214,
88.5755522866357,89.5741855207499,90.5728187548642,91.106186954104),
 .UNSPECIFIED.);
#1347=B_SPLINE_CURVE_WITH_KNOTS('',3,(#49995,#49996,#49997,#49998,#49999,
#50000,#50001,#50002,#50003,#50004),.UNSPECIFIED.,.F.,.F.,(4,1,1,1,1,1,
1,4),(78.5398163397449,78.893801721047,79.8924349551613,80.8910681892755,
81.8897014233898,82.888334657504,83.8869678916183,84.8230016469245),
 .UNSPECIFIED.);
#1348=B_SPLINE_CURVE_WITH_KNOTS('',3,(#50005,#50006,#50007,#50008,#50009,
#50010,#50011,#50012,#50013,#50014,#50015),.UNSPECIFIED.,.F.,.F.,(4,1,1,
1,1,1,1,1,4),(78.5398163397448,78.5892199454931,79.5878531796074,80.5864864137216,
81.5851196478359,82.5837528819501,83.5823861160644,84.5810193501787,84.8230016469244),
 .UNSPECIFIED.);
#1349=B_SPLINE_CURVE_WITH_KNOTS('',3,(#50020,#50021,#50022,#50023,#50024,
#50025,#50026,#50027,#50028,#50029),.UNSPECIFIED.,.F.,.F.,(4,1,1,1,1,1,
1,4),(72.2566310325653,72.9020023163615,73.9006355504758,74.89926878459,
75.8979020187043,76.8965352528185,77.8951684869328,78.5398163397449),
 .UNSPECIFIED.);
#1350=B_SPLINE_CURVE_WITH_KNOTS('',3,(#50030,#50031,#50032,#50033,#50034,
#50035,#50036,#50037,#50038,#50039),.UNSPECIFIED.,.F.,.F.,(4,1,1,1,1,1,
1,4),(72.2566310325653,72.5974205408076,73.5960537749218,74.5946870090361,
75.5933202431503,76.5919534772646,77.5905867113789,78.5398163397448),
 .UNSPECIFIED.);
#1351=B_SPLINE_CURVE_WITH_KNOTS('',3,(#50044,#50045,#50046,#50047,#50048,
#50049,#50050,#50051,#50052,#50053),.UNSPECIFIED.,.F.,.F.,(4,1,1,1,1,1,
1,4),(65.9734457253857,66.910202911676,67.9088361457902,68.9074693799045,
69.9061026140187,70.904735848133,71.9033690822472,72.2566310325653),
 .UNSPECIFIED.);
#1352=B_SPLINE_CURVE_WITH_KNOTS('',3,(#50054,#50055,#50056,#50057,#50058,
#50059,#50060,#50061,#50062,#50063),.UNSPECIFIED.,.F.,.F.,(4,1,1,1,1,1,
1,4),(65.9734457253856,66.6056211361221,67.6042543702363,68.6028876043506,
69.6015208384648,70.6001540725791,71.5987873066933,72.2566310325653),
 .UNSPECIFIED.);
#1353=B_SPLINE_CURVE_WITH_KNOTS('',3,(#50068,#50069,#50070,#50071,#50072,
#50073,#50074,#50075,#50076,#50077,#50078),.UNSPECIFIED.,.F.,.F.,(4,1,1,
1,1,1,1,1,4),(59.6902604182061,59.9197702728762,60.9184035069904,61.9170367411047,
62.9156699752189,63.9143032093332,64.9129364434474,65.9115696775617,65.9734457253857),
 .UNSPECIFIED.);
#1354=B_SPLINE_CURVE_WITH_KNOTS('',3,(#50079,#50080,#50081,#50082,#50083,
#50084,#50085,#50086,#50087,#50088),.UNSPECIFIED.,.F.,.F.,(4,1,1,1,1,1,
1,4),(59.6902604182061,60.6138217314365,61.6124549655508,62.611088199665,
63.6097214337793,64.6083546678935,65.6069879020078,65.9734457253856),
 .UNSPECIFIED.);
#1355=B_SPLINE_CURVE_WITH_KNOTS('',3,(#50093,#50094,#50095,#50096,#50097,
#50098,#50099,#50100,#50101,#50102),.UNSPECIFIED.,.F.,.F.,(4,1,1,1,1,1,
1,4),(53.4070751110265,53.9279708681906,54.9266041023049,55.9252373364192,
56.9238705705334,57.9225038046477,58.9211370387619,59.6902604182061),
 .UNSPECIFIED.);
#1356=B_SPLINE_CURVE_WITH_KNOTS('',3,(#50103,#50104,#50105,#50106,#50107,
#50108,#50109,#50110,#50111,#50112,#50113),.UNSPECIFIED.,.F.,.F.,(4,1,1,
1,1,1,1,1,4),(53.4070751110265,53.6233890926367,54.622022326751,55.6206555608652,
56.6192887949795,57.6179220290938,58.616555263208,59.6151884973223,59.6902604182061),
 .UNSPECIFIED.);
#1357=B_SPLINE_CURVE_WITH_KNOTS('',3,(#50118,#50119,#50120,#50121,#50122,
#50123,#50124,#50125,#50126,#50127),.UNSPECIFIED.,.F.,.F.,(4,1,1,1,1,1,
1,4),(47.1238898038469,47.9361714635051,48.9348046976194,49.9334379317336,
50.9320711658479,51.9307043999621,52.9293376340764,53.4070751110265),
 .UNSPECIFIED.);
#1358=B_SPLINE_CURVE_WITH_KNOTS('',3,(#50128,#50129,#50130,#50131,#50132,
#50133,#50134,#50135,#50136,#50137),.UNSPECIFIED.,.F.,.F.,(4,1,1,1,1,1,
1,4),(47.1238898038469,47.6315896879512,48.6302229220655,49.6288561561797,
50.627489390294,51.6261226244082,52.6247558585225,53.4070751110265),
 .UNSPECIFIED.);
#1359=B_SPLINE_CURVE_WITH_KNOTS('',3,(#50142,#50143,#50144,#50145,#50146,
#50147,#50148,#50149,#50150,#50151,#50152),.UNSPECIFIED.,.F.,.F.,(4,1,1,
1,1,1,1,1,4),(40.8407044966673,40.9457388247053,41.9443720588196,42.9430052929338,
43.9416385270481,44.9402717611624,45.9389049952766,46.9375382293909,47.1238898038469),
 .UNSPECIFIED.);
#1360=B_SPLINE_CURVE_WITH_KNOTS('',3,(#50153,#50154,#50155,#50156,#50157,
#50158,#50159,#50160,#50161,#50162),.UNSPECIFIED.,.F.,.F.,(4,1,1,1,1,1,
1,4),(40.8407044966673,41.6397902832657,42.6384235173799,43.6370567514942,
44.6356899856084,45.6343232197227,46.6329564538369,47.1238898038469),
 .UNSPECIFIED.);
#1361=B_SPLINE_CURVE_WITH_KNOTS('',3,(#50167,#50168,#50169,#50170,#50171,
#50172,#50173,#50174,#50175,#50176),.UNSPECIFIED.,.F.,.F.,(4,1,1,1,1,1,
1,4),(34.5575191894877,34.9539394200198,35.9525726541341,36.9512058882483,
37.9498391223626,38.9484723564768,39.9471055905911,40.8407044966673),
 .UNSPECIFIED.);
#1362=B_SPLINE_CURVE_WITH_KNOTS('',3,(#50177,#50178,#50179,#50180,#50181,
#50182,#50183,#50184,#50185,#50186,#50187),.UNSPECIFIED.,.F.,.F.,(4,1,1,
1,1,1,1,1,4),(34.5575191894877,34.6493576444659,35.6479908785801,36.6466241126944,
37.6452573468086,38.6438905809229,39.6425238150372,40.6411570491514,40.8407044966673),
 .UNSPECIFIED.);
#1363=B_SPLINE_CURVE_WITH_KNOTS('',3,(#50192,#50193,#50194,#50195,#50196,
#50197,#50198,#50199,#50200,#50201),.UNSPECIFIED.,.F.,.F.,(4,1,1,1,1,1,
1,4),(28.2743338823081,28.9621400153343,29.9607732494485,30.9594064835628,
31.958039717677,32.9566729517913,33.9553061859055,34.5575191894877),
 .UNSPECIFIED.);
#1364=B_SPLINE_CURVE_WITH_KNOTS('',3,(#50202,#50203,#50204,#50205,#50206,
#50207,#50208,#50209,#50210,#50211),.UNSPECIFIED.,.F.,.F.,(4,1,1,1,1,1,
1,4),(28.2743338823081,28.6575582397804,29.6561914738946,30.6548247080089,
31.6534579421231,32.6520911762374,33.6507244103516,34.5575191894877),
 .UNSPECIFIED.);
#1365=B_SPLINE_CURVE_WITH_KNOTS('',3,(#50216,#50217,#50218,#50219,#50220,
#50221,#50222,#50223,#50224,#50225),.UNSPECIFIED.,.F.,.F.,(4,1,1,1,1,1,
1,4),(21.9911485751286,22.9703406106487,23.968973844763,24.9676070788772,
25.9662403129915,26.9648735471058,27.96350678122,28.2743338823081),
 .UNSPECIFIED.);
#1366=B_SPLINE_CURVE_WITH_KNOTS('',3,(#50226,#50227,#50228,#50229,#50230,
#50231,#50232,#50233,#50234,#50235),.UNSPECIFIED.,.F.,.F.,(4,1,1,1,1,1,
1,4),(21.9911485751285,22.6657588350948,23.6643920692091,24.6630253033233,
25.6616585374376,26.6602917715518,27.6589250056661,28.2743338823081),
 .UNSPECIFIED.);
#1367=B_SPLINE_CURVE_WITH_KNOTS('',3,(#50237,#50238,#50239,#50240,#50241,
#50242,#50243,#50244,#50245,#50246,#50247,#50248,#50249,#50250,#50251,#50252,
#50253,#50254,#50255,#50256,#50257,#50258,#50259,#50260,#50261,#50262,#50263,
#50264,#50265,#50266,#50267,#50268,#50269,#50270,#50271,#50272,#50273,#50274,
#50275,#50276,#50277,#50278,#50279,#50280,#50281,#50282,#50283,#50284,#50285,
#50286,#50287,#50288,#50289,#50290,#50291,#50292,#50293,#50294,#50295,#50296,
#50297,#50298,#50299,#50300,#50301,#50302,#50303),.UNSPECIFIED.,.F.,.F.,
(4,3,3,3,3,3,3,3,3,3,3,3,3,3,3,3,3,3,3,3,3,3,4),(-0.744397949170599,-0.723512326373845,
-0.67814128146552,-0.660070814808423,-0.64143235554036,-0.603511610277582,
-0.580894867390611,-0.559926333296091,-0.499651315427941,-0.461264137672083,
-0.440585195641156,-0.425519770416711,-0.378746357789259,-0.331403063065602,
-0.308554318991755,-0.284756837114195,-0.222432053558095,-0.166824040168571,
-0.151081566327468,-0.135602715089046,-0.067801357544523,-0.0036955840594098,
0.),.UNSPECIFIED.);
#1368=B_SPLINE_CURVE_WITH_KNOTS('',3,(#50306,#50307,#50308,#50309,#50310,
#50311,#50312,#50313,#50314,#50315,#50316,#50317,#50318,#50319,#50320,#50321,
#50322,#50323,#50324,#50325,#50326,#50327,#50328,#50329,#50330,#50331,#50332,
#50333,#50334,#50335,#50336,#50337,#50338,#50339,#50340,#50341,#50342,#50343,
#50344,#50345,#50346,#50347,#50348,#50349,#50350,#50351,#50352,#50353,#50354,
#50355,#50356,#50357,#50358,#50359,#50360,#50361,#50362,#50363,#50364,#50365,
#50366),.UNSPECIFIED.,.F.,.F.,(4,3,3,3,3,3,3,3,3,3,3,3,3,3,3,3,3,3,3,3,
4),(-0.741270768406385,-0.716169767752366,-0.669333551356706,-0.640523177314207,
-0.621116769028352,-0.55668187280839,-0.539299960590835,-0.476625058521356,
-0.415643967217881,-0.398597659266647,-0.383300584194447,-0.34148003658708,
-0.279262972561836,-0.262172158015018,-0.245773277293746,-0.18432995797031,
-0.134120924057982,-0.117952339761776,-0.0589761698808879,-0.00426655107714081,
0.),.UNSPECIFIED.);
#1369=B_SPLINE_CURVE_WITH_KNOTS('',3,(#50951,#50952,#50953,#50954),
 .UNSPECIFIED.,.F.,.F.,(4,4),(140.259980297833,140.743350880823),
 .UNSPECIFIED.);
#1370=B_SPLINE_CURVE_WITH_KNOTS('',3,(#50956,#50957,#50958,#50959,#50960,
#50961,#50962,#50963,#50964,#50965,#50966,#50967,#50968,#50969,#50970,#50971,
#50972,#50973,#50974,#50975,#50976,#50977,#50978,#50979,#50980,#50981,#50982,
#50983,#50984,#50985,#50986,#50987,#50988,#50989,#50990,#50991,#50992,#50993,
#50994,#50995,#50996,#50997,#50998,#50999,#51000,#51001,#51002,#51003,#51004,
#51005,#51006,#51007,#51008,#51009,#51010,#51011,#51012,#51013,#51014,#51015,
#51016,#51017,#51018,#51019,#51020,#51021,#51022),.UNSPECIFIED.,.F.,.F.,
(4,3,3,3,3,3,3,3,3,3,3,3,3,3,3,3,3,3,3,3,3,3,4),(-0.744397949170588,-0.723512326373835,
-0.678141283557063,-0.660070791965409,-0.641432356264828,-0.603511105696609,
-0.580893242636312,-0.559926125386239,-0.49965110747392,-0.461263890974675,
-0.440584493156864,-0.425519175711549,-0.378746357789258,-0.331403063065601,
-0.308554312972659,-0.284756838770636,-0.222432070198544,-0.166824052648908,
-0.151081614936169,-0.135602719887486,-0.0678013599437428,-0.00369554913725607,
0.),.UNSPECIFIED.);
#1371=B_SPLINE_CURVE_WITH_KNOTS('',3,(#51023,#51024,#51025,#51026,#51027,
#51028,#51029,#51030,#51031,#51032),.UNSPECIFIED.,.F.,.F.,(4,1,1,1,1,1,
1,4),(15.7392613255823,16.6739594304093,17.6725926645235,18.6712258986378,
19.6698591327521,20.6684923668663,21.6671256009806,21.9911485751285),
 .UNSPECIFIED.);
#1372=B_SPLINE_CURVE_WITH_KNOTS('',3,(#51035,#51036,#51037,#51038,#51039,
#51040,#51041,#51042,#51043,#51044,#51045,#51046,#51047,#51048,#51049,#51050,
#51051,#51052,#51053,#51054,#51055,#51056,#51057,#51058,#51059,#51060,#51061,
#51062,#51063,#51064,#51065,#51066,#51067,#51068,#51069,#51070,#51071,#51072,
#51073,#51074,#51075,#51076,#51077,#51078,#51079,#51080,#51081,#51082,#51083,
#51084,#51085,#51086,#51087,#51088,#51089,#51090,#51091,#51092,#51093,#51094,
#51095),.UNSPECIFIED.,.F.,.F.,(4,3,3,3,3,3,3,3,3,3,3,3,3,3,3,3,3,3,3,3,
4),(-0.741270768406348,-0.71616976775233,-0.669333551356673,-0.640523157685122,
-0.621116757431072,-0.556681858729078,-0.539299941990702,-0.476625031186337,
-0.415643911212875,-0.398597683318881,-0.383300587660851,-0.341480036587073,
-0.279263169943563,-0.262173473385454,-0.245773527378364,-0.184330145533773,
-0.134121233214564,-0.117952257539906,-0.0589761287699529,-0.00426656137973672,
0.),.UNSPECIFIED.);
#1373=B_SPLINE_CURVE_WITH_KNOTS('',3,(#51098,#51099,#51100,#51101,#51102,
#51103,#51104,#51105,#51106),.UNSPECIFIED.,.F.,.F.,(4,1,1,1,1,1,4),(16.9785412059632,
17.9771744400775,18.9758076741917,19.974440908306,20.9730741424202,21.9717073765345,
21.9911485751286),.UNSPECIFIED.);
#1526=SHAPE_REPRESENTATION_RELATIONSHIP('SRR','None',#59315,#1546);
#1546=ADVANCED_BREP_SHAPE_REPRESENTATION('',(#1593),#59202);
#1573=STYLED_ITEM('',(#59593),#1593);
#1593=MANIFOLD_SOLID_BREP('Socket head screw',#22822);
#1802=FACE_BOUND('',#5264,.T.);
#1803=FACE_BOUND('',#5273,.T.);
#1804=FACE_BOUND('',#5424,.T.);
#2238=PLANE('',#24712);
#2239=PLANE('',#24714);
#2240=PLANE('',#24722);
#2241=PLANE('',#24726);
#2242=PLANE('',#24727);
#2243=PLANE('',#24728);
#2244=PLANE('',#24729);
#2245=PLANE('',#24730);
#2246=PLANE('',#24731);
#2247=PLANE('',#24732);
#2248=PLANE('',#24733);
#2249=PLANE('',#24734);
#2250=PLANE('',#24736);
#2251=PLANE('',#24737);
#2252=PLANE('',#24739);
#2253=PLANE('',#24740);
#2254=PLANE('',#24742);
#2255=PLANE('',#24743);
#2256=PLANE('',#24745);
#2257=PLANE('',#24746);
#2258=PLANE('',#24748);
#2259=PLANE('',#24749);
#2260=PLANE('',#24751);
#2261=PLANE('',#24752);
#2262=PLANE('',#24754);
#2263=PLANE('',#24755);
#2264=PLANE('',#24757);
#2265=PLANE('',#24758);
#2266=PLANE('',#24760);
#2267=PLANE('',#24761);
#2268=PLANE('',#24763);
#2269=PLANE('',#24764);
#2270=PLANE('',#24766);
#2271=PLANE('',#24767);
#2272=PLANE('',#24769);
#2273=PLANE('',#24770);
#2274=PLANE('',#24772);
#2275=PLANE('',#24773);
#2276=PLANE('',#24775);
#2277=PLANE('',#24776);
#2278=PLANE('',#24778);
#2279=PLANE('',#24779);
#2280=PLANE('',#24781);
#2281=PLANE('',#24782);
#2282=PLANE('',#24785);
#2283=PLANE('',#24786);
#2284=PLANE('',#24789);
#2285=PLANE('',#24790);
#2286=PLANE('',#24792);
#2287=PLANE('',#24793);
#2288=PLANE('',#24795);
#2289=PLANE('',#24796);
#2290=PLANE('',#24798);
#2291=PLANE('',#24799);
#2292=PLANE('',#24801);
#2293=PLANE('',#24802);
#2294=PLANE('',#24804);
#2295=PLANE('',#24805);
#2296=PLANE('',#24807);
#2297=PLANE('',#24808);
#2298=PLANE('',#24810);
#2299=PLANE('',#24811);
#2300=PLANE('',#24813);
#2301=PLANE('',#24814);
#2302=PLANE('',#24816);
#2303=PLANE('',#24817);
#2304=PLANE('',#24819);
#2305=PLANE('',#24820);
#2306=PLANE('',#24822);
#2307=PLANE('',#24823);
#2308=PLANE('',#24825);
#2309=PLANE('',#24826);
#2310=PLANE('',#24828);
#2311=PLANE('',#24829);
#2312=PLANE('',#24831);
#2313=PLANE('',#24832);
#2314=PLANE('',#24834);
#2315=PLANE('',#24835);
#2316=PLANE('',#24837);
#2317=PLANE('',#24838);
#2318=PLANE('',#24840);
#2319=PLANE('',#24841);
#2320=PLANE('',#24843);
#2321=PLANE('',#24844);
#2322=PLANE('',#24846);
#2323=PLANE('',#24847);
#2324=PLANE('',#24849);
#2325=PLANE('',#24850);
#2326=PLANE('',#24852);
#2327=PLANE('',#24853);
#2328=PLANE('',#24855);
#2329=PLANE('',#24856);
#2330=PLANE('',#24858);
#2331=PLANE('',#24859);
#2332=PLANE('',#24861);
#2333=PLANE('',#24862);
#2334=PLANE('',#24864);
#2335=PLANE('',#24865);
#2336=PLANE('',#24867);
#2337=PLANE('',#24868);
#2338=PLANE('',#24870);
#2339=PLANE('',#24871);
#2340=PLANE('',#24873);
#2341=PLANE('',#24874);
#2342=PLANE('',#24876);
#2343=PLANE('',#24877);
#2344=PLANE('',#24879);
#2345=PLANE('',#24880);
#2346=PLANE('',#24882);
#2347=PLANE('',#24883);
#2348=PLANE('',#24885);
#2349=PLANE('',#24886);
#2350=PLANE('',#24888);
#2351=PLANE('',#24889);
#2352=PLANE('',#24891);
#2353=PLANE('',#24893);
#2354=PLANE('',#24894);
#2355=PLANE('',#24895);
#2356=PLANE('',#24897);
#2357=PLANE('',#24898);
#2358=PLANE('',#24900);
#2359=PLANE('',#24901);
#2360=PLANE('',#24903);
#2361=PLANE('',#24904);
#2362=PLANE('',#24906);
#2363=PLANE('',#24907);
#2364=PLANE('',#24909);
#2365=PLANE('',#24910);
#2366=PLANE('',#24912);
#2367=PLANE('',#24913);
#2368=PLANE('',#24915);
#2369=PLANE('',#24916);
#2370=PLANE('',#24918);
#2371=PLANE('',#24919);
#2372=PLANE('',#24921);
#2373=PLANE('',#24922);
#2374=PLANE('',#24924);
#2375=PLANE('',#24925);
#2376=PLANE('',#24927);
#2377=PLANE('',#24928);
#2378=PLANE('',#24930);
#2379=PLANE('',#24931);
#2380=PLANE('',#24933);
#2381=PLANE('',#24934);
#2382=PLANE('',#24936);
#2383=PLANE('',#24937);
#2384=PLANE('',#24939);
#2385=PLANE('',#24940);
#2386=PLANE('',#24942);
#2387=PLANE('',#24943);
#2388=PLANE('',#24945);
#2389=PLANE('',#24946);
#2390=PLANE('',#24948);
#2391=PLANE('',#24949);
#2392=PLANE('',#24951);
#2393=PLANE('',#24995);
#2589=CYLINDRICAL_SURFACE('',#24662,0.3933);
#2590=CYLINDRICAL_SURFACE('',#24666,0.3933);
#2591=CYLINDRICAL_SURFACE('',#24667,0.3933);
#2592=CYLINDRICAL_SURFACE('',#24668,0.3933);
#2593=CYLINDRICAL_SURFACE('',#24669,0.3933);
#2594=CYLINDRICAL_SURFACE('',#24670,0.3933);
#2595=CYLINDRICAL_SURFACE('',#24671,0.3933);
#2596=CYLINDRICAL_SURFACE('',#24672,0.3933);
#2597=CYLINDRICAL_SURFACE('',#24673,0.3933);
#2598=CYLINDRICAL_SURFACE('',#24674,0.3933);
#2599=CYLINDRICAL_SURFACE('',#24675,0.3933);
#2600=CYLINDRICAL_SURFACE('',#24676,0.3933);
#2601=CYLINDRICAL_SURFACE('',#24677,0.3933);
#2602=CYLINDRICAL_SURFACE('',#24678,0.3933);
#2603=CYLINDRICAL_SURFACE('',#24679,0.3933);
#2604=CYLINDRICAL_SURFACE('',#24680,0.3933);
#2605=CYLINDRICAL_SURFACE('',#24681,0.3933);
#2606=CYLINDRICAL_SURFACE('',#24682,0.3933);
#2607=CYLINDRICAL_SURFACE('',#24683,0.3933);
#2608=CYLINDRICAL_SURFACE('',#24684,0.3933);
#2609=CYLINDRICAL_SURFACE('',#24685,0.3933);
#2610=CYLINDRICAL_SURFACE('',#24686,0.3933);
#2611=CYLINDRICAL_SURFACE('',#24687,0.3933);
#2612=CYLINDRICAL_SURFACE('',#24689,0.322275);
#2613=CYLINDRICAL_SURFACE('',#24691,0.322275);
#2614=CYLINDRICAL_SURFACE('',#24692,0.322275);
#2615=CYLINDRICAL_SURFACE('',#24693,0.322275);
#2616=CYLINDRICAL_SURFACE('',#24694,0.322275);
#2617=CYLINDRICAL_SURFACE('',#24695,0.322275);
#2618=CYLINDRICAL_SURFACE('',#24696,0.322275);
#2619=CYLINDRICAL_SURFACE('',#24697,0.322275);
#2620=CYLINDRICAL_SURFACE('',#24698,0.322275);
#2621=CYLINDRICAL_SURFACE('',#24699,0.322275);
#2622=CYLINDRICAL_SURFACE('',#24700,0.322275);
#2623=CYLINDRICAL_SURFACE('',#24701,0.322275);
#2624=CYLINDRICAL_SURFACE('',#24702,0.322275);
#2625=CYLINDRICAL_SURFACE('',#24703,0.322275);
#2626=CYLINDRICAL_SURFACE('',#24704,0.322275);
#2627=CYLINDRICAL_SURFACE('',#24705,0.322275);
#2628=CYLINDRICAL_SURFACE('',#24706,0.322275);
#2629=CYLINDRICAL_SURFACE('',#24707,0.322275);
#2630=CYLINDRICAL_SURFACE('',#24708,0.322275);
#2631=CYLINDRICAL_SURFACE('',#24709,0.322275);
#2632=CYLINDRICAL_SURFACE('',#24710,0.322275);
#2633=CYLINDRICAL_SURFACE('',#24711,0.322275);
#2634=CYLINDRICAL_SURFACE('',#24716,0.322275);
#2635=CYLINDRICAL_SURFACE('',#24717,0.3933);
#2636=CYLINDRICAL_SURFACE('',#24956,0.65);
#3703=FACE_OUTER_BOUND('',#5211,.T.);
#3704=FACE_OUTER_BOUND('',#5212,.T.);
#3705=FACE_OUTER_BOUND('',#5213,.T.);
#3706=FACE_OUTER_BOUND('',#5214,.T.);
#3707=FACE_OUTER_BOUND('',#5215,.T.);
#3708=FACE_OUTER_BOUND('',#5216,.T.);
#3709=FACE_OUTER_BOUND('',#5217,.T.);
#3710=FACE_OUTER_BOUND('',#5218,.T.);
#3711=FACE_OUTER_BOUND('',#5219,.T.);
#3712=FACE_OUTER_BOUND('',#5220,.T.);
#3713=FACE_OUTER_BOUND('',#5221,.T.);
#3714=FACE_OUTER_BOUND('',#5222,.T.);
#3715=FACE_OUTER_BOUND('',#5223,.T.);
#3716=FACE_OUTER_BOUND('',#5224,.T.);
#3717=FACE_OUTER_BOUND('',#5225,.T.);
#3718=FACE_OUTER_BOUND('',#5226,.T.);
#3719=FACE_OUTER_BOUND('',#5227,.T.);
#3720=FACE_OUTER_BOUND('',#5228,.T.);
#3721=FACE_OUTER_BOUND('',#5229,.T.);
#3722=FACE_OUTER_BOUND('',#5230,.T.);
#3723=FACE_OUTER_BOUND('',#5231,.T.);
#3724=FACE_OUTER_BOUND('',#5232,.T.);
#3725=FACE_OUTER_BOUND('',#5233,.T.);
#3726=FACE_OUTER_BOUND('',#5234,.T.);
#3727=FACE_OUTER_BOUND('',#5235,.T.);
#3728=FACE_OUTER_BOUND('',#5236,.T.);
#3729=FACE_OUTER_BOUND('',#5237,.T.);
#3730=FACE_OUTER_BOUND('',#5238,.T.);
#3731=FACE_OUTER_BOUND('',#5239,.T.);
#3732=FACE_OUTER_BOUND('',#5240,.T.);
#3733=FACE_OUTER_BOUND('',#5241,.T.);
#3734=FACE_OUTER_BOUND('',#5242,.T.);
#3735=FACE_OUTER_BOUND('',#5243,.T.);
#3736=FACE_OUTER_BOUND('',#5244,.T.);
#3737=FACE_OUTER_BOUND('',#5245,.T.);
#3738=FACE_OUTER_BOUND('',#5246,.T.);
#3739=FACE_OUTER_BOUND('',#5247,.T.);
#3740=FACE_OUTER_BOUND('',#5248,.T.);
#3741=FACE_OUTER_BOUND('',#5249,.T.);
#3742=FACE_OUTER_BOUND('',#5250,.T.);
#3743=FACE_OUTER_BOUND('',#5251,.T.);
#3744=FACE_OUTER_BOUND('',#5252,.T.);
#3745=FACE_OUTER_BOUND('',#5253,.T.);
#3746=FACE_OUTER_BOUND('',#5254,.T.);
#3747=FACE_OUTER_BOUND('',#5255,.T.);
#3748=FACE_OUTER_BOUND('',#5256,.T.);
#3749=FACE_OUTER_BOUND('',#5257,.T.);
#3750=FACE_OUTER_BOUND('',#5258,.T.);
#3751=FACE_OUTER_BOUND('',#5259,.T.);
#3752=FACE_OUTER_BOUND('',#5260,.T.);
#3753=FACE_OUTER_BOUND('',#5261,.T.);
#3754=FACE_OUTER_BOUND('',#5262,.T.);
#3755=FACE_OUTER_BOUND('',#5263,.T.);
#3756=FACE_OUTER_BOUND('',#5265,.T.);
#3757=FACE_OUTER_BOUND('',#5266,.T.);
#3758=FACE_OUTER_BOUND('',#5267,.T.);
#3759=FACE_OUTER_BOUND('',#5268,.T.);
#3760=FACE_OUTER_BOUND('',#5269,.T.);
#3761=FACE_OUTER_BOUND('',#5270,.T.);
#3762=FACE_OUTER_BOUND('',#5271,.T.);
#3763=FACE_OUTER_BOUND('',#5272,.T.);
#3764=FACE_OUTER_BOUND('',#5274,.T.);
#3765=FACE_OUTER_BOUND('',#5275,.T.);
#3766=FACE_OUTER_BOUND('',#5276,.T.);
#3767=FACE_OUTER_BOUND('',#5277,.T.);
#3768=FACE_OUTER_BOUND('',#5278,.T.);
#3769=FACE_OUTER_BOUND('',#5279,.T.);
#3770=FACE_OUTER_BOUND('',#5280,.T.);
#3771=FACE_OUTER_BOUND('',#5281,.T.);
#3772=FACE_OUTER_BOUND('',#5282,.T.);
#3773=FACE_OUTER_BOUND('',#5283,.T.);
#3774=FACE_OUTER_BOUND('',#5284,.T.);
#3775=FACE_OUTER_BOUND('',#5285,.T.);
#3776=FACE_OUTER_BOUND('',#5286,.T.);
#3777=FACE_OUTER_BOUND('',#5287,.T.);
#3778=FACE_OUTER_BOUND('',#5288,.T.);
#3779=FACE_OUTER_BOUND('',#5289,.T.);
#3780=FACE_OUTER_BOUND('',#5290,.T.);
#3781=FACE_OUTER_BOUND('',#5291,.T.);
#3782=FACE_OUTER_BOUND('',#5292,.T.);
#3783=FACE_OUTER_BOUND('',#5293,.T.);
#3784=FACE_OUTER_BOUND('',#5294,.T.);
#3785=FACE_OUTER_BOUND('',#5295,.T.);
#3786=FACE_OUTER_BOUND('',#5296,.T.);
#3787=FACE_OUTER_BOUND('',#5297,.T.);
#3788=FACE_OUTER_BOUND('',#5298,.T.);
#3789=FACE_OUTER_BOUND('',#5299,.T.);
#3790=FACE_OUTER_BOUND('',#5300,.T.);
#3791=FACE_OUTER_BOUND('',#5301,.T.);
#3792=FACE_OUTER_BOUND('',#5302,.T.);
#3793=FACE_OUTER_BOUND('',#5303,.T.);
#3794=FACE_OUTER_BOUND('',#5304,.T.);
#3795=FACE_OUTER_BOUND('',#5305,.T.);
#3796=FACE_OUTER_BOUND('',#5306,.T.);
#3797=FACE_OUTER_BOUND('',#5307,.T.);
#3798=FACE_OUTER_BOUND('',#5308,.T.);
#3799=FACE_OUTER_BOUND('',#5309,.T.);
#3800=FACE_OUTER_BOUND('',#5310,.T.);
#3801=FACE_OUTER_BOUND('',#5311,.T.);
#3802=FACE_OUTER_BOUND('',#5312,.T.);
#3803=FACE_OUTER_BOUND('',#5313,.T.);
#3804=FACE_OUTER_BOUND('',#5314,.T.);
#3805=FACE_OUTER_BOUND('',#5315,.T.);
#3806=FACE_OUTER_BOUND('',#5316,.T.);
#3807=FACE_OUTER_BOUND('',#5317,.T.);
#3808=FACE_OUTER_BOUND('',#5318,.T.);
#3809=FACE_OUTER_BOUND('',#5319,.T.);
#3810=FACE_OUTER_BOUND('',#5320,.T.);
#3811=FACE_OUTER_BOUND('',#5321,.T.);
#3812=FACE_OUTER_BOUND('',#5322,.T.);
#3813=FACE_OUTER_BOUND('',#5323,.T.);
#3814=FACE_OUTER_BOUND('',#5324,.T.);
#3815=FACE_OUTER_BOUND('',#5325,.T.);
#3816=FACE_OUTER_BOUND('',#5326,.T.);
#3817=FACE_OUTER_BOUND('',#5327,.T.);
#3818=FACE_OUTER_BOUND('',#5328,.T.);
#3819=FACE_OUTER_BOUND('',#5329,.T.);
#3820=FACE_OUTER_BOUND('',#5330,.T.);
#3821=FACE_OUTER_BOUND('',#5331,.T.);
#3822=FACE_OUTER_BOUND('',#5332,.T.);
#3823=FACE_OUTER_BOUND('',#5333,.T.);
#3824=FACE_OUTER_BOUND('',#5334,.T.);
#3825=FACE_OUTER_BOUND('',#5335,.T.);
#3826=FACE_OUTER_BOUND('',#5336,.T.);
#3827=FACE_OUTER_BOUND('',#5337,.T.);
#3828=FACE_OUTER_BOUND('',#5338,.T.);
#3829=FACE_OUTER_BOUND('',#5339,.T.);
#3830=FACE_OUTER_BOUND('',#5340,.T.);
#3831=FACE_OUTER_BOUND('',#5341,.T.);
#3832=FACE_OUTER_BOUND('',#5342,.T.);
#3833=FACE_OUTER_BOUND('',#5343,.T.);
#3834=FACE_OUTER_BOUND('',#5344,.T.);
#3835=FACE_OUTER_BOUND('',#5345,.T.);
#3836=FACE_OUTER_BOUND('',#5346,.T.);
#3837=FACE_OUTER_BOUND('',#5347,.T.);
#3838=FACE_OUTER_BOUND('',#5348,.T.);
#3839=FACE_OUTER_BOUND('',#5349,.T.);
#3840=FACE_OUTER_BOUND('',#5350,.T.);
#3841=FACE_OUTER_BOUND('',#5351,.T.);
#3842=FACE_OUTER_BOUND('',#5352,.T.);
#3843=FACE_OUTER_BOUND('',#5353,.T.);
#3844=FACE_OUTER_BOUND('',#5354,.T.);
#3845=FACE_OUTER_BOUND('',#5355,.T.);
#3846=FACE_OUTER_BOUND('',#5356,.T.);
#3847=FACE_OUTER_BOUND('',#5357,.T.);
#3848=FACE_OUTER_BOUND('',#5358,.T.);
#3849=FACE_OUTER_BOUND('',#5359,.T.);
#3850=FACE_OUTER_BOUND('',#5360,.T.);
#3851=FACE_OUTER_BOUND('',#5361,.T.);
#3852=FACE_OUTER_BOUND('',#5362,.T.);
#3853=FACE_OUTER_BOUND('',#5363,.T.);
#3854=FACE_OUTER_BOUND('',#5364,.T.);
#3855=FACE_OUTER_BOUND('',#5365,.T.);
#3856=FACE_OUTER_BOUND('',#5366,.T.);
#3857=FACE_OUTER_BOUND('',#5367,.T.);
#3858=FACE_OUTER_BOUND('',#5368,.T.);
#3859=FACE_OUTER_BOUND('',#5369,.T.);
#3860=FACE_OUTER_BOUND('',#5370,.T.);
#3861=FACE_OUTER_BOUND('',#5371,.T.);
#3862=FACE_OUTER_BOUND('',#5372,.T.);
#3863=FACE_OUTER_BOUND('',#5373,.T.);
#3864=FACE_OUTER_BOUND('',#5374,.T.);
#3865=FACE_OUTER_BOUND('',#5375,.T.);
#3866=FACE_OUTER_BOUND('',#5376,.T.);
#3867=FACE_OUTER_BOUND('',#5377,.T.);
#3868=FACE_OUTER_BOUND('',#5378,.T.);
#3869=FACE_OUTER_BOUND('',#5379,.T.);
#3870=FACE_OUTER_BOUND('',#5380,.T.);
#3871=FACE_OUTER_BOUND('',#5381,.T.);
#3872=FACE_OUTER_BOUND('',#5382,.T.);
#3873=FACE_OUTER_BOUND('',#5383,.T.);
#3874=FACE_OUTER_BOUND('',#5384,.T.);
#3875=FACE_OUTER_BOUND('',#5385,.T.);
#3876=FACE_OUTER_BOUND('',#5386,.T.);
#3877=FACE_OUTER_BOUND('',#5387,.T.);
#3878=FACE_OUTER_BOUND('',#5388,.T.);
#3879=FACE_OUTER_BOUND('',#5389,.T.);
#3880=FACE_OUTER_BOUND('',#5390,.T.);
#3881=FACE_OUTER_BOUND('',#5391,.T.);
#3882=FACE_OUTER_BOUND('',#5392,.T.);
#3883=FACE_OUTER_BOUND('',#5393,.T.);
#3884=FACE_OUTER_BOUND('',#5394,.T.);
#3885=FACE_OUTER_BOUND('',#5395,.T.);
#3886=FACE_OUTER_BOUND('',#5396,.T.);
#3887=FACE_OUTER_BOUND('',#5397,.T.);
#3888=FACE_OUTER_BOUND('',#5398,.T.);
#3889=FACE_OUTER_BOUND('',#5399,.T.);
#3890=FACE_OUTER_BOUND('',#5400,.T.);
#3891=FACE_OUTER_BOUND('',#5401,.T.);
#3892=FACE_OUTER_BOUND('',#5402,.T.);
#3893=FACE_OUTER_BOUND('',#5403,.T.);
#3894=FACE_OUTER_BOUND('',#5404,.T.);
#3895=FACE_OUTER_BOUND('',#5405,.T.);
#3896=FACE_OUTER_BOUND('',#5406,.T.);
#3897=FACE_OUTER_BOUND('',#5407,.T.);
#3898=FACE_OUTER_BOUND('',#5408,.T.);
#3899=FACE_OUTER_BOUND('',#5409,.T.);
#3900=FACE_OUTER_BOUND('',#5410,.T.);
#3901=FACE_OUTER_BOUND('',#5411,.T.);
#3902=FACE_OUTER_BOUND('',#5412,.T.);
#3903=FACE_OUTER_BOUND('',#5413,.T.);
#3904=FACE_OUTER_BOUND('',#5414,.T.);
#3905=FACE_OUTER_BOUND('',#5415,.T.);
#3906=FACE_OUTER_BOUND('',#5416,.T.);
#3907=FACE_OUTER_BOUND('',#5417,.T.);
#3908=FACE_OUTER_BOUND('',#5418,.T.);
#3909=FACE_OUTER_BOUND('',#5419,.T.);
#3910=FACE_OUTER_BOUND('',#5420,.T.);
#3911=FACE_OUTER_BOUND('',#5421,.T.);
#3912=FACE_OUTER_BOUND('',#5422,.T.);
#3913=FACE_OUTER_BOUND('',#5423,.T.);
#5211=EDGE_LOOP('',(#19922,#19923,#19924,#19925,#19926,#19927,#19928,#19929));
#5212=EDGE_LOOP('',(#19930,#19931,#19932,#19933));
#5213=EDGE_LOOP('',(#19934,#19935,#19936,#19937));
#5214=EDGE_LOOP('',(#19938,#19939,#19940,#19941));
#5215=EDGE_LOOP('',(#19942,#19943,#19944,#19945));
#5216=EDGE_LOOP('',(#19946,#19947,#19948,#19949));
#5217=EDGE_LOOP('',(#19950,#19951,#19952,#19953));
#5218=EDGE_LOOP('',(#19954,#19955,#19956,#19957));
#5219=EDGE_LOOP('',(#19958,#19959,#19960,#19961));
#5220=EDGE_LOOP('',(#19962,#19963,#19964,#19965));
#5221=EDGE_LOOP('',(#19966,#19967,#19968,#19969));
#5222=EDGE_LOOP('',(#19970,#19971,#19972,#19973));
#5223=EDGE_LOOP('',(#19974,#19975,#19976,#19977));
#5224=EDGE_LOOP('',(#19978,#19979,#19980,#19981));
#5225=EDGE_LOOP('',(#19982,#19983,#19984,#19985));
#5226=EDGE_LOOP('',(#19986,#19987,#19988,#19989));
#5227=EDGE_LOOP('',(#19990,#19991,#19992,#19993));
#5228=EDGE_LOOP('',(#19994,#19995,#19996,#19997));
#5229=EDGE_LOOP('',(#19998,#19999,#20000,#20001));
#5230=EDGE_LOOP('',(#20002,#20003,#20004,#20005));
#5231=EDGE_LOOP('',(#20006,#20007,#20008,#20009));
#5232=EDGE_LOOP('',(#20010,#20011,#20012,#20013));
#5233=EDGE_LOOP('',(#20014,#20015,#20016,#20017,#20018));
#5234=EDGE_LOOP('',(#20019,#20020,#20021,#20022));
#5235=EDGE_LOOP('',(#20023,#20024,#20025,#20026));
#5236=EDGE_LOOP('',(#20027,#20028,#20029,#20030));
#5237=EDGE_LOOP('',(#20031,#20032,#20033,#20034));
#5238=EDGE_LOOP('',(#20035,#20036,#20037,#20038));
#5239=EDGE_LOOP('',(#20039,#20040,#20041,#20042));
#5240=EDGE_LOOP('',(#20043,#20044,#20045,#20046));
#5241=EDGE_LOOP('',(#20047,#20048,#20049,#20050));
#5242=EDGE_LOOP('',(#20051,#20052,#20053,#20054));
#5243=EDGE_LOOP('',(#20055,#20056,#20057,#20058));
#5244=EDGE_LOOP('',(#20059,#20060,#20061,#20062));
#5245=EDGE_LOOP('',(#20063,#20064,#20065,#20066));
#5246=EDGE_LOOP('',(#20067,#20068,#20069,#20070));
#5247=EDGE_LOOP('',(#20071,#20072,#20073,#20074));
#5248=EDGE_LOOP('',(#20075,#20076,#20077,#20078));
#5249=EDGE_LOOP('',(#20079,#20080,#20081,#20082));
#5250=EDGE_LOOP('',(#20083,#20084,#20085,#20086));
#5251=EDGE_LOOP('',(#20087,#20088,#20089,#20090));
#5252=EDGE_LOOP('',(#20091,#20092,#20093,#20094));
#5253=EDGE_LOOP('',(#20095,#20096,#20097,#20098));
#5254=EDGE_LOOP('',(#20099,#20100,#20101,#20102));
#5255=EDGE_LOOP('',(#20103,#20104,#20105,#20106));
#5256=EDGE_LOOP('',(#20107,#20108,#20109,#20110));
#5257=EDGE_LOOP('',(#20111,#20112,#20113,#20114,#20115,#20116,#20117,#20118,
#20119,#20120,#20121,#20122,#20123,#20124,#20125,#20126,#20127,#20128,#20129,
#20130,#20131,#20132,#20133,#20134,#20135,#20136,#20137,#20138,#20139,#20140,
#20141,#20142,#20143,#20144,#20145,#20146,#20147,#20148,#20149,#20150,#20151,
#20152,#20153,#20154,#20155,#20156,#20157,#20158,#20159));
#5258=EDGE_LOOP('',(#20160,#20161,#20162,#20163,#20164));
#5259=EDGE_LOOP('',(#20165,#20166,#20167,#20168));
#5260=EDGE_LOOP('',(#20169,#20170,#20171,#20172,#20173,#20174,#20175,#20176,
#20177,#20178,#20179,#20180,#20181,#20182,#20183,#20184,#20185,#20186,#20187,
#20188,#20189,#20190,#20191,#20192,#20193,#20194,#20195,#20196,#20197,#20198,
#20199,#20200,#20201,#20202,#20203,#20204,#20205,#20206,#20207,#20208,#20209,
#20210,#20211,#20212,#20213,#20214,#20215,#20216));
#5261=EDGE_LOOP('',(#20217,#20218,#20219));
#5262=EDGE_LOOP('',(#20220,#20221,#20222,#20223,#20224,#20225));
#5263=EDGE_LOOP('',(#20226));
#5264=EDGE_LOOP('',(#20227));
#5265=EDGE_LOOP('',(#20228,#20229,#20230));
#5266=EDGE_LOOP('',(#20231,#20232,#20233,#20234));
#5267=EDGE_LOOP('',(#20235,#20236,#20237,#20238));
#5268=EDGE_LOOP('',(#20239,#20240,#20241,#20242));
#5269=EDGE_LOOP('',(#20243,#20244,#20245,#20246));
#5270=EDGE_LOOP('',(#20247,#20248,#20249,#20250));
#5271=EDGE_LOOP('',(#20251,#20252,#20253,#20254));
#5272=EDGE_LOOP('',(#20255,#20256,#20257,#20258,#20259,#20260));
#5273=EDGE_LOOP('',(#20261));
#5274=EDGE_LOOP('',(#20262,#20263,#20264,#20265));
#5275=EDGE_LOOP('',(#20266,#20267,#20268));
#5276=EDGE_LOOP('',(#20269,#20270,#20271,#20272));
#5277=EDGE_LOOP('',(#20273,#20274,#20275));
#5278=EDGE_LOOP('',(#20276,#20277,#20278,#20279));
#5279=EDGE_LOOP('',(#20280,#20281,#20282));
#5280=EDGE_LOOP('',(#20283,#20284,#20285,#20286));
#5281=EDGE_LOOP('',(#20287,#20288,#20289));
#5282=EDGE_LOOP('',(#20290,#20291,#20292,#20293));
#5283=EDGE_LOOP('',(#20294,#20295,#20296));
#5284=EDGE_LOOP('',(#20297,#20298,#20299,#20300));
#5285=EDGE_LOOP('',(#20301,#20302,#20303));
#5286=EDGE_LOOP('',(#20304,#20305,#20306,#20307));
#5287=EDGE_LOOP('',(#20308,#20309,#20310));
#5288=EDGE_LOOP('',(#20311,#20312,#20313,#20314));
#5289=EDGE_LOOP('',(#20315,#20316,#20317));
#5290=EDGE_LOOP('',(#20318,#20319,#20320,#20321));
#5291=EDGE_LOOP('',(#20322,#20323,#20324));
#5292=EDGE_LOOP('',(#20325,#20326,#20327,#20328));
#5293=EDGE_LOOP('',(#20329,#20330,#20331));
#5294=EDGE_LOOP('',(#20332,#20333,#20334,#20335));
#5295=EDGE_LOOP('',(#20336,#20337,#20338));
#5296=EDGE_LOOP('',(#20339,#20340,#20341,#20342));
#5297=EDGE_LOOP('',(#20343,#20344,#20345));
#5298=EDGE_LOOP('',(#20346,#20347,#20348,#20349));
#5299=EDGE_LOOP('',(#20350,#20351,#20352));
#5300=EDGE_LOOP('',(#20353,#20354,#20355,#20356));
#5301=EDGE_LOOP('',(#20357,#20358,#20359));
#5302=EDGE_LOOP('',(#20360,#20361,#20362,#20363));
#5303=EDGE_LOOP('',(#20364,#20365,#20366));
#5304=EDGE_LOOP('',(#20367,#20368,#20369,#20370));
#5305=EDGE_LOOP('',(#20371,#20372,#20373));
#5306=EDGE_LOOP('',(#20374,#20375,#20376,#20377));
#5307=EDGE_LOOP('',(#20378,#20379,#20380,#20381));
#5308=EDGE_LOOP('',(#20382,#20383,#20384,#20385));
#5309=EDGE_LOOP('',(#20386,#20387,#20388,#20389));
#5310=EDGE_LOOP('',(#20390,#20391,#20392,#20393));
#5311=EDGE_LOOP('',(#20394,#20395,#20396));
#5312=EDGE_LOOP('',(#20397,#20398,#20399,#20400));
#5313=EDGE_LOOP('',(#20401,#20402,#20403));
#5314=EDGE_LOOP('',(#20404,#20405,#20406,#20407));
#5315=EDGE_LOOP('',(#20408,#20409,#20410));
#5316=EDGE_LOOP('',(#20411,#20412,#20413,#20414));
#5317=EDGE_LOOP('',(#20415,#20416,#20417));
#5318=EDGE_LOOP('',(#20418,#20419,#20420,#20421));
#5319=EDGE_LOOP('',(#20422,#20423,#20424));
#5320=EDGE_LOOP('',(#20425,#20426,#20427,#20428));
#5321=EDGE_LOOP('',(#20429,#20430,#20431));
#5322=EDGE_LOOP('',(#20432,#20433,#20434,#20435));
#5323=EDGE_LOOP('',(#20436,#20437,#20438));
#5324=EDGE_LOOP('',(#20439,#20440,#20441,#20442));
#5325=EDGE_LOOP('',(#20443,#20444,#20445));
#5326=EDGE_LOOP('',(#20446,#20447,#20448,#20449));
#5327=EDGE_LOOP('',(#20450,#20451,#20452));
#5328=EDGE_LOOP('',(#20453,#20454,#20455,#20456));
#5329=EDGE_LOOP('',(#20457,#20458,#20459));
#5330=EDGE_LOOP('',(#20460,#20461,#20462,#20463));
#5331=EDGE_LOOP('',(#20464,#20465,#20466));
#5332=EDGE_LOOP('',(#20467,#20468,#20469,#20470));
#5333=EDGE_LOOP('',(#20471,#20472,#20473));
#5334=EDGE_LOOP('',(#20474,#20475,#20476,#20477));
#5335=EDGE_LOOP('',(#20478,#20479,#20480));
#5336=EDGE_LOOP('',(#20481,#20482,#20483,#20484));
#5337=EDGE_LOOP('',(#20485,#20486,#20487));
#5338=EDGE_LOOP('',(#20488,#20489,#20490,#20491));
#5339=EDGE_LOOP('',(#20492,#20493,#20494));
#5340=EDGE_LOOP('',(#20495,#20496,#20497,#20498));
#5341=EDGE_LOOP('',(#20499,#20500,#20501));
#5342=EDGE_LOOP('',(#20502,#20503,#20504,#20505));
#5343=EDGE_LOOP('',(#20506,#20507,#20508));
#5344=EDGE_LOOP('',(#20509,#20510,#20511,#20512));
#5345=EDGE_LOOP('',(#20513,#20514,#20515));
#5346=EDGE_LOOP('',(#20516,#20517,#20518,#20519));
#5347=EDGE_LOOP('',(#20520,#20521,#20522));
#5348=EDGE_LOOP('',(#20523,#20524,#20525,#20526));
#5349=EDGE_LOOP('',(#20527,#20528,#20529));
#5350=EDGE_LOOP('',(#20530,#20531,#20532,#20533));
#5351=EDGE_LOOP('',(#20534,#20535,#20536));
#5352=EDGE_LOOP('',(#20537,#20538,#20539,#20540));
#5353=EDGE_LOOP('',(#20541,#20542,#20543));
#5354=EDGE_LOOP('',(#20544,#20545,#20546,#20547));
#5355=EDGE_LOOP('',(#20548,#20549,#20550));
#5356=EDGE_LOOP('',(#20551,#20552,#20553,#20554));
#5357=EDGE_LOOP('',(#20555,#20556,#20557));
#5358=EDGE_LOOP('',(#20558,#20559,#20560,#20561));
#5359=EDGE_LOOP('',(#20562,#20563,#20564));
#5360=EDGE_LOOP('',(#20565,#20566,#20567,#20568));
#5361=EDGE_LOOP('',(#20569,#20570,#20571));
#5362=EDGE_LOOP('',(#20572,#20573,#20574,#20575));
#5363=EDGE_LOOP('',(#20576,#20577,#20578));
#5364=EDGE_LOOP('',(#20579,#20580,#20581,#20582));
#5365=EDGE_LOOP('',(#20583,#20584,#20585));
#5366=EDGE_LOOP('',(#20586,#20587,#20588,#20589));
#5367=EDGE_LOOP('',(#20590,#20591,#20592));
#5368=EDGE_LOOP('',(#20593,#20594,#20595,#20596));
#5369=EDGE_LOOP('',(#20597,#20598,#20599));
#5370=EDGE_LOOP('',(#20600,#20601,#20602,#20603));
#5371=EDGE_LOOP('',(#20604,#20605,#20606));
#5372=EDGE_LOOP('',(#20607,#20608,#20609,#20610));
#5373=EDGE_LOOP('',(#20611,#20612,#20613));
#5374=EDGE_LOOP('',(#20614,#20615,#20616,#20617));
#5375=EDGE_LOOP('',(#20618,#20619,#20620));
#5376=EDGE_LOOP('',(#20621,#20622,#20623,#20624));
#5377=EDGE_LOOP('',(#20625,#20626,#20627));
#5378=EDGE_LOOP('',(#20628,#20629,#20630));
#5379=EDGE_LOOP('',(#20631,#20632,#20633,#20634));
#5380=EDGE_LOOP('',(#20635,#20636,#20637,#20638));
#5381=EDGE_LOOP('',(#20639,#20640,#20641));
#5382=EDGE_LOOP('',(#20642,#20643,#20644,#20645));
#5383=EDGE_LOOP('',(#20646,#20647,#20648));
#5384=EDGE_LOOP('',(#20649,#20650,#20651,#20652));
#5385=EDGE_LOOP('',(#20653,#20654,#20655));
#5386=EDGE_LOOP('',(#20656,#20657,#20658,#20659));
#5387=EDGE_LOOP('',(#20660,#20661,#20662));
#5388=EDGE_LOOP('',(#20663,#20664,#20665,#20666));
#5389=EDGE_LOOP('',(#20667,#20668,#20669));
#5390=EDGE_LOOP('',(#20670,#20671,#20672,#20673));
#5391=EDGE_LOOP('',(#20674,#20675,#20676));
#5392=EDGE_LOOP('',(#20677,#20678,#20679,#20680));
#5393=EDGE_LOOP('',(#20681,#20682,#20683));
#5394=EDGE_LOOP('',(#20684,#20685,#20686,#20687));
#5395=EDGE_LOOP('',(#20688,#20689,#20690));
#5396=EDGE_LOOP('',(#20691,#20692,#20693,#20694));
#5397=EDGE_LOOP('',(#20695,#20696,#20697));
#5398=EDGE_LOOP('',(#20698,#20699,#20700,#20701));
#5399=EDGE_LOOP('',(#20702,#20703,#20704));
#5400=EDGE_LOOP('',(#20705,#20706,#20707,#20708));
#5401=EDGE_LOOP('',(#20709,#20710,#20711));
#5402=EDGE_LOOP('',(#20712,#20713,#20714,#20715));
#5403=EDGE_LOOP('',(#20716,#20717,#20718));
#5404=EDGE_LOOP('',(#20719,#20720,#20721,#20722));
#5405=EDGE_LOOP('',(#20723,#20724,#20725));
#5406=EDGE_LOOP('',(#20726,#20727,#20728,#20729));
#5407=EDGE_LOOP('',(#20730,#20731,#20732));
#5408=EDGE_LOOP('',(#20733,#20734,#20735,#20736));
#5409=EDGE_LOOP('',(#20737,#20738,#20739));
#5410=EDGE_LOOP('',(#20740,#20741,#20742,#20743));
#5411=EDGE_LOOP('',(#20744,#20745,#20746));
#5412=EDGE_LOOP('',(#20747,#20748,#20749,#20750));
#5413=EDGE_LOOP('',(#20751,#20752,#20753));
#5414=EDGE_LOOP('',(#20754,#20755,#20756,#20757));
#5415=EDGE_LOOP('',(#20758,#20759,#20760));
#5416=EDGE_LOOP('',(#20761,#20762,#20763,#20764));
#5417=EDGE_LOOP('',(#20765,#20766,#20767));
#5418=EDGE_LOOP('',(#20768));
#5419=EDGE_LOOP('',(#20769,#20770,#20771,#20772));
#5420=EDGE_LOOP('',(#20773,#20774,#20775,#20776));
#5421=EDGE_LOOP('',(#20777,#20778,#20779,#20780,#20781,#20782,#20783,#20784,
#20785,#20786,#20787,#20788,#20789,#20790,#20791,#20792,#20793,#20794,#20795,
#20796,#20797,#20798,#20799,#20800,#20801,#20802,#20803,#20804,#20805,#20806,
#20807,#20808,#20809,#20810,#20811,#20812,#20813,#20814,#20815,#20816,#20817,
#20818,#20819,#20820,#20821,#20822,#20823,#20824,#20825,#20826,#20827,#20828,
#20829,#20830,#20831,#20832,#20833,#20834,#20835,#20836,#20837,#20838,#20839,
#20840,#20841,#20842,#20843,#20844,#20845,#20846,#20847,#20848,#20849,#20850,
#20851,#20852,#20853,#20854,#20855,#20856,#20857,#20858,#20859,#20860,#20861,
#20862,#20863,#20864,#20865,#20866,#20867,#20868,#20869,#20870,#20871,#20872,
#20873,#20874,#20875,#20876,#20877,#20878,#20879,#20880,#20881,#20882,#20883,
#20884,#20885,#20886,#20887,#20888,#20889,#20890,#20891,#20892,#20893,#20894,
#20895,#20896,#20897,#20898,#20899,#20900,#20901,#20902,#20903,#20904,#20905,
#20906,#20907,#20908,#20909,#20910,#20911,#20912,#20913,#20914,#20915,#20916,
#20917,#20918,#20919,#20920,#20921,#20922,#20923,#20924));
#5422=EDGE_LOOP('',(#20925,#20926,#20927,#20928,#20929,#20930,#20931,#20932,
#20933,#20934,#20935,#20936,#20937,#20938,#20939,#20940,#20941,#20942,#20943,
#20944,#20945,#20946,#20947,#20948,#20949,#20950,#20951,#20952,#20953,#20954,
#20955,#20956,#20957,#20958,#20959,#20960,#20961,#20962,#20963,#20964,#20965,
#20966,#20967,#20968,#20969,#20970,#20971,#20972,#20973,#20974,#20975,#20976,
#20977,#20978,#20979,#20980,#20981,#20982,#20983,#20984,#20985,#20986,#20987,
#20988,#20989,#20990,#20991,#20992,#20993,#20994,#20995,#20996,#20997,#20998,
#20999,#21000));
#5423=EDGE_LOOP('',(#21001));
#5424=EDGE_LOOP('',(#21002,#21003,#21004,#21005,#21006,#21007));
#6562=LINE('',#48577,#7995);
#6563=LINE('',#48595,#7996);
#6564=LINE('',#48612,#7997);
#6565=LINE('',#48660,#7998);
#6566=LINE('',#48708,#7999);
#6567=LINE('',#48756,#8000);
#6568=LINE('',#48810,#8001);
#6569=LINE('',#48858,#8002);
#6570=LINE('',#48906,#8003);
#6571=LINE('',#48960,#8004);
#6572=LINE('',#49008,#8005);
#6573=LINE('',#49056,#8006);
#6574=LINE('',#49104,#8007);
#6575=LINE('',#49158,#8008);
#6576=LINE('',#49206,#8009);
#6577=LINE('',#49254,#8010);
#6578=LINE('',#49308,#8011);
#6579=LINE('',#49356,#8012);
#6580=LINE('',#49404,#8013);
#6581=LINE('',#49452,#8014);
#6582=LINE('',#49506,#8015);
#6583=LINE('',#49554,#8016);
#6584=LINE('',#49602,#8017);
#6585=LINE('',#49656,#8018);
#6586=LINE('',#49703,#8019);
#6587=LINE('',#49723,#8020);
#6588=LINE('',#49748,#8021);
#6589=LINE('',#49773,#8022);
#6590=LINE('',#49797,#8023);
#6591=LINE('',#49822,#8024);
#6592=LINE('',#49847,#8025);
#6593=LINE('',#49871,#8026);
#6594=LINE('',#49895,#8027);
#6595=LINE('',#49920,#8028);
#6596=LINE('',#49945,#8029);
#6597=LINE('',#49969,#8030);
#6598=LINE('',#49994,#8031);
#6599=LINE('',#50019,#8032);
#6600=LINE('',#50043,#8033);
#6601=LINE('',#50067,#8034);
#6602=LINE('',#50092,#8035);
#6603=LINE('',#50117,#8036);
#6604=LINE('',#50141,#8037);
#6605=LINE('',#50166,#8038);
#6606=LINE('',#50191,#8039);
#6607=LINE('',#50215,#8040);
#6608=LINE('',#51703,#8041);
#6609=LINE('',#51708,#8042);
#6610=LINE('',#51710,#8043);
#6611=LINE('',#51712,#8044);
#6612=LINE('',#51713,#8045);
#6613=LINE('',#51716,#8046);
#6614=LINE('',#51718,#8047);
#6615=LINE('',#51719,#8048);
#6616=LINE('',#51722,#8049);
#6617=LINE('',#51724,#8050);
#6618=LINE('',#51725,#8051);
#6619=LINE('',#51728,#8052);
#6620=LINE('',#51730,#8053);
#6621=LINE('',#51731,#8054);
#6622=LINE('',#51734,#8055);
#6623=LINE('',#51736,#8056);
#6624=LINE('',#51737,#8057);
#6625=LINE('',#51739,#8058);
#6626=LINE('',#51740,#8059);
#6627=LINE('',#51745,#8060);
#6628=LINE('',#51747,#8061);
#6629=LINE('',#51749,#8062);
#6630=LINE('',#51750,#8063);
#6631=LINE('',#51754,#8064);
#6632=LINE('',#51757,#8065);
#6633=LINE('',#51758,#8066);
#6634=LINE('',#51764,#8067);
#6635=LINE('',#51766,#8068);
#6636=LINE('',#51768,#8069);
#6637=LINE('',#51769,#8070);
#6638=LINE('',#51773,#8071);
#6639=LINE('',#51776,#8072);
#6640=LINE('',#51777,#8073);
#6641=LINE('',#51783,#8074);
#6642=LINE('',#51785,#8075);
#6643=LINE('',#51787,#8076);
#6644=LINE('',#51788,#8077);
#6645=LINE('',#51792,#8078);
#6646=LINE('',#51795,#8079);
#6647=LINE('',#51796,#8080);
#6648=LINE('',#51802,#8081);
#6649=LINE('',#51804,#8082);
#6650=LINE('',#51806,#8083);
#6651=LINE('',#51807,#8084);
#6652=LINE('',#51811,#8085);
#6653=LINE('',#51814,#8086);
#6654=LINE('',#51815,#8087);
#6655=LINE('',#51821,#8088);
#6656=LINE('',#51823,#8089);
#6657=LINE('',#51825,#8090);
#6658=LINE('',#51826,#8091);
#6659=LINE('',#51830,#8092);
#6660=LINE('',#51833,#8093);
#6661=LINE('',#51834,#8094);
#6662=LINE('',#51840,#8095);
#6663=LINE('',#51842,#8096);
#6664=LINE('',#51844,#8097);
#6665=LINE('',#51845,#8098);
#6666=LINE('',#51849,#8099);
#6667=LINE('',#51852,#8100);
#6668=LINE('',#51853,#8101);
#6669=LINE('',#51859,#8102);
#6670=LINE('',#51861,#8103);
#6671=LINE('',#51863,#8104);
#6672=LINE('',#51864,#8105);
#6673=LINE('',#51868,#8106);
#6674=LINE('',#51871,#8107);
#6675=LINE('',#51872,#8108);
#6676=LINE('',#51878,#8109);
#6677=LINE('',#51880,#8110);
#6678=LINE('',#51882,#8111);
#6679=LINE('',#51883,#8112);
#6680=LINE('',#51887,#8113);
#6681=LINE('',#51890,#8114);
#6682=LINE('',#51891,#8115);
#6683=LINE('',#51897,#8116);
#6684=LINE('',#51899,#8117);
#6685=LINE('',#51901,#8118);
#6686=LINE('',#51902,#8119);
#6687=LINE('',#51907,#8120);
#6688=LINE('',#51911,#8121);
#6689=LINE('',#51912,#8122);
#6690=LINE('',#51920,#8123);
#6691=LINE('',#51922,#8124);
#6692=LINE('',#51924,#8125);
#6693=LINE('',#51925,#8126);
#6694=LINE('',#51929,#8127);
#6695=LINE('',#51932,#8128);
#6696=LINE('',#51933,#8129);
#6697=LINE('',#51939,#8130);
#6698=LINE('',#51941,#8131);
#6699=LINE('',#51943,#8132);
#6700=LINE('',#51944,#8133);
#6701=LINE('',#51948,#8134);
#6702=LINE('',#51951,#8135);
#6703=LINE('',#51952,#8136);
#6704=LINE('',#51958,#8137);
#6705=LINE('',#51960,#8138);
#6706=LINE('',#51962,#8139);
#6707=LINE('',#51963,#8140);
#6708=LINE('',#51967,#8141);
#6709=LINE('',#51970,#8142);
#6710=LINE('',#51971,#8143);
#6711=LINE('',#51977,#8144);
#6712=LINE('',#51979,#8145);
#6713=LINE('',#51981,#8146);
#6714=LINE('',#51982,#8147);
#6715=LINE('',#51986,#8148);
#6716=LINE('',#51989,#8149);
#6717=LINE('',#51990,#8150);
#6718=LINE('',#51996,#8151);
#6719=LINE('',#51998,#8152);
#6720=LINE('',#52000,#8153);
#6721=LINE('',#52001,#8154);
#6722=LINE('',#52005,#8155);
#6723=LINE('',#52008,#8156);
#6724=LINE('',#52009,#8157);
#6725=LINE('',#52015,#8158);
#6726=LINE('',#52017,#8159);
#6727=LINE('',#52019,#8160);
#6728=LINE('',#52020,#8161);
#6729=LINE('',#52024,#8162);
#6730=LINE('',#52027,#8163);
#6731=LINE('',#52028,#8164);
#6732=LINE('',#52034,#8165);
#6733=LINE('',#52036,#8166);
#6734=LINE('',#52038,#8167);
#6735=LINE('',#52039,#8168);
#6736=LINE('',#52043,#8169);
#6737=LINE('',#52046,#8170);
#6738=LINE('',#52047,#8171);
#6739=LINE('',#52053,#8172);
#6740=LINE('',#52055,#8173);
#6741=LINE('',#52057,#8174);
#6742=LINE('',#52058,#8175);
#6743=LINE('',#52062,#8176);
#6744=LINE('',#52065,#8177);
#6745=LINE('',#52066,#8178);
#6746=LINE('',#52072,#8179);
#6747=LINE('',#52074,#8180);
#6748=LINE('',#52076,#8181);
#6749=LINE('',#52077,#8182);
#6750=LINE('',#52081,#8183);
#6751=LINE('',#52084,#8184);
#6752=LINE('',#52085,#8185);
#6753=LINE('',#52091,#8186);
#6754=LINE('',#52093,#8187);
#6755=LINE('',#52095,#8188);
#6756=LINE('',#52096,#8189);
#6757=LINE('',#52100,#8190);
#6758=LINE('',#52103,#8191);
#6759=LINE('',#52104,#8192);
#6760=LINE('',#52110,#8193);
#6761=LINE('',#52112,#8194);
#6762=LINE('',#52114,#8195);
#6763=LINE('',#52115,#8196);
#6764=LINE('',#52119,#8197);
#6765=LINE('',#52122,#8198);
#6766=LINE('',#52123,#8199);
#6767=LINE('',#52129,#8200);
#6768=LINE('',#52131,#8201);
#6769=LINE('',#52133,#8202);
#6770=LINE('',#52134,#8203);
#6771=LINE('',#52138,#8204);
#6772=LINE('',#52141,#8205);
#6773=LINE('',#52142,#8206);
#6774=LINE('',#52148,#8207);
#6775=LINE('',#52150,#8208);
#6776=LINE('',#52152,#8209);
#6777=LINE('',#52153,#8210);
#6778=LINE('',#52157,#8211);
#6779=LINE('',#52160,#8212);
#6780=LINE('',#52161,#8213);
#6781=LINE('',#52167,#8214);
#6782=LINE('',#52169,#8215);
#6783=LINE('',#52171,#8216);
#6784=LINE('',#52172,#8217);
#6785=LINE('',#52176,#8218);
#6786=LINE('',#52179,#8219);
#6787=LINE('',#52180,#8220);
#6788=LINE('',#52186,#8221);
#6789=LINE('',#52188,#8222);
#6790=LINE('',#52190,#8223);
#6791=LINE('',#52191,#8224);
#6792=LINE('',#52195,#8225);
#6793=LINE('',#52198,#8226);
#6794=LINE('',#52199,#8227);
#6795=LINE('',#52205,#8228);
#6796=LINE('',#52207,#8229);
#6797=LINE('',#52209,#8230);
#6798=LINE('',#52210,#8231);
#6799=LINE('',#52214,#8232);
#6800=LINE('',#52217,#8233);
#6801=LINE('',#52218,#8234);
#6802=LINE('',#52224,#8235);
#6803=LINE('',#52226,#8236);
#6804=LINE('',#52228,#8237);
#6805=LINE('',#52229,#8238);
#6806=LINE('',#52233,#8239);
#6807=LINE('',#52236,#8240);
#6808=LINE('',#52237,#8241);
#6809=LINE('',#52245,#8242);
#6810=LINE('',#52246,#8243);
#6811=LINE('',#52249,#8244);
#6812=LINE('',#52251,#8245);
#6813=LINE('',#52252,#8246);
#6814=LINE('',#52255,#8247);
#6815=LINE('',#52256,#8248);
#6816=LINE('',#52262,#8249);
#6817=LINE('',#52264,#8250);
#6818=LINE('',#52266,#8251);
#6819=LINE('',#52267,#8252);
#6820=LINE('',#52271,#8253);
#6821=LINE('',#52274,#8254);
#6822=LINE('',#52275,#8255);
#6823=LINE('',#52281,#8256);
#6824=LINE('',#52283,#8257);
#6825=LINE('',#52285,#8258);
#6826=LINE('',#52286,#8259);
#6827=LINE('',#52290,#8260);
#6828=LINE('',#52293,#8261);
#6829=LINE('',#52294,#8262);
#6830=LINE('',#52300,#8263);
#6831=LINE('',#52302,#8264);
#6832=LINE('',#52304,#8265);
#6833=LINE('',#52305,#8266);
#6834=LINE('',#52309,#8267);
#6835=LINE('',#52312,#8268);
#6836=LINE('',#52313,#8269);
#6837=LINE('',#52319,#8270);
#6838=LINE('',#52321,#8271);
#6839=LINE('',#52323,#8272);
#6840=LINE('',#52324,#8273);
#6841=LINE('',#52328,#8274);
#6842=LINE('',#52331,#8275);
#6843=LINE('',#52332,#8276);
#6844=LINE('',#52338,#8277);
#6845=LINE('',#52340,#8278);
#6846=LINE('',#52342,#8279);
#6847=LINE('',#52343,#8280);
#6848=LINE('',#52347,#8281);
#6849=LINE('',#52350,#8282);
#6850=LINE('',#52351,#8283);
#6851=LINE('',#52357,#8284);
#6852=LINE('',#52359,#8285);
#6853=LINE('',#52361,#8286);
#6854=LINE('',#52362,#8287);
#6855=LINE('',#52366,#8288);
#6856=LINE('',#52369,#8289);
#6857=LINE('',#52370,#8290);
#6858=LINE('',#52376,#8291);
#6859=LINE('',#52378,#8292);
#6860=LINE('',#52380,#8293);
#6861=LINE('',#52381,#8294);
#6862=LINE('',#52385,#8295);
#6863=LINE('',#52388,#8296);
#6864=LINE('',#52389,#8297);
#6865=LINE('',#52395,#8298);
#6866=LINE('',#52397,#8299);
#6867=LINE('',#52399,#8300);
#6868=LINE('',#52400,#8301);
#6869=LINE('',#52404,#8302);
#6870=LINE('',#52407,#8303);
#6871=LINE('',#52408,#8304);
#6872=LINE('',#52414,#8305);
#6873=LINE('',#52416,#8306);
#6874=LINE('',#52418,#8307);
#6875=LINE('',#52419,#8308);
#6876=LINE('',#52423,#8309);
#6877=LINE('',#52426,#8310);
#6878=LINE('',#52427,#8311);
#6879=LINE('',#52434,#8312);
#6880=LINE('',#52438,#8313);
#6881=LINE('',#52456,#8314);
#6882=LINE('',#52480,#8315);
#7995=VECTOR('',#29424,0.4);
#7996=VECTOR('',#29427,0.4);
#7997=VECTOR('',#29434,0.4);
#7998=VECTOR('',#29437,0.4);
#7999=VECTOR('',#29440,0.4);
#8000=VECTOR('',#29443,0.4);
#8001=VECTOR('',#29446,0.4);
#8002=VECTOR('',#29449,0.4);
#8003=VECTOR('',#29452,0.4);
#8004=VECTOR('',#29455,0.4);
#8005=VECTOR('',#29458,0.4);
#8006=VECTOR('',#29461,0.4);
#8007=VECTOR('',#29464,0.4);
#8008=VECTOR('',#29467,0.4);
#8009=VECTOR('',#29470,0.4);
#8010=VECTOR('',#29473,0.4);
#8011=VECTOR('',#29476,0.4);
#8012=VECTOR('',#29479,0.4);
#8013=VECTOR('',#29482,0.4);
#8014=VECTOR('',#29485,0.4);
#8015=VECTOR('',#29488,0.4);
#8016=VECTOR('',#29491,0.4);
#8017=VECTOR('',#29494,0.4);
#8018=VECTOR('',#29497,0.4);
#8019=VECTOR('',#29502,0.322275);
#8020=VECTOR('',#29507,0.322275);
#8021=VECTOR('',#29510,0.322275);
#8022=VECTOR('',#29513,0.322275);
#8023=VECTOR('',#29516,0.322275);
#8024=VECTOR('',#29519,0.322275);
#8025=VECTOR('',#29522,0.322275);
#8026=VECTOR('',#29525,0.322275);
#8027=VECTOR('',#29528,0.322275);
#8028=VECTOR('',#29531,0.322275);
#8029=VECTOR('',#29534,0.322275);
#8030=VECTOR('',#29537,0.322275);
#8031=VECTOR('',#29540,0.322275);
#8032=VECTOR('',#29543,0.322275);
#8033=VECTOR('',#29546,0.322275);
#8034=VECTOR('',#29549,0.322275);
#8035=VECTOR('',#29552,0.322275);
#8036=VECTOR('',#29555,0.322275);
#8037=VECTOR('',#29558,0.322275);
#8038=VECTOR('',#29561,0.322275);
#8039=VECTOR('',#29564,0.322275);
#8040=VECTOR('',#29567,0.322275);
#8041=VECTOR('',#29594,0.149995599935465);
#8042=VECTOR('',#29599,1.);
#8043=VECTOR('',#29600,1.);
#8044=VECTOR('',#29601,1.);
#8045=VECTOR('',#29602,1.);
#8046=VECTOR('',#29605,1.);
#8047=VECTOR('',#29606,1.);
#8048=VECTOR('',#29607,1.);
#8049=VECTOR('',#29610,1.);
#8050=VECTOR('',#29611,1.);
#8051=VECTOR('',#29612,1.);
#8052=VECTOR('',#29615,1.);
#8053=VECTOR('',#29616,1.);
#8054=VECTOR('',#29617,1.);
#8055=VECTOR('',#29620,1.);
#8056=VECTOR('',#29621,1.);
#8057=VECTOR('',#29622,1.);
#8058=VECTOR('',#29625,1.);
#8059=VECTOR('',#29626,1.);
#8060=VECTOR('',#29631,1.);
#8061=VECTOR('',#29632,1.);
#8062=VECTOR('',#29633,1.);
#8063=VECTOR('',#29634,1.);
#8064=VECTOR('',#29639,1.);
#8065=VECTOR('',#29642,1.);
#8066=VECTOR('',#29643,1.);
#8067=VECTOR('',#29650,1.);
#8068=VECTOR('',#29651,1.);
#8069=VECTOR('',#29652,1.);
#8070=VECTOR('',#29653,1.);
#8071=VECTOR('',#29658,1.);
#8072=VECTOR('',#29661,1.);
#8073=VECTOR('',#29662,1.);
#8074=VECTOR('',#29669,1.);
#8075=VECTOR('',#29670,1.);
#8076=VECTOR('',#29671,1.);
#8077=VECTOR('',#29672,1.);
#8078=VECTOR('',#29677,1.);
#8079=VECTOR('',#29680,1.);
#8080=VECTOR('',#29681,1.);
#8081=VECTOR('',#29688,1.);
#8082=VECTOR('',#29689,1.);
#8083=VECTOR('',#29690,1.);
#8084=VECTOR('',#29691,1.);
#8085=VECTOR('',#29696,1.);
#8086=VECTOR('',#29699,1.);
#8087=VECTOR('',#29700,1.);
#8088=VECTOR('',#29707,1.);
#8089=VECTOR('',#29708,1.);
#8090=VECTOR('',#29709,1.);
#8091=VECTOR('',#29710,1.);
#8092=VECTOR('',#29715,1.);
#8093=VECTOR('',#29718,1.);
#8094=VECTOR('',#29719,1.);
#8095=VECTOR('',#29726,1.);
#8096=VECTOR('',#29727,1.);
#8097=VECTOR('',#29728,1.);
#8098=VECTOR('',#29729,1.);
#8099=VECTOR('',#29734,1.);
#8100=VECTOR('',#29737,1.);
#8101=VECTOR('',#29738,1.);
#8102=VECTOR('',#29745,1.);
#8103=VECTOR('',#29746,1.);
#8104=VECTOR('',#29747,1.);
#8105=VECTOR('',#29748,1.);
#8106=VECTOR('',#29753,1.);
#8107=VECTOR('',#29756,1.);
#8108=VECTOR('',#29757,1.);
#8109=VECTOR('',#29764,1.);
#8110=VECTOR('',#29765,1.);
#8111=VECTOR('',#29766,1.);
#8112=VECTOR('',#29767,1.);
#8113=VECTOR('',#29772,1.);
#8114=VECTOR('',#29775,1.);
#8115=VECTOR('',#29776,1.);
#8116=VECTOR('',#29783,1.);
#8117=VECTOR('',#29784,1.);
#8118=VECTOR('',#29785,1.);
#8119=VECTOR('',#29786,1.);
#8120=VECTOR('',#29791,1.);
#8121=VECTOR('',#29796,1.);
#8122=VECTOR('',#29797,1.);
#8123=VECTOR('',#29806,1.);
#8124=VECTOR('',#29807,1.);
#8125=VECTOR('',#29808,1.);
#8126=VECTOR('',#29809,1.);
#8127=VECTOR('',#29814,1.);
#8128=VECTOR('',#29817,1.);
#8129=VECTOR('',#29818,1.);
#8130=VECTOR('',#29825,1.);
#8131=VECTOR('',#29826,1.);
#8132=VECTOR('',#29827,1.);
#8133=VECTOR('',#29828,1.);
#8134=VECTOR('',#29833,1.);
#8135=VECTOR('',#29836,1.);
#8136=VECTOR('',#29837,1.);
#8137=VECTOR('',#29844,1.);
#8138=VECTOR('',#29845,1.);
#8139=VECTOR('',#29846,1.);
#8140=VECTOR('',#29847,1.);
#8141=VECTOR('',#29852,1.);
#8142=VECTOR('',#29855,1.);
#8143=VECTOR('',#29856,1.);
#8144=VECTOR('',#29863,1.);
#8145=VECTOR('',#29864,1.);
#8146=VECTOR('',#29865,1.);
#8147=VECTOR('',#29866,1.);
#8148=VECTOR('',#29871,1.);
#8149=VECTOR('',#29874,1.);
#8150=VECTOR('',#29875,1.);
#8151=VECTOR('',#29882,1.);
#8152=VECTOR('',#29883,1.);
#8153=VECTOR('',#29884,1.);
#8154=VECTOR('',#29885,1.);
#8155=VECTOR('',#29890,1.);
#8156=VECTOR('',#29893,1.);
#8157=VECTOR('',#29894,1.);
#8158=VECTOR('',#29901,1.);
#8159=VECTOR('',#29902,1.);
#8160=VECTOR('',#29903,1.);
#8161=VECTOR('',#29904,1.);
#8162=VECTOR('',#29909,1.);
#8163=VECTOR('',#29912,1.);
#8164=VECTOR('',#29913,1.);
#8165=VECTOR('',#29920,1.);
#8166=VECTOR('',#29921,1.);
#8167=VECTOR('',#29922,1.);
#8168=VECTOR('',#29923,1.);
#8169=VECTOR('',#29928,1.);
#8170=VECTOR('',#29931,1.);
#8171=VECTOR('',#29932,1.);
#8172=VECTOR('',#29939,1.);
#8173=VECTOR('',#29940,1.);
#8174=VECTOR('',#29941,1.);
#8175=VECTOR('',#29942,1.);
#8176=VECTOR('',#29947,1.);
#8177=VECTOR('',#29950,1.);
#8178=VECTOR('',#29951,1.);
#8179=VECTOR('',#29958,1.);
#8180=VECTOR('',#29959,1.);
#8181=VECTOR('',#29960,1.);
#8182=VECTOR('',#29961,1.);
#8183=VECTOR('',#29966,1.);
#8184=VECTOR('',#29969,1.);
#8185=VECTOR('',#29970,1.);
#8186=VECTOR('',#29977,1.);
#8187=VECTOR('',#29978,1.);
#8188=VECTOR('',#29979,1.);
#8189=VECTOR('',#29980,1.);
#8190=VECTOR('',#29985,1.);
#8191=VECTOR('',#29988,1.);
#8192=VECTOR('',#29989,1.);
#8193=VECTOR('',#29996,1.);
#8194=VECTOR('',#29997,1.);
#8195=VECTOR('',#29998,1.);
#8196=VECTOR('',#29999,1.);
#8197=VECTOR('',#30004,1.);
#8198=VECTOR('',#30007,1.);
#8199=VECTOR('',#30008,1.);
#8200=VECTOR('',#30015,1.);
#8201=VECTOR('',#30016,1.);
#8202=VECTOR('',#30017,1.);
#8203=VECTOR('',#30018,1.);
#8204=VECTOR('',#30023,1.);
#8205=VECTOR('',#30026,1.);
#8206=VECTOR('',#30027,1.);
#8207=VECTOR('',#30034,1.);
#8208=VECTOR('',#30035,1.);
#8209=VECTOR('',#30036,1.);
#8210=VECTOR('',#30037,1.);
#8211=VECTOR('',#30042,1.);
#8212=VECTOR('',#30045,1.);
#8213=VECTOR('',#30046,1.);
#8214=VECTOR('',#30053,1.);
#8215=VECTOR('',#30054,1.);
#8216=VECTOR('',#30055,1.);
#8217=VECTOR('',#30056,1.);
#8218=VECTOR('',#30061,1.);
#8219=VECTOR('',#30064,1.);
#8220=VECTOR('',#30065,1.);
#8221=VECTOR('',#30072,1.);
#8222=VECTOR('',#30073,1.);
#8223=VECTOR('',#30074,1.);
#8224=VECTOR('',#30075,1.);
#8225=VECTOR('',#30080,1.);
#8226=VECTOR('',#30083,1.);
#8227=VECTOR('',#30084,1.);
#8228=VECTOR('',#30091,1.);
#8229=VECTOR('',#30092,1.);
#8230=VECTOR('',#30093,1.);
#8231=VECTOR('',#30094,1.);
#8232=VECTOR('',#30099,1.);
#8233=VECTOR('',#30102,1.);
#8234=VECTOR('',#30103,1.);
#8235=VECTOR('',#30110,1.);
#8236=VECTOR('',#30111,1.);
#8237=VECTOR('',#30112,1.);
#8238=VECTOR('',#30113,1.);
#8239=VECTOR('',#30118,1.);
#8240=VECTOR('',#30121,1.);
#8241=VECTOR('',#30122,1.);
#8242=VECTOR('',#30131,1.);
#8243=VECTOR('',#30132,1.);
#8244=VECTOR('',#30135,1.);
#8245=VECTOR('',#30136,1.);
#8246=VECTOR('',#30137,1.);
#8247=VECTOR('',#30140,1.);
#8248=VECTOR('',#30141,1.);
#8249=VECTOR('',#30148,1.);
#8250=VECTOR('',#30149,1.);
#8251=VECTOR('',#30150,1.);
#8252=VECTOR('',#30151,1.);
#8253=VECTOR('',#30156,1.);
#8254=VECTOR('',#30159,1.);
#8255=VECTOR('',#30160,1.);
#8256=VECTOR('',#30167,1.);
#8257=VECTOR('',#30168,1.);
#8258=VECTOR('',#30169,1.);
#8259=VECTOR('',#30170,1.);
#8260=VECTOR('',#30175,1.);
#8261=VECTOR('',#30178,1.);
#8262=VECTOR('',#30179,1.);
#8263=VECTOR('',#30186,1.);
#8264=VECTOR('',#30187,1.);
#8265=VECTOR('',#30188,1.);
#8266=VECTOR('',#30189,1.);
#8267=VECTOR('',#30194,1.);
#8268=VECTOR('',#30197,1.);
#8269=VECTOR('',#30198,1.);
#8270=VECTOR('',#30205,1.);
#8271=VECTOR('',#30206,1.);
#8272=VECTOR('',#30207,1.);
#8273=VECTOR('',#30208,1.);
#8274=VECTOR('',#30213,1.);
#8275=VECTOR('',#30216,1.);
#8276=VECTOR('',#30217,1.);
#8277=VECTOR('',#30224,1.);
#8278=VECTOR('',#30225,1.);
#8279=VECTOR('',#30226,1.);
#8280=VECTOR('',#30227,1.);
#8281=VECTOR('',#30232,1.);
#8282=VECTOR('',#30235,1.);
#8283=VECTOR('',#30236,1.);
#8284=VECTOR('',#30243,1.);
#8285=VECTOR('',#30244,1.);
#8286=VECTOR('',#30245,1.);
#8287=VECTOR('',#30246,1.);
#8288=VECTOR('',#30251,1.);
#8289=VECTOR('',#30254,1.);
#8290=VECTOR('',#30255,1.);
#8291=VECTOR('',#30262,1.);
#8292=VECTOR('',#30263,1.);
#8293=VECTOR('',#30264,1.);
#8294=VECTOR('',#30265,1.);
#8295=VECTOR('',#30270,1.);
#8296=VECTOR('',#30273,1.);
#8297=VECTOR('',#30274,1.);
#8298=VECTOR('',#30281,1.);
#8299=VECTOR('',#30282,1.);
#8300=VECTOR('',#30283,1.);
#8301=VECTOR('',#30284,1.);
#8302=VECTOR('',#30289,1.);
#8303=VECTOR('',#30292,1.);
#8304=VECTOR('',#30293,1.);
#8305=VECTOR('',#30300,1.);
#8306=VECTOR('',#30301,1.);
#8307=VECTOR('',#30302,1.);
#8308=VECTOR('',#30303,1.);
#8309=VECTOR('',#30308,1.);
#8310=VECTOR('',#30311,1.);
#8311=VECTOR('',#30312,1.);
#8312=VECTOR('',#30323,0.37);
#8313=VECTOR('',#30328,0.63);
#8314=VECTOR('',#30363,0.65);
#8315=VECTOR('',#30408,0.62);
#9045=CIRCLE('',#24663,0.3933);
#9046=CIRCLE('',#24664,0.3933);
#9047=CIRCLE('',#24665,0.3933);
#9048=CIRCLE('',#24688,0.3933);
#9049=CIRCLE('',#24690,0.322275);
#9050=CIRCLE('',#24713,0.3933);
#9051=CIRCLE('',#24715,0.322275);
#9052=CIRCLE('',#24718,0.3933);
#9053=CIRCLE('',#24720,0.04);
#9054=CIRCLE('',#24721,0.4333);
#9055=CIRCLE('',#24723,0.61);
#9056=CIRCLE('',#24725,0.29999119987093);
#9057=CIRCLE('',#24735,0.65);
#9058=CIRCLE('',#24738,0.65);
#9059=CIRCLE('',#24741,0.65);
#9060=CIRCLE('',#24744,0.65);
#9061=CIRCLE('',#24747,0.65);
#9062=CIRCLE('',#24750,0.65);
#9063=CIRCLE('',#24753,0.65);
#9064=CIRCLE('',#24756,0.65);
#9065=CIRCLE('',#24759,0.65);
#9066=CIRCLE('',#24762,0.65);
#9067=CIRCLE('',#24765,0.65);
#9068=CIRCLE('',#24768,0.65);
#9069=CIRCLE('',#24771,0.65);
#9070=CIRCLE('',#24774,0.65);
#9071=CIRCLE('',#24777,0.65);
#9072=CIRCLE('',#24780,0.65);
#9073=CIRCLE('',#24783,0.65);
#9074=CIRCLE('',#24784,0.65);
#9075=CIRCLE('',#24787,0.65);
#9076=CIRCLE('',#24788,0.65);
#9077=CIRCLE('',#24791,0.65);
#9078=CIRCLE('',#24794,0.65);
#9079=CIRCLE('',#24797,0.65);
#9080=CIRCLE('',#24800,0.65);
#9081=CIRCLE('',#24803,0.65);
#9082=CIRCLE('',#24806,0.65);
#9083=CIRCLE('',#24809,0.65);
#9084=CIRCLE('',#24812,0.65);
#9085=CIRCLE('',#24815,0.65);
#9086=CIRCLE('',#24818,0.65);
#9087=CIRCLE('',#24821,0.65);
#9088=CIRCLE('',#24824,0.65);
#9089=CIRCLE('',#24827,0.65);
#9090=CIRCLE('',#24830,0.65);
#9091=CIRCLE('',#24833,0.65);
#9092=CIRCLE('',#24836,0.65);
#9093=CIRCLE('',#24839,0.65);
#9094=CIRCLE('',#24842,0.65);
#9095=CIRCLE('',#24845,0.65);
#9096=CIRCLE('',#24848,0.65);
#9097=CIRCLE('',#24851,0.65);
#9098=CIRCLE('',#24854,0.65);
#9099=CIRCLE('',#24857,0.65);
#9100=CIRCLE('',#24860,0.65);
#9101=CIRCLE('',#24863,0.65);
#9102=CIRCLE('',#24866,0.65);
#9103=CIRCLE('',#24869,0.65);
#9104=CIRCLE('',#24872,0.65);
#9105=CIRCLE('',#24875,0.65);
#9106=CIRCLE('',#24878,0.65);
#9107=CIRCLE('',#24881,0.65);
#9108=CIRCLE('',#24884,0.65);
#9109=CIRCLE('',#24887,0.65);
#9110=CIRCLE('',#24890,0.65);
#9111=CIRCLE('',#24892,0.65);
#9112=CIRCLE('',#24896,0.65);
#9113=CIRCLE('',#24899,0.65);
#9114=CIRCLE('',#24902,0.65);
#9115=CIRCLE('',#24905,0.65);
#9116=CIRCLE('',#24908,0.65);
#9117=CIRCLE('',#24911,0.65);
#9118=CIRCLE('',#24914,0.65);
#9119=CIRCLE('',#24917,0.65);
#9120=CIRCLE('',#24920,0.65);
#9121=CIRCLE('',#24923,0.65);
#9122=CIRCLE('',#24926,0.65);
#9123=CIRCLE('',#24929,0.65);
#9124=CIRCLE('',#24932,0.65);
#9125=CIRCLE('',#24935,0.65);
#9126=CIRCLE('',#24938,0.65);
#9127=CIRCLE('',#24941,0.65);
#9128=CIRCLE('',#24944,0.65);
#9129=CIRCLE('',#24947,0.65);
#9130=CIRCLE('',#24950,0.65);
#9131=CIRCLE('',#24952,0.34);
#9132=CIRCLE('',#24955,0.65);
#9133=CIRCLE('',#24957,0.65);
#9134=CIRCLE('',#24958,0.65);
#9135=CIRCLE('',#24959,0.65);
#9136=CIRCLE('',#24960,0.65);
#9137=CIRCLE('',#24961,0.65);
#9138=CIRCLE('',#24962,0.65);
#9139=CIRCLE('',#24963,0.65);
#9140=CIRCLE('',#24964,0.65);
#9141=CIRCLE('',#24965,0.65);
#9142=CIRCLE('',#24966,0.65);
#9143=CIRCLE('',#24967,0.65);
#9144=CIRCLE('',#24968,0.65);
#9145=CIRCLE('',#24969,0.65);
#9146=CIRCLE('',#24970,0.65);
#9147=CIRCLE('',#24971,0.65);
#9148=CIRCLE('',#24972,0.65);
#9149=CIRCLE('',#24973,0.65);
#9150=CIRCLE('',#24974,0.65);
#9151=CIRCLE('',#24975,0.65);
#9152=CIRCLE('',#24976,0.65);
#9153=CIRCLE('',#24977,0.65);
#9154=CIRCLE('',#24978,0.65);
#9155=CIRCLE('',#24979,0.65);
#9156=CIRCLE('',#24980,0.65);
#9157=CIRCLE('',#24981,0.65);
#9158=CIRCLE('',#24982,0.65);
#9159=CIRCLE('',#24983,0.65);
#9160=CIRCLE('',#24984,0.65);
#9161=CIRCLE('',#24985,0.65);
#9162=CIRCLE('',#24986,0.65);
#9163=CIRCLE('',#24987,0.65);
#9164=CIRCLE('',#24988,0.65);
#9165=CIRCLE('',#24989,0.65);
#9166=CIRCLE('',#24990,0.65);
#9167=CIRCLE('',#24991,0.65);
#9168=CIRCLE('',#24992,0.65);
#9169=CIRCLE('',#24994,0.59);
#10897=VERTEX_POINT('',#48575);
#10898=VERTEX_POINT('',#48576);
#10899=VERTEX_POINT('',#48578);
#10900=VERTEX_POINT('',#48592);
#10901=VERTEX_POINT('',#48594);
#10902=VERTEX_POINT('',#48597);
#10903=VERTEX_POINT('',#48610);
#10904=VERTEX_POINT('',#48611);
#10905=VERTEX_POINT('',#48658);
#10906=VERTEX_POINT('',#48659);
#10907=VERTEX_POINT('',#48706);
#10908=VERTEX_POINT('',#48707);
#10909=VERTEX_POINT('',#48754);
#10910=VERTEX_POINT('',#48755);
#10911=VERTEX_POINT('',#48808);
#10912=VERTEX_POINT('',#48809);
#10913=VERTEX_POINT('',#48856);
#10914=VERTEX_POINT('',#48857);
#10915=VERTEX_POINT('',#48904);
#10916=VERTEX_POINT('',#48905);
#10917=VERTEX_POINT('',#48958);
#10918=VERTEX_POINT('',#48959);
#10919=VERTEX_POINT('',#49006);
#10920=VERTEX_POINT('',#49007);
#10921=VERTEX_POINT('',#49054);
#10922=VERTEX_POINT('',#49055);
#10923=VERTEX_POINT('',#49102);
#10924=VERTEX_POINT('',#49103);
#10925=VERTEX_POINT('',#49156);
#10926=VERTEX_POINT('',#49157);
#10927=VERTEX_POINT('',#49204);
#10928=VERTEX_POINT('',#49205);
#10929=VERTEX_POINT('',#49252);
#10930=VERTEX_POINT('',#49253);
#10931=VERTEX_POINT('',#49306);
#10932=VERTEX_POINT('',#49307);
#10933=VERTEX_POINT('',#49354);
#10934=VERTEX_POINT('',#49355);
#10935=VERTEX_POINT('',#49402);
#10936=VERTEX_POINT('',#49403);
#10937=VERTEX_POINT('',#49450);
#10938=VERTEX_POINT('',#49451);
#10939=VERTEX_POINT('',#49504);
#10940=VERTEX_POINT('',#49505);
#10941=VERTEX_POINT('',#49552);
#10942=VERTEX_POINT('',#49553);
#10943=VERTEX_POINT('',#49600);
#10944=VERTEX_POINT('',#49601);
#10945=VERTEX_POINT('',#49654);
#10946=VERTEX_POINT('',#49655);
#10947=VERTEX_POINT('',#49657);
#10948=VERTEX_POINT('',#49701);
#10949=VERTEX_POINT('',#49702);
#10950=VERTEX_POINT('',#49704);
#10951=VERTEX_POINT('',#49712);
#10952=VERTEX_POINT('',#49721);
#10953=VERTEX_POINT('',#49722);
#10954=VERTEX_POINT('',#49746);
#10955=VERTEX_POINT('',#49747);
#10956=VERTEX_POINT('',#49771);
#10957=VERTEX_POINT('',#49772);
#10958=VERTEX_POINT('',#49795);
#10959=VERTEX_POINT('',#49796);
#10960=VERTEX_POINT('',#49820);
#10961=VERTEX_POINT('',#49821);
#10962=VERTEX_POINT('',#49845);
#10963=VERTEX_POINT('',#49846);
#10964=VERTEX_POINT('',#49869);
#10965=VERTEX_POINT('',#49870);
#10966=VERTEX_POINT('',#49893);
#10967=VERTEX_POINT('',#49894);
#10968=VERTEX_POINT('',#49918);
#10969=VERTEX_POINT('',#49919);
#10970=VERTEX_POINT('',#49943);
#10971=VERTEX_POINT('',#49944);
#10972=VERTEX_POINT('',#49967);
#10973=VERTEX_POINT('',#49968);
#10974=VERTEX_POINT('',#49992);
#10975=VERTEX_POINT('',#49993);
#10976=VERTEX_POINT('',#50017);
#10977=VERTEX_POINT('',#50018);
#10978=VERTEX_POINT('',#50041);
#10979=VERTEX_POINT('',#50042);
#10980=VERTEX_POINT('',#50065);
#10981=VERTEX_POINT('',#50066);
#10982=VERTEX_POINT('',#50090);
#10983=VERTEX_POINT('',#50091);
#10984=VERTEX_POINT('',#50115);
#10985=VERTEX_POINT('',#50116);
#10986=VERTEX_POINT('',#50139);
#10987=VERTEX_POINT('',#50140);
#10988=VERTEX_POINT('',#50164);
#10989=VERTEX_POINT('',#50165);
#10990=VERTEX_POINT('',#50189);
#10991=VERTEX_POINT('',#50190);
#10992=VERTEX_POINT('',#50213);
#10993=VERTEX_POINT('',#50214);
#10994=VERTEX_POINT('',#50304);
#10995=VERTEX_POINT('',#50955);
#10996=VERTEX_POINT('',#51034);
#10997=VERTEX_POINT('',#51694);
#10998=VERTEX_POINT('',#51698);
#10999=VERTEX_POINT('',#51701);
#11000=VERTEX_POINT('',#51702);
#11001=VERTEX_POINT('',#51706);
#11002=VERTEX_POINT('',#51707);
#11003=VERTEX_POINT('',#51709);
#11004=VERTEX_POINT('',#51711);
#11005=VERTEX_POINT('',#51715);
#11006=VERTEX_POINT('',#51717);
#11007=VERTEX_POINT('',#51721);
#11008=VERTEX_POINT('',#51723);
#11009=VERTEX_POINT('',#51727);
#11010=VERTEX_POINT('',#51729);
#11011=VERTEX_POINT('',#51733);
#11012=VERTEX_POINT('',#51735);
#11013=VERTEX_POINT('',#51743);
#11014=VERTEX_POINT('',#51744);
#11015=VERTEX_POINT('',#51746);
#11016=VERTEX_POINT('',#51748);
#11017=VERTEX_POINT('',#51752);
#11018=VERTEX_POINT('',#51756);
#11019=VERTEX_POINT('',#51762);
#11020=VERTEX_POINT('',#51763);
#11021=VERTEX_POINT('',#51765);
#11022=VERTEX_POINT('',#51767);
#11023=VERTEX_POINT('',#51771);
#11024=VERTEX_POINT('',#51775);
#11025=VERTEX_POINT('',#51781);
#11026=VERTEX_POINT('',#51782);
#11027=VERTEX_POINT('',#51784);
#11028=VERTEX_POINT('',#51786);
#11029=VERTEX_POINT('',#51790);
#11030=VERTEX_POINT('',#51794);
#11031=VERTEX_POINT('',#51800);
#11032=VERTEX_POINT('',#51801);
#11033=VERTEX_POINT('',#51803);
#11034=VERTEX_POINT('',#51805);
#11035=VERTEX_POINT('',#51809);
#11036=VERTEX_POINT('',#51813);
#11037=VERTEX_POINT('',#51819);
#11038=VERTEX_POINT('',#51820);
#11039=VERTEX_POINT('',#51822);
#11040=VERTEX_POINT('',#51824);
#11041=VERTEX_POINT('',#51828);
#11042=VERTEX_POINT('',#51832);
#11043=VERTEX_POINT('',#51838);
#11044=VERTEX_POINT('',#51839);
#11045=VERTEX_POINT('',#51841);
#11046=VERTEX_POINT('',#51843);
#11047=VERTEX_POINT('',#51847);
#11048=VERTEX_POINT('',#51851);
#11049=VERTEX_POINT('',#51857);
#11050=VERTEX_POINT('',#51858);
#11051=VERTEX_POINT('',#51860);
#11052=VERTEX_POINT('',#51862);
#11053=VERTEX_POINT('',#51866);
#11054=VERTEX_POINT('',#51870);
#11055=VERTEX_POINT('',#51876);
#11056=VERTEX_POINT('',#51877);
#11057=VERTEX_POINT('',#51879);
#11058=VERTEX_POINT('',#51881);
#11059=VERTEX_POINT('',#51885);
#11060=VERTEX_POINT('',#51889);
#11061=VERTEX_POINT('',#51895);
#11062=VERTEX_POINT('',#51896);
#11063=VERTEX_POINT('',#51898);
#11064=VERTEX_POINT('',#51900);
#11065=VERTEX_POINT('',#51904);
#11066=VERTEX_POINT('',#51906);
#11067=VERTEX_POINT('',#51910);
#11068=VERTEX_POINT('',#51914);
#11069=VERTEX_POINT('',#51918);
#11070=VERTEX_POINT('',#51919);
#11071=VERTEX_POINT('',#51921);
#11072=VERTEX_POINT('',#51923);
#11073=VERTEX_POINT('',#51927);
#11074=VERTEX_POINT('',#51931);
#11075=VERTEX_POINT('',#51937);
#11076=VERTEX_POINT('',#51938);
#11077=VERTEX_POINT('',#51940);
#11078=VERTEX_POINT('',#51942);
#11079=VERTEX_POINT('',#51946);
#11080=VERTEX_POINT('',#51950);
#11081=VERTEX_POINT('',#51956);
#11082=VERTEX_POINT('',#51957);
#11083=VERTEX_POINT('',#51959);
#11084=VERTEX_POINT('',#51961);
#11085=VERTEX_POINT('',#51965);
#11086=VERTEX_POINT('',#51969);
#11087=VERTEX_POINT('',#51975);
#11088=VERTEX_POINT('',#51976);
#11089=VERTEX_POINT('',#51978);
#11090=VERTEX_POINT('',#51980);
#11091=VERTEX_POINT('',#51984);
#11092=VERTEX_POINT('',#51988);
#11093=VERTEX_POINT('',#51994);
#11094=VERTEX_POINT('',#51995);
#11095=VERTEX_POINT('',#51997);
#11096=VERTEX_POINT('',#51999);
#11097=VERTEX_POINT('',#52003);
#11098=VERTEX_POINT('',#52007);
#11099=VERTEX_POINT('',#52013);
#11100=VERTEX_POINT('',#52014);
#11101=VERTEX_POINT('',#52016);
#11102=VERTEX_POINT('',#52018);
#11103=VERTEX_POINT('',#52022);
#11104=VERTEX_POINT('',#52026);
#11105=VERTEX_POINT('',#52032);
#11106=VERTEX_POINT('',#52033);
#11107=VERTEX_POINT('',#52035);
#11108=VERTEX_POINT('',#52037);
#11109=VERTEX_POINT('',#52041);
#11110=VERTEX_POINT('',#52045);
#11111=VERTEX_POINT('',#52051);
#11112=VERTEX_POINT('',#52052);
#11113=VERTEX_POINT('',#52054);
#11114=VERTEX_POINT('',#52056);
#11115=VERTEX_POINT('',#52060);
#11116=VERTEX_POINT('',#52064);
#11117=VERTEX_POINT('',#52070);
#11118=VERTEX_POINT('',#52071);
#11119=VERTEX_POINT('',#52073);
#11120=VERTEX_POINT('',#52075);
#11121=VERTEX_POINT('',#52079);
#11122=VERTEX_POINT('',#52083);
#11123=VERTEX_POINT('',#52089);
#11124=VERTEX_POINT('',#52090);
#11125=VERTEX_POINT('',#52092);
#11126=VERTEX_POINT('',#52094);
#11127=VERTEX_POINT('',#52098);
#11128=VERTEX_POINT('',#52102);
#11129=VERTEX_POINT('',#52108);
#11130=VERTEX_POINT('',#52109);
#11131=VERTEX_POINT('',#52111);
#11132=VERTEX_POINT('',#52113);
#11133=VERTEX_POINT('',#52117);
#11134=VERTEX_POINT('',#52121);
#11135=VERTEX_POINT('',#52127);
#11136=VERTEX_POINT('',#52128);
#11137=VERTEX_POINT('',#52130);
#11138=VERTEX_POINT('',#52132);
#11139=VERTEX_POINT('',#52136);
#11140=VERTEX_POINT('',#52140);
#11141=VERTEX_POINT('',#52146);
#11142=VERTEX_POINT('',#52147);
#11143=VERTEX_POINT('',#52149);
#11144=VERTEX_POINT('',#52151);
#11145=VERTEX_POINT('',#52155);
#11146=VERTEX_POINT('',#52159);
#11147=VERTEX_POINT('',#52165);
#11148=VERTEX_POINT('',#52166);
#11149=VERTEX_POINT('',#52168);
#11150=VERTEX_POINT('',#52170);
#11151=VERTEX_POINT('',#52174);
#11152=VERTEX_POINT('',#52178);
#11153=VERTEX_POINT('',#52184);
#11154=VERTEX_POINT('',#52185);
#11155=VERTEX_POINT('',#52187);
#11156=VERTEX_POINT('',#52189);
#11157=VERTEX_POINT('',#52193);
#11158=VERTEX_POINT('',#52197);
#11159=VERTEX_POINT('',#52203);
#11160=VERTEX_POINT('',#52204);
#11161=VERTEX_POINT('',#52206);
#11162=VERTEX_POINT('',#52208);
#11163=VERTEX_POINT('',#52212);
#11164=VERTEX_POINT('',#52216);
#11165=VERTEX_POINT('',#52222);
#11166=VERTEX_POINT('',#52223);
#11167=VERTEX_POINT('',#52225);
#11168=VERTEX_POINT('',#52227);
#11169=VERTEX_POINT('',#52231);
#11170=VERTEX_POINT('',#52235);
#11171=VERTEX_POINT('',#52241);
#11172=VERTEX_POINT('',#52242);
#11173=VERTEX_POINT('',#52244);
#11174=VERTEX_POINT('',#52248);
#11175=VERTEX_POINT('',#52250);
#11176=VERTEX_POINT('',#52254);
#11177=VERTEX_POINT('',#52260);
#11178=VERTEX_POINT('',#52261);
#11179=VERTEX_POINT('',#52263);
#11180=VERTEX_POINT('',#52265);
#11181=VERTEX_POINT('',#52269);
#11182=VERTEX_POINT('',#52273);
#11183=VERTEX_POINT('',#52279);
#11184=VERTEX_POINT('',#52280);
#11185=VERTEX_POINT('',#52282);
#11186=VERTEX_POINT('',#52284);
#11187=VERTEX_POINT('',#52288);
#11188=VERTEX_POINT('',#52292);
#11189=VERTEX_POINT('',#52298);
#11190=VERTEX_POINT('',#52299);
#11191=VERTEX_POINT('',#52301);
#11192=VERTEX_POINT('',#52303);
#11193=VERTEX_POINT('',#52307);
#11194=VERTEX_POINT('',#52311);
#11195=VERTEX_POINT('',#52317);
#11196=VERTEX_POINT('',#52318);
#11197=VERTEX_POINT('',#52320);
#11198=VERTEX_POINT('',#52322);
#11199=VERTEX_POINT('',#52326);
#11200=VERTEX_POINT('',#52330);
#11201=VERTEX_POINT('',#52336);
#11202=VERTEX_POINT('',#52337);
#11203=VERTEX_POINT('',#52339);
#11204=VERTEX_POINT('',#52341);
#11205=VERTEX_POINT('',#52345);
#11206=VERTEX_POINT('',#52349);
#11207=VERTEX_POINT('',#52355);
#11208=VERTEX_POINT('',#52356);
#11209=VERTEX_POINT('',#52358);
#11210=VERTEX_POINT('',#52360);
#11211=VERTEX_POINT('',#52364);
#11212=VERTEX_POINT('',#52368);
#11213=VERTEX_POINT('',#52374);
#11214=VERTEX_POINT('',#52375);
#11215=VERTEX_POINT('',#52377);
#11216=VERTEX_POINT('',#52379);
#11217=VERTEX_POINT('',#52383);
#11218=VERTEX_POINT('',#52387);
#11219=VERTEX_POINT('',#52393);
#11220=VERTEX_POINT('',#52394);
#11221=VERTEX_POINT('',#52396);
#11222=VERTEX_POINT('',#52398);
#11223=VERTEX_POINT('',#52402);
#11224=VERTEX_POINT('',#52406);
#11225=VERTEX_POINT('',#52412);
#11226=VERTEX_POINT('',#52413);
#11227=VERTEX_POINT('',#52415);
#11228=VERTEX_POINT('',#52417);
#11229=VERTEX_POINT('',#52421);
#11230=VERTEX_POINT('',#52425);
#11231=VERTEX_POINT('',#52431);
#11232=VERTEX_POINT('',#52436);
#11233=VERTEX_POINT('',#52478);
#13965=EDGE_CURVE('',#10897,#10898,#6562,.T.);
#13966=EDGE_CURVE('',#10897,#10899,#1277,.T.);
#13967=EDGE_CURVE('',#10899,#10900,#9045,.T.);
#13968=EDGE_CURVE('',#10900,#10901,#6563,.T.);
#13969=EDGE_CURVE('',#10901,#10901,#9046,.T.);
#13970=EDGE_CURVE('',#10900,#10902,#9047,.T.);
#13971=EDGE_CURVE('',#10902,#10898,#1278,.T.);
#13972=EDGE_CURVE('',#10903,#10904,#6564,.T.);
#13973=EDGE_CURVE('',#10903,#10897,#1279,.T.);
#13974=EDGE_CURVE('',#10898,#10904,#1280,.T.);
#13975=EDGE_CURVE('',#10905,#10906,#6565,.T.);
#13976=EDGE_CURVE('',#10905,#10903,#1281,.T.);
#13977=EDGE_CURVE('',#10904,#10906,#1282,.T.);
#13978=EDGE_CURVE('',#10907,#10908,#6566,.T.);
#13979=EDGE_CURVE('',#10907,#10905,#1283,.T.);
#13980=EDGE_CURVE('',#10906,#10908,#1284,.T.);
#13981=EDGE_CURVE('',#10909,#10910,#6567,.T.);
#13982=EDGE_CURVE('',#10909,#10907,#1285,.T.);
#13983=EDGE_CURVE('',#10908,#10910,#1286,.T.);
#13984=EDGE_CURVE('',#10911,#10912,#6568,.T.);
#13985=EDGE_CURVE('',#10911,#10909,#1287,.T.);
#13986=EDGE_CURVE('',#10910,#10912,#1288,.T.);
#13987=EDGE_CURVE('',#10913,#10914,#6569,.T.);
#13988=EDGE_CURVE('',#10913,#10911,#1289,.T.);
#13989=EDGE_CURVE('',#10912,#10914,#1290,.T.);
#13990=EDGE_CURVE('',#10915,#10916,#6570,.T.);
#13991=EDGE_CURVE('',#10915,#10913,#1291,.T.);
#13992=EDGE_CURVE('',#10914,#10916,#1292,.T.);
#13993=EDGE_CURVE('',#10917,#10918,#6571,.T.);
#13994=EDGE_CURVE('',#10917,#10915,#1293,.T.);
#13995=EDGE_CURVE('',#10916,#10918,#1294,.T.);
#13996=EDGE_CURVE('',#10919,#10920,#6572,.T.);
#13997=EDGE_CURVE('',#10919,#10917,#1295,.T.);
#13998=EDGE_CURVE('',#10918,#10920,#1296,.T.);
#13999=EDGE_CURVE('',#10921,#10922,#6573,.T.);
#14000=EDGE_CURVE('',#10921,#10919,#1297,.T.);
#14001=EDGE_CURVE('',#10920,#10922,#1298,.T.);
#14002=EDGE_CURVE('',#10923,#10924,#6574,.T.);
#14003=EDGE_CURVE('',#10923,#10921,#1299,.T.);
#14004=EDGE_CURVE('',#10922,#10924,#1300,.T.);
#14005=EDGE_CURVE('',#10925,#10926,#6575,.T.);
#14006=EDGE_CURVE('',#10925,#10923,#1301,.T.);
#14007=EDGE_CURVE('',#10924,#10926,#1302,.T.);
#14008=EDGE_CURVE('',#10927,#10928,#6576,.T.);
#14009=EDGE_CURVE('',#10927,#10925,#1303,.T.);
#14010=EDGE_CURVE('',#10926,#10928,#1304,.T.);
#14011=EDGE_CURVE('',#10929,#10930,#6577,.T.);
#14012=EDGE_CURVE('',#10929,#10927,#1305,.T.);
#14013=EDGE_CURVE('',#10928,#10930,#1306,.T.);
#14014=EDGE_CURVE('',#10931,#10932,#6578,.T.);
#14015=EDGE_CURVE('',#10931,#10929,#1307,.T.);
#14016=EDGE_CURVE('',#10930,#10932,#1308,.T.);
#14017=EDGE_CURVE('',#10933,#10934,#6579,.T.);
#14018=EDGE_CURVE('',#10933,#10931,#1309,.T.);
#14019=EDGE_CURVE('',#10932,#10934,#1310,.T.);
#14020=EDGE_CURVE('',#10935,#10936,#6580,.T.);
#14021=EDGE_CURVE('',#10935,#10933,#1311,.T.);
#14022=EDGE_CURVE('',#10934,#10936,#1312,.T.);
#14023=EDGE_CURVE('',#10937,#10938,#6581,.T.);
#14024=EDGE_CURVE('',#10937,#10935,#1313,.T.);
#14025=EDGE_CURVE('',#10936,#10938,#1314,.T.);
#14026=EDGE_CURVE('',#10939,#10940,#6582,.T.);
#14027=EDGE_CURVE('',#10939,#10937,#1315,.T.);
#14028=EDGE_CURVE('',#10938,#10940,#1316,.T.);
#14029=EDGE_CURVE('',#10941,#10942,#6583,.T.);
#14030=EDGE_CURVE('',#10941,#10939,#1317,.T.);
#14031=EDGE_CURVE('',#10940,#10942,#1318,.T.);
#14032=EDGE_CURVE('',#10943,#10944,#6584,.T.);
#14033=EDGE_CURVE('',#10943,#10941,#1319,.T.);
#14034=EDGE_CURVE('',#10942,#10944,#1320,.T.);
#14035=EDGE_CURVE('',#10945,#10946,#6585,.T.);
#14036=EDGE_CURVE('',#10947,#10945,#9048,.T.);
#14037=EDGE_CURVE('',#10947,#10943,#1321,.T.);
#14038=EDGE_CURVE('',#10944,#10946,#1322,.T.);
#14039=EDGE_CURVE('',#10948,#10949,#6586,.T.);
#14040=EDGE_CURVE('',#10948,#10950,#1323,.T.);
#14041=EDGE_CURVE('',#10951,#10950,#9049,.T.);
#14042=EDGE_CURVE('',#10949,#10951,#1324,.T.);
#14043=EDGE_CURVE('',#10952,#10953,#6587,.T.);
#14044=EDGE_CURVE('',#10952,#10948,#1325,.T.);
#14045=EDGE_CURVE('',#10953,#10949,#1326,.T.);
#14046=EDGE_CURVE('',#10954,#10955,#6588,.T.);
#14047=EDGE_CURVE('',#10954,#10952,#1327,.T.);
#14048=EDGE_CURVE('',#10955,#10953,#1328,.T.);
#14049=EDGE_CURVE('',#10956,#10957,#6589,.T.);
#14050=EDGE_CURVE('',#10956,#10954,#1329,.T.);
#14051=EDGE_CURVE('',#10957,#10955,#1330,.T.);
#14052=EDGE_CURVE('',#10958,#10959,#6590,.T.);
#14053=EDGE_CURVE('',#10958,#10956,#1331,.T.);
#14054=EDGE_CURVE('',#10959,#10957,#1332,.T.);
#14055=EDGE_CURVE('',#10960,#10961,#6591,.T.);
#14056=EDGE_CURVE('',#10960,#10958,#1333,.T.);
#14057=EDGE_CURVE('',#10961,#10959,#1334,.T.);
#14058=EDGE_CURVE('',#10962,#10963,#6592,.T.);
#14059=EDGE_CURVE('',#10962,#10960,#1335,.T.);
#14060=EDGE_CURVE('',#10963,#10961,#1336,.T.);
#14061=EDGE_CURVE('',#10964,#10965,#6593,.T.);
#14062=EDGE_CURVE('',#10964,#10962,#1337,.T.);
#14063=EDGE_CURVE('',#10965,#10963,#1338,.T.);
#14064=EDGE_CURVE('',#10966,#10967,#6594,.T.);
#14065=EDGE_CURVE('',#10966,#10964,#1339,.T.);
#14066=EDGE_CURVE('',#10967,#10965,#1340,.T.);
#14067=EDGE_CURVE('',#10968,#10969,#6595,.T.);
#14068=EDGE_CURVE('',#10968,#10966,#1341,.T.);
#14069=EDGE_CURVE('',#10969,#10967,#1342,.T.);
#14070=EDGE_CURVE('',#10970,#10971,#6596,.T.);
#14071=EDGE_CURVE('',#10970,#10968,#1343,.T.);
#14072=EDGE_CURVE('',#10971,#10969,#1344,.T.);
#14073=EDGE_CURVE('',#10972,#10973,#6597,.T.);
#14074=EDGE_CURVE('',#10972,#10970,#1345,.T.);
#14075=EDGE_CURVE('',#10973,#10971,#1346,.T.);
#14076=EDGE_CURVE('',#10974,#10975,#6598,.T.);
#14077=EDGE_CURVE('',#10974,#10972,#1347,.T.);
#14078=EDGE_CURVE('',#10975,#10973,#1348,.T.);
#14079=EDGE_CURVE('',#10976,#10977,#6599,.T.);
#14080=EDGE_CURVE('',#10976,#10974,#1349,.T.);
#14081=EDGE_CURVE('',#10977,#10975,#1350,.T.);
#14082=EDGE_CURVE('',#10978,#10979,#6600,.T.);
#14083=EDGE_CURVE('',#10978,#10976,#1351,.T.);
#14084=EDGE_CURVE('',#10979,#10977,#1352,.T.);
#14085=EDGE_CURVE('',#10980,#10981,#6601,.T.);
#14086=EDGE_CURVE('',#10980,#10978,#1353,.T.);
#14087=EDGE_CURVE('',#10981,#10979,#1354,.T.);
#14088=EDGE_CURVE('',#10982,#10983,#6602,.T.);
#14089=EDGE_CURVE('',#10982,#10980,#1355,.T.);
#14090=EDGE_CURVE('',#10983,#10981,#1356,.T.);
#14091=EDGE_CURVE('',#10984,#10985,#6603,.T.);
#14092=EDGE_CURVE('',#10984,#10982,#1357,.T.);
#14093=EDGE_CURVE('',#10985,#10983,#1358,.T.);
#14094=EDGE_CURVE('',#10986,#10987,#6604,.T.);
#14095=EDGE_CURVE('',#10986,#10984,#1359,.T.);
#14096=EDGE_CURVE('',#10987,#10985,#1360,.T.);
#14097=EDGE_CURVE('',#10988,#10989,#6605,.T.);
#14098=EDGE_CURVE('',#10988,#10986,#1361,.T.);
#14099=EDGE_CURVE('',#10989,#10987,#1362,.T.);
#14100=EDGE_CURVE('',#10990,#10991,#6606,.T.);
#14101=EDGE_CURVE('',#10990,#10988,#1363,.T.);
#14102=EDGE_CURVE('',#10991,#10989,#1364,.T.);
#14103=EDGE_CURVE('',#10992,#10993,#6607,.T.);
#14104=EDGE_CURVE('',#10992,#10990,#1365,.T.);
#14105=EDGE_CURVE('',#10993,#10991,#1366,.T.);
#14106=EDGE_CURVE('',#10950,#10947,#1367,.T.);
#14107=EDGE_CURVE('',#10994,#10947,#9050,.T.);
#14108=EDGE_CURVE('',#10994,#10951,#1368,.T.);
#14109=EDGE_CURVE('',#10946,#10994,#1369,.T.);
#14110=EDGE_CURVE('',#10995,#10902,#1370,.T.);
#14111=EDGE_CURVE('',#10995,#10993,#1371,.T.);
#14112=EDGE_CURVE('',#10899,#10996,#1372,.T.);
#14113=EDGE_CURVE('',#10996,#10995,#9051,.T.);
#14114=EDGE_CURVE('',#10996,#10992,#1373,.T.);
#14115=EDGE_CURVE('',#10945,#10994,#9052,.T.);
#14116=EDGE_CURVE('',#10945,#10997,#9053,.T.);
#14117=EDGE_CURVE('',#10997,#10997,#9054,.T.);
#14118=EDGE_CURVE('',#10998,#10998,#9055,.T.);
#14119=EDGE_CURVE('',#10999,#11000,#6608,.T.);
#14120=EDGE_CURVE('',#11000,#11000,#9056,.T.);
#14121=EDGE_CURVE('',#11001,#11002,#6609,.T.);
#14122=EDGE_CURVE('',#11001,#11003,#6610,.T.);
#14123=EDGE_CURVE('',#11003,#11004,#6611,.T.);
#14124=EDGE_CURVE('',#11002,#11004,#6612,.T.);
#14125=EDGE_CURVE('',#11005,#11001,#6613,.T.);
#14126=EDGE_CURVE('',#11005,#11006,#6614,.T.);
#14127=EDGE_CURVE('',#11006,#11003,#6615,.T.);
#14128=EDGE_CURVE('',#11007,#11005,#6616,.T.);
#14129=EDGE_CURVE('',#11007,#11008,#6617,.T.);
#14130=EDGE_CURVE('',#11008,#11006,#6618,.T.);
#14131=EDGE_CURVE('',#11009,#11007,#6619,.T.);
#14132=EDGE_CURVE('',#11009,#11010,#6620,.T.);
#14133=EDGE_CURVE('',#11010,#11008,#6621,.T.);
#14134=EDGE_CURVE('',#11011,#11009,#6622,.T.);
#14135=EDGE_CURVE('',#11011,#11012,#6623,.T.);
#14136=EDGE_CURVE('',#11012,#11010,#6624,.T.);
#14137=EDGE_CURVE('',#11002,#11011,#6625,.T.);
#14138=EDGE_CURVE('',#11004,#11012,#6626,.T.);
#14139=EDGE_CURVE('',#11013,#11014,#6627,.T.);
#14140=EDGE_CURVE('',#11013,#11015,#6628,.T.);
#14141=EDGE_CURVE('',#11016,#11015,#6629,.T.);
#14142=EDGE_CURVE('',#11014,#11016,#6630,.T.);
#14143=EDGE_CURVE('',#11014,#11017,#9057,.T.);
#14144=EDGE_CURVE('',#11016,#11017,#6631,.T.);
#14145=EDGE_CURVE('',#11017,#11018,#6632,.T.);
#14146=EDGE_CURVE('',#11015,#11018,#6633,.T.);
#14147=EDGE_CURVE('',#11018,#11013,#9058,.T.);
#14148=EDGE_CURVE('',#11019,#11020,#6634,.T.);
#14149=EDGE_CURVE('',#11019,#11021,#6635,.T.);
#14150=EDGE_CURVE('',#11022,#11021,#6636,.T.);
#14151=EDGE_CURVE('',#11020,#11022,#6637,.T.);
#14152=EDGE_CURVE('',#11020,#11023,#9059,.T.);
#14153=EDGE_CURVE('',#11022,#11023,#6638,.T.);
#14154=EDGE_CURVE('',#11023,#11024,#6639,.T.);
#14155=EDGE_CURVE('',#11021,#11024,#6640,.T.);
#14156=EDGE_CURVE('',#11024,#11019,#9060,.T.);
#14157=EDGE_CURVE('',#11025,#11026,#6641,.T.);
#14158=EDGE_CURVE('',#11025,#11027,#6642,.T.);
#14159=EDGE_CURVE('',#11028,#11027,#6643,.T.);
#14160=EDGE_CURVE('',#11026,#11028,#6644,.T.);
#14161=EDGE_CURVE('',#11026,#11029,#9061,.T.);
#14162=EDGE_CURVE('',#11028,#11029,#6645,.T.);
#14163=EDGE_CURVE('',#11029,#11030,#6646,.T.);
#14164=EDGE_CURVE('',#11027,#11030,#6647,.T.);
#14165=EDGE_CURVE('',#11030,#11025,#9062,.T.);
#14166=EDGE_CURVE('',#11031,#11032,#6648,.T.);
#14167=EDGE_CURVE('',#11031,#11033,#6649,.T.);
#14168=EDGE_CURVE('',#11034,#11033,#6650,.T.);
#14169=EDGE_CURVE('',#11032,#11034,#6651,.T.);
#14170=EDGE_CURVE('',#11032,#11035,#9063,.T.);
#14171=EDGE_CURVE('',#11034,#11035,#6652,.T.);
#14172=EDGE_CURVE('',#11035,#11036,#6653,.T.);
#14173=EDGE_CURVE('',#11033,#11036,#6654,.T.);
#14174=EDGE_CURVE('',#11036,#11031,#9064,.T.);
#14175=EDGE_CURVE('',#11037,#11038,#6655,.T.);
#14176=EDGE_CURVE('',#11037,#11039,#6656,.T.);
#14177=EDGE_CURVE('',#11040,#11039,#6657,.T.);
#14178=EDGE_CURVE('',#11038,#11040,#6658,.T.);
#14179=EDGE_CURVE('',#11038,#11041,#9065,.T.);
#14180=EDGE_CURVE('',#11040,#11041,#6659,.T.);
#14181=EDGE_CURVE('',#11041,#11042,#6660,.T.);
#14182=EDGE_CURVE('',#11039,#11042,#6661,.T.);
#14183=EDGE_CURVE('',#11042,#11037,#9066,.T.);
#14184=EDGE_CURVE('',#11043,#11044,#6662,.T.);
#14185=EDGE_CURVE('',#11043,#11045,#6663,.T.);
#14186=EDGE_CURVE('',#11046,#11045,#6664,.T.);
#14187=EDGE_CURVE('',#11044,#11046,#6665,.T.);
#14188=EDGE_CURVE('',#11044,#11047,#9067,.T.);
#14189=EDGE_CURVE('',#11046,#11047,#6666,.T.);
#14190=EDGE_CURVE('',#11047,#11048,#6667,.T.);
#14191=EDGE_CURVE('',#11045,#11048,#6668,.T.);
#14192=EDGE_CURVE('',#11048,#11043,#9068,.T.);
#14193=EDGE_CURVE('',#11049,#11050,#6669,.T.);
#14194=EDGE_CURVE('',#11049,#11051,#6670,.T.);
#14195=EDGE_CURVE('',#11052,#11051,#6671,.T.);
#14196=EDGE_CURVE('',#11050,#11052,#6672,.T.);
#14197=EDGE_CURVE('',#11050,#11053,#9069,.T.);
#14198=EDGE_CURVE('',#11052,#11053,#6673,.T.);
#14199=EDGE_CURVE('',#11053,#11054,#6674,.T.);
#14200=EDGE_CURVE('',#11051,#11054,#6675,.T.);
#14201=EDGE_CURVE('',#11054,#11049,#9070,.T.);
#14202=EDGE_CURVE('',#11055,#11056,#6676,.T.);
#14203=EDGE_CURVE('',#11055,#11057,#6677,.T.);
#14204=EDGE_CURVE('',#11058,#11057,#6678,.T.);
#14205=EDGE_CURVE('',#11056,#11058,#6679,.T.);
#14206=EDGE_CURVE('',#11056,#11059,#9071,.T.);
#14207=EDGE_CURVE('',#11058,#11059,#6680,.T.);
#14208=EDGE_CURVE('',#11059,#11060,#6681,.T.);
#14209=EDGE_CURVE('',#11057,#11060,#6682,.T.);
#14210=EDGE_CURVE('',#11060,#11055,#9072,.T.);
#14211=EDGE_CURVE('',#11061,#11062,#6683,.T.);
#14212=EDGE_CURVE('',#11061,#11063,#6684,.T.);
#14213=EDGE_CURVE('',#11064,#11063,#6685,.T.);
#14214=EDGE_CURVE('',#11062,#11064,#6686,.T.);
#14215=EDGE_CURVE('',#11062,#11065,#9073,.T.);
#14216=EDGE_CURVE('',#11064,#11066,#6687,.T.);
#14217=EDGE_CURVE('',#11065,#11066,#9074,.T.);
#14218=EDGE_CURVE('',#11066,#11067,#6688,.T.);
#14219=EDGE_CURVE('',#11063,#11067,#6689,.T.);
#14220=EDGE_CURVE('',#11067,#11068,#9075,.T.);
#14221=EDGE_CURVE('',#11068,#11061,#9076,.T.);
#14222=EDGE_CURVE('',#11069,#11070,#6690,.T.);
#14223=EDGE_CURVE('',#11069,#11071,#6691,.T.);
#14224=EDGE_CURVE('',#11072,#11071,#6692,.T.);
#14225=EDGE_CURVE('',#11070,#11072,#6693,.T.);
#14226=EDGE_CURVE('',#11070,#11073,#9077,.T.);
#14227=EDGE_CURVE('',#11072,#11073,#6694,.T.);
#14228=EDGE_CURVE('',#11073,#11074,#6695,.T.);
#14229=EDGE_CURVE('',#11071,#11074,#6696,.T.);
#14230=EDGE_CURVE('',#11074,#11069,#9078,.T.);
#14231=EDGE_CURVE('',#11075,#11076,#6697,.T.);
#14232=EDGE_CURVE('',#11075,#11077,#6698,.T.);
#14233=EDGE_CURVE('',#11078,#11077,#6699,.T.);
#14234=EDGE_CURVE('',#11076,#11078,#6700,.T.);
#14235=EDGE_CURVE('',#11076,#11079,#9079,.T.);
#14236=EDGE_CURVE('',#11078,#11079,#6701,.T.);
#14237=EDGE_CURVE('',#11079,#11080,#6702,.T.);
#14238=EDGE_CURVE('',#11077,#11080,#6703,.T.);
#14239=EDGE_CURVE('',#11080,#11075,#9080,.T.);
#14240=EDGE_CURVE('',#11081,#11082,#6704,.T.);
#14241=EDGE_CURVE('',#11081,#11083,#6705,.T.);
#14242=EDGE_CURVE('',#11084,#11083,#6706,.T.);
#14243=EDGE_CURVE('',#11082,#11084,#6707,.T.);
#14244=EDGE_CURVE('',#11082,#11085,#9081,.T.);
#14245=EDGE_CURVE('',#11084,#11085,#6708,.T.);
#14246=EDGE_CURVE('',#11085,#11086,#6709,.T.);
#14247=EDGE_CURVE('',#11083,#11086,#6710,.T.);
#14248=EDGE_CURVE('',#11086,#11081,#9082,.T.);
#14249=EDGE_CURVE('',#11087,#11088,#6711,.T.);
#14250=EDGE_CURVE('',#11087,#11089,#6712,.T.);
#14251=EDGE_CURVE('',#11090,#11089,#6713,.T.);
#14252=EDGE_CURVE('',#11088,#11090,#6714,.T.);
#14253=EDGE_CURVE('',#11088,#11091,#9083,.T.);
#14254=EDGE_CURVE('',#11090,#11091,#6715,.T.);
#14255=EDGE_CURVE('',#11091,#11092,#6716,.T.);
#14256=EDGE_CURVE('',#11089,#11092,#6717,.T.);
#14257=EDGE_CURVE('',#11092,#11087,#9084,.T.);
#14258=EDGE_CURVE('',#11093,#11094,#6718,.T.);
#14259=EDGE_CURVE('',#11093,#11095,#6719,.T.);
#14260=EDGE_CURVE('',#11096,#11095,#6720,.T.);
#14261=EDGE_CURVE('',#11094,#11096,#6721,.T.);
#14262=EDGE_CURVE('',#11094,#11097,#9085,.T.);
#14263=EDGE_CURVE('',#11096,#11097,#6722,.T.);
#14264=EDGE_CURVE('',#11097,#11098,#6723,.T.);
#14265=EDGE_CURVE('',#11095,#11098,#6724,.T.);
#14266=EDGE_CURVE('',#11098,#11093,#9086,.T.);
#14267=EDGE_CURVE('',#11099,#11100,#6725,.T.);
#14268=EDGE_CURVE('',#11099,#11101,#6726,.T.);
#14269=EDGE_CURVE('',#11102,#11101,#6727,.T.);
#14270=EDGE_CURVE('',#11100,#11102,#6728,.T.);
#14271=EDGE_CURVE('',#11100,#11103,#9087,.T.);
#14272=EDGE_CURVE('',#11102,#11103,#6729,.T.);
#14273=EDGE_CURVE('',#11103,#11104,#6730,.T.);
#14274=EDGE_CURVE('',#11101,#11104,#6731,.T.);
#14275=EDGE_CURVE('',#11104,#11099,#9088,.T.);
#14276=EDGE_CURVE('',#11105,#11106,#6732,.T.);
#14277=EDGE_CURVE('',#11105,#11107,#6733,.T.);
#14278=EDGE_CURVE('',#11108,#11107,#6734,.T.);
#14279=EDGE_CURVE('',#11106,#11108,#6735,.T.);
#14280=EDGE_CURVE('',#11106,#11109,#9089,.T.);
#14281=EDGE_CURVE('',#11108,#11109,#6736,.T.);
#14282=EDGE_CURVE('',#11109,#11110,#6737,.T.);
#14283=EDGE_CURVE('',#11107,#11110,#6738,.T.);
#14284=EDGE_CURVE('',#11110,#11105,#9090,.T.);
#14285=EDGE_CURVE('',#11111,#11112,#6739,.T.);
#14286=EDGE_CURVE('',#11111,#11113,#6740,.T.);
#14287=EDGE_CURVE('',#11114,#11113,#6741,.T.);
#14288=EDGE_CURVE('',#11112,#11114,#6742,.T.);
#14289=EDGE_CURVE('',#11112,#11115,#9091,.T.);
#14290=EDGE_CURVE('',#11114,#11115,#6743,.T.);
#14291=EDGE_CURVE('',#11115,#11116,#6744,.T.);
#14292=EDGE_CURVE('',#11113,#11116,#6745,.T.);
#14293=EDGE_CURVE('',#11116,#11111,#9092,.T.);
#14294=EDGE_CURVE('',#11117,#11118,#6746,.T.);
#14295=EDGE_CURVE('',#11117,#11119,#6747,.T.);
#14296=EDGE_CURVE('',#11120,#11119,#6748,.T.);
#14297=EDGE_CURVE('',#11118,#11120,#6749,.T.);
#14298=EDGE_CURVE('',#11118,#11121,#9093,.T.);
#14299=EDGE_CURVE('',#11120,#11121,#6750,.T.);
#14300=EDGE_CURVE('',#11121,#11122,#6751,.T.);
#14301=EDGE_CURVE('',#11119,#11122,#6752,.T.);
#14302=EDGE_CURVE('',#11122,#11117,#9094,.T.);
#14303=EDGE_CURVE('',#11123,#11124,#6753,.T.);
#14304=EDGE_CURVE('',#11123,#11125,#6754,.T.);
#14305=EDGE_CURVE('',#11126,#11125,#6755,.T.);
#14306=EDGE_CURVE('',#11124,#11126,#6756,.T.);
#14307=EDGE_CURVE('',#11124,#11127,#9095,.T.);
#14308=EDGE_CURVE('',#11126,#11127,#6757,.T.);
#14309=EDGE_CURVE('',#11127,#11128,#6758,.T.);
#14310=EDGE_CURVE('',#11125,#11128,#6759,.T.);
#14311=EDGE_CURVE('',#11128,#11123,#9096,.T.);
#14312=EDGE_CURVE('',#11129,#11130,#6760,.T.);
#14313=EDGE_CURVE('',#11129,#11131,#6761,.T.);
#14314=EDGE_CURVE('',#11132,#11131,#6762,.T.);
#14315=EDGE_CURVE('',#11130,#11132,#6763,.T.);
#14316=EDGE_CURVE('',#11130,#11133,#9097,.T.);
#14317=EDGE_CURVE('',#11132,#11133,#6764,.T.);
#14318=EDGE_CURVE('',#11133,#11134,#6765,.T.);
#14319=EDGE_CURVE('',#11131,#11134,#6766,.T.);
#14320=EDGE_CURVE('',#11134,#11129,#9098,.T.);
#14321=EDGE_CURVE('',#11135,#11136,#6767,.T.);
#14322=EDGE_CURVE('',#11135,#11137,#6768,.T.);
#14323=EDGE_CURVE('',#11138,#11137,#6769,.T.);
#14324=EDGE_CURVE('',#11136,#11138,#6770,.T.);
#14325=EDGE_CURVE('',#11136,#11139,#9099,.T.);
#14326=EDGE_CURVE('',#11138,#11139,#6771,.T.);
#14327=EDGE_CURVE('',#11139,#11140,#6772,.T.);
#14328=EDGE_CURVE('',#11137,#11140,#6773,.T.);
#14329=EDGE_CURVE('',#11140,#11135,#9100,.T.);
#14330=EDGE_CURVE('',#11141,#11142,#6774,.T.);
#14331=EDGE_CURVE('',#11141,#11143,#6775,.T.);
#14332=EDGE_CURVE('',#11144,#11143,#6776,.T.);
#14333=EDGE_CURVE('',#11142,#11144,#6777,.T.);
#14334=EDGE_CURVE('',#11142,#11145,#9101,.T.);
#14335=EDGE_CURVE('',#11144,#11145,#6778,.T.);
#14336=EDGE_CURVE('',#11145,#11146,#6779,.T.);
#14337=EDGE_CURVE('',#11143,#11146,#6780,.T.);
#14338=EDGE_CURVE('',#11146,#11141,#9102,.T.);
#14339=EDGE_CURVE('',#11147,#11148,#6781,.T.);
#14340=EDGE_CURVE('',#11147,#11149,#6782,.T.);
#14341=EDGE_CURVE('',#11150,#11149,#6783,.T.);
#14342=EDGE_CURVE('',#11148,#11150,#6784,.T.);
#14343=EDGE_CURVE('',#11148,#11151,#9103,.T.);
#14344=EDGE_CURVE('',#11150,#11151,#6785,.T.);
#14345=EDGE_CURVE('',#11151,#11152,#6786,.T.);
#14346=EDGE_CURVE('',#11149,#11152,#6787,.T.);
#14347=EDGE_CURVE('',#11152,#11147,#9104,.T.);
#14348=EDGE_CURVE('',#11153,#11154,#6788,.T.);
#14349=EDGE_CURVE('',#11153,#11155,#6789,.T.);
#14350=EDGE_CURVE('',#11156,#11155,#6790,.T.);
#14351=EDGE_CURVE('',#11154,#11156,#6791,.T.);
#14352=EDGE_CURVE('',#11154,#11157,#9105,.T.);
#14353=EDGE_CURVE('',#11156,#11157,#6792,.T.);
#14354=EDGE_CURVE('',#11157,#11158,#6793,.T.);
#14355=EDGE_CURVE('',#11155,#11158,#6794,.T.);
#14356=EDGE_CURVE('',#11158,#11153,#9106,.T.);
#14357=EDGE_CURVE('',#11159,#11160,#6795,.T.);
#14358=EDGE_CURVE('',#11159,#11161,#6796,.T.);
#14359=EDGE_CURVE('',#11162,#11161,#6797,.T.);
#14360=EDGE_CURVE('',#11160,#11162,#6798,.T.);
#14361=EDGE_CURVE('',#11160,#11163,#9107,.T.);
#14362=EDGE_CURVE('',#11162,#11163,#6799,.T.);
#14363=EDGE_CURVE('',#11163,#11164,#6800,.T.);
#14364=EDGE_CURVE('',#11161,#11164,#6801,.T.);
#14365=EDGE_CURVE('',#11164,#11159,#9108,.T.);
#14366=EDGE_CURVE('',#11165,#11166,#6802,.T.);
#14367=EDGE_CURVE('',#11165,#11167,#6803,.T.);
#14368=EDGE_CURVE('',#11168,#11167,#6804,.T.);
#14369=EDGE_CURVE('',#11166,#11168,#6805,.T.);
#14370=EDGE_CURVE('',#11166,#11169,#9109,.T.);
#14371=EDGE_CURVE('',#11168,#11169,#6806,.T.);
#14372=EDGE_CURVE('',#11169,#11170,#6807,.T.);
#14373=EDGE_CURVE('',#11167,#11170,#6808,.T.);
#14374=EDGE_CURVE('',#11170,#11165,#9110,.T.);
#14375=EDGE_CURVE('',#11171,#11172,#9111,.T.);
#14376=EDGE_CURVE('',#11171,#11173,#6809,.T.);
#14377=EDGE_CURVE('',#11173,#11172,#6810,.T.);
#14378=EDGE_CURVE('',#11174,#11171,#6811,.T.);
#14379=EDGE_CURVE('',#11174,#11175,#6812,.T.);
#14380=EDGE_CURVE('',#11173,#11175,#6813,.T.);
#14381=EDGE_CURVE('',#11172,#11176,#6814,.T.);
#14382=EDGE_CURVE('',#11175,#11176,#6815,.T.);
#14383=EDGE_CURVE('',#11176,#11174,#9112,.T.);
#14384=EDGE_CURVE('',#11177,#11178,#6816,.T.);
#14385=EDGE_CURVE('',#11177,#11179,#6817,.T.);
#14386=EDGE_CURVE('',#11180,#11179,#6818,.T.);
#14387=EDGE_CURVE('',#11178,#11180,#6819,.T.);
#14388=EDGE_CURVE('',#11178,#11181,#9113,.T.);
#14389=EDGE_CURVE('',#11180,#11181,#6820,.T.);
#14390=EDGE_CURVE('',#11181,#11182,#6821,.T.);
#14391=EDGE_CURVE('',#11179,#11182,#6822,.T.);
#14392=EDGE_CURVE('',#11182,#11177,#9114,.T.);
#14393=EDGE_CURVE('',#11183,#11184,#6823,.T.);
#14394=EDGE_CURVE('',#11183,#11185,#6824,.T.);
#14395=EDGE_CURVE('',#11186,#11185,#6825,.T.);
#14396=EDGE_CURVE('',#11184,#11186,#6826,.T.);
#14397=EDGE_CURVE('',#11184,#11187,#9115,.T.);
#14398=EDGE_CURVE('',#11186,#11187,#6827,.T.);
#14399=EDGE_CURVE('',#11187,#11188,#6828,.T.);
#14400=EDGE_CURVE('',#11185,#11188,#6829,.T.);
#14401=EDGE_CURVE('',#11188,#11183,#9116,.T.);
#14402=EDGE_CURVE('',#11189,#11190,#6830,.T.);
#14403=EDGE_CURVE('',#11189,#11191,#6831,.T.);
#14404=EDGE_CURVE('',#11192,#11191,#6832,.T.);
#14405=EDGE_CURVE('',#11190,#11192,#6833,.T.);
#14406=EDGE_CURVE('',#11190,#11193,#9117,.T.);
#14407=EDGE_CURVE('',#11192,#11193,#6834,.T.);
#14408=EDGE_CURVE('',#11193,#11194,#6835,.T.);
#14409=EDGE_CURVE('',#11191,#11194,#6836,.T.);
#14410=EDGE_CURVE('',#11194,#11189,#9118,.T.);
#14411=EDGE_CURVE('',#11195,#11196,#6837,.T.);
#14412=EDGE_CURVE('',#11195,#11197,#6838,.T.);
#14413=EDGE_CURVE('',#11198,#11197,#6839,.T.);
#14414=EDGE_CURVE('',#11196,#11198,#6840,.T.);
#14415=EDGE_CURVE('',#11196,#11199,#9119,.T.);
#14416=EDGE_CURVE('',#11198,#11199,#6841,.T.);
#14417=EDGE_CURVE('',#11199,#11200,#6842,.T.);
#14418=EDGE_CURVE('',#11197,#11200,#6843,.T.);
#14419=EDGE_CURVE('',#11200,#11195,#9120,.T.);
#14420=EDGE_CURVE('',#11201,#11202,#6844,.T.);
#14421=EDGE_CURVE('',#11201,#11203,#6845,.T.);
#14422=EDGE_CURVE('',#11204,#11203,#6846,.T.);
#14423=EDGE_CURVE('',#11202,#11204,#6847,.T.);
#14424=EDGE_CURVE('',#11202,#11205,#9121,.T.);
#14425=EDGE_CURVE('',#11204,#11205,#6848,.T.);
#14426=EDGE_CURVE('',#11205,#11206,#6849,.T.);
#14427=EDGE_CURVE('',#11203,#11206,#6850,.T.);
#14428=EDGE_CURVE('',#11206,#11201,#9122,.T.);
#14429=EDGE_CURVE('',#11207,#11208,#6851,.T.);
#14430=EDGE_CURVE('',#11207,#11209,#6852,.T.);
#14431=EDGE_CURVE('',#11210,#11209,#6853,.T.);
#14432=EDGE_CURVE('',#11208,#11210,#6854,.T.);
#14433=EDGE_CURVE('',#11208,#11211,#9123,.T.);
#14434=EDGE_CURVE('',#11210,#11211,#6855,.T.);
#14435=EDGE_CURVE('',#11211,#11212,#6856,.T.);
#14436=EDGE_CURVE('',#11209,#11212,#6857,.T.);
#14437=EDGE_CURVE('',#11212,#11207,#9124,.T.);
#14438=EDGE_CURVE('',#11213,#11214,#6858,.T.);
#14439=EDGE_CURVE('',#11213,#11215,#6859,.T.);
#14440=EDGE_CURVE('',#11216,#11215,#6860,.T.);
#14441=EDGE_CURVE('',#11214,#11216,#6861,.T.);
#14442=EDGE_CURVE('',#11214,#11217,#9125,.T.);
#14443=EDGE_CURVE('',#11216,#11217,#6862,.T.);
#14444=EDGE_CURVE('',#11217,#11218,#6863,.T.);
#14445=EDGE_CURVE('',#11215,#11218,#6864,.T.);
#14446=EDGE_CURVE('',#11218,#11213,#9126,.T.);
#14447=EDGE_CURVE('',#11219,#11220,#6865,.T.);
#14448=EDGE_CURVE('',#11219,#11221,#6866,.T.);
#14449=EDGE_CURVE('',#11222,#11221,#6867,.T.);
#14450=EDGE_CURVE('',#11220,#11222,#6868,.T.);
#14451=EDGE_CURVE('',#11220,#11223,#9127,.T.);
#14452=EDGE_CURVE('',#11222,#11223,#6869,.T.);
#14453=EDGE_CURVE('',#11223,#11224,#6870,.T.);
#14454=EDGE_CURVE('',#11221,#11224,#6871,.T.);
#14455=EDGE_CURVE('',#11224,#11219,#9128,.T.);
#14456=EDGE_CURVE('',#11225,#11226,#6872,.T.);
#14457=EDGE_CURVE('',#11225,#11227,#6873,.T.);
#14458=EDGE_CURVE('',#11228,#11227,#6874,.T.);
#14459=EDGE_CURVE('',#11226,#11228,#6875,.T.);
#14460=EDGE_CURVE('',#11226,#11229,#9129,.T.);
#14461=EDGE_CURVE('',#11228,#11229,#6876,.T.);
#14462=EDGE_CURVE('',#11229,#11230,#6877,.T.);
#14463=EDGE_CURVE('',#11227,#11230,#6878,.T.);
#14464=EDGE_CURVE('',#11230,#11225,#9130,.T.);
#14465=EDGE_CURVE('',#11231,#11231,#9131,.T.);
#14466=EDGE_CURVE('',#10901,#11231,#6879,.T.);
#14467=EDGE_CURVE('',#11232,#11232,#9132,.T.);
#14468=EDGE_CURVE('',#11232,#10998,#6880,.T.);
#14469=EDGE_CURVE('',#11223,#11014,#9133,.T.);
#14470=EDGE_CURVE('',#11023,#11220,#9134,.T.);
#14471=EDGE_CURVE('',#11217,#11020,#9135,.T.);
#14472=EDGE_CURVE('',#11029,#11214,#9136,.T.);
#14473=EDGE_CURVE('',#11211,#11026,#9137,.T.);
#14474=EDGE_CURVE('',#11035,#11208,#9138,.T.);
#14475=EDGE_CURVE('',#11205,#11032,#9139,.T.);
#14476=EDGE_CURVE('',#11041,#11202,#9140,.T.);
#14477=EDGE_CURVE('',#11199,#11038,#9141,.T.);
#14478=EDGE_CURVE('',#11047,#11196,#9142,.T.);
#14479=EDGE_CURVE('',#11193,#11044,#9143,.T.);
#14480=EDGE_CURVE('',#11053,#11190,#9144,.T.);
#14481=EDGE_CURVE('',#11187,#11050,#9145,.T.);
#14482=EDGE_CURVE('',#11059,#11184,#9146,.T.);
#14483=EDGE_CURVE('',#11181,#11056,#9147,.T.);
#14484=EDGE_CURVE('',#11066,#11178,#9148,.T.);
#14485=EDGE_CURVE('',#11068,#11232,#6881,.T.);
#14486=EDGE_CURVE('',#11073,#11062,#9149,.T.);
#14487=EDGE_CURVE('',#11169,#11070,#9150,.T.);
#14488=EDGE_CURVE('',#11079,#11166,#9151,.T.);
#14489=EDGE_CURVE('',#11163,#11076,#9152,.T.);
#14490=EDGE_CURVE('',#11085,#11160,#9153,.T.);
#14491=EDGE_CURVE('',#11157,#11082,#9154,.T.);
#14492=EDGE_CURVE('',#11091,#11154,#9155,.T.);
#14493=EDGE_CURVE('',#11151,#11088,#9156,.T.);
#14494=EDGE_CURVE('',#11097,#11148,#9157,.T.);
#14495=EDGE_CURVE('',#11145,#11094,#9158,.T.);
#14496=EDGE_CURVE('',#11103,#11142,#9159,.T.);
#14497=EDGE_CURVE('',#11139,#11100,#9160,.T.);
#14498=EDGE_CURVE('',#11109,#11136,#9161,.T.);
#14499=EDGE_CURVE('',#11133,#11106,#9162,.T.);
#14500=EDGE_CURVE('',#11115,#11130,#9163,.T.);
#14501=EDGE_CURVE('',#11127,#11112,#9164,.T.);
#14502=EDGE_CURVE('',#11121,#11124,#9165,.T.);
#14503=EDGE_CURVE('',#11172,#11118,#9166,.T.);
#14504=EDGE_CURVE('',#11229,#11171,#9167,.T.);
#14505=EDGE_CURVE('',#11017,#11226,#9168,.T.);
#14506=EDGE_CURVE('',#11233,#11233,#9169,.T.);
#14507=EDGE_CURVE('',#11233,#11065,#6882,.T.);
#19922=ORIENTED_EDGE('',*,*,#13965,.F.);
#19923=ORIENTED_EDGE('',*,*,#13966,.T.);
#19924=ORIENTED_EDGE('',*,*,#13967,.T.);
#19925=ORIENTED_EDGE('',*,*,#13968,.T.);
#19926=ORIENTED_EDGE('',*,*,#13969,.T.);
#19927=ORIENTED_EDGE('',*,*,#13968,.F.);
#19928=ORIENTED_EDGE('',*,*,#13970,.T.);
#19929=ORIENTED_EDGE('',*,*,#13971,.T.);
#19930=ORIENTED_EDGE('',*,*,#13972,.F.);
#19931=ORIENTED_EDGE('',*,*,#13973,.T.);
#19932=ORIENTED_EDGE('',*,*,#13965,.T.);
#19933=ORIENTED_EDGE('',*,*,#13974,.T.);
#19934=ORIENTED_EDGE('',*,*,#13975,.F.);
#19935=ORIENTED_EDGE('',*,*,#13976,.T.);
#19936=ORIENTED_EDGE('',*,*,#13972,.T.);
#19937=ORIENTED_EDGE('',*,*,#13977,.T.);
#19938=ORIENTED_EDGE('',*,*,#13978,.F.);
#19939=ORIENTED_EDGE('',*,*,#13979,.T.);
#19940=ORIENTED_EDGE('',*,*,#13975,.T.);
#19941=ORIENTED_EDGE('',*,*,#13980,.T.);
#19942=ORIENTED_EDGE('',*,*,#13981,.F.);
#19943=ORIENTED_EDGE('',*,*,#13982,.T.);
#19944=ORIENTED_EDGE('',*,*,#13978,.T.);
#19945=ORIENTED_EDGE('',*,*,#13983,.T.);
#19946=ORIENTED_EDGE('',*,*,#13984,.F.);
#19947=ORIENTED_EDGE('',*,*,#13985,.T.);
#19948=ORIENTED_EDGE('',*,*,#13981,.T.);
#19949=ORIENTED_EDGE('',*,*,#13986,.T.);
#19950=ORIENTED_EDGE('',*,*,#13987,.F.);
#19951=ORIENTED_EDGE('',*,*,#13988,.T.);
#19952=ORIENTED_EDGE('',*,*,#13984,.T.);
#19953=ORIENTED_EDGE('',*,*,#13989,.T.);
#19954=ORIENTED_EDGE('',*,*,#13990,.F.);
#19955=ORIENTED_EDGE('',*,*,#13991,.T.);
#19956=ORIENTED_EDGE('',*,*,#13987,.T.);
#19957=ORIENTED_EDGE('',*,*,#13992,.T.);
#19958=ORIENTED_EDGE('',*,*,#13993,.F.);
#19959=ORIENTED_EDGE('',*,*,#13994,.T.);
#19960=ORIENTED_EDGE('',*,*,#13990,.T.);
#19961=ORIENTED_EDGE('',*,*,#13995,.T.);
#19962=ORIENTED_EDGE('',*,*,#13996,.F.);
#19963=ORIENTED_EDGE('',*,*,#13997,.T.);
#19964=ORIENTED_EDGE('',*,*,#13993,.T.);
#19965=ORIENTED_EDGE('',*,*,#13998,.T.);
#19966=ORIENTED_EDGE('',*,*,#13999,.F.);
#19967=ORIENTED_EDGE('',*,*,#14000,.T.);
#19968=ORIENTED_EDGE('',*,*,#13996,.T.);
#19969=ORIENTED_EDGE('',*,*,#14001,.T.);
#19970=ORIENTED_EDGE('',*,*,#14002,.F.);
#19971=ORIENTED_EDGE('',*,*,#14003,.T.);
#19972=ORIENTED_EDGE('',*,*,#13999,.T.);
#19973=ORIENTED_EDGE('',*,*,#14004,.T.);
#19974=ORIENTED_EDGE('',*,*,#14005,.F.);
#19975=ORIENTED_EDGE('',*,*,#14006,.T.);
#19976=ORIENTED_EDGE('',*,*,#14002,.T.);
#19977=ORIENTED_EDGE('',*,*,#14007,.T.);
#19978=ORIENTED_EDGE('',*,*,#14008,.F.);
#19979=ORIENTED_EDGE('',*,*,#14009,.T.);
#19980=ORIENTED_EDGE('',*,*,#14005,.T.);
#19981=ORIENTED_EDGE('',*,*,#14010,.T.);
#19982=ORIENTED_EDGE('',*,*,#14011,.F.);
#19983=ORIENTED_EDGE('',*,*,#14012,.T.);
#19984=ORIENTED_EDGE('',*,*,#14008,.T.);
#19985=ORIENTED_EDGE('',*,*,#14013,.T.);
#19986=ORIENTED_EDGE('',*,*,#14014,.F.);
#19987=ORIENTED_EDGE('',*,*,#14015,.T.);
#19988=ORIENTED_EDGE('',*,*,#14011,.T.);
#19989=ORIENTED_EDGE('',*,*,#14016,.T.);
#19990=ORIENTED_EDGE('',*,*,#14017,.F.);
#19991=ORIENTED_EDGE('',*,*,#14018,.T.);
#19992=ORIENTED_EDGE('',*,*,#14014,.T.);
#19993=ORIENTED_EDGE('',*,*,#14019,.T.);
#19994=ORIENTED_EDGE('',*,*,#14020,.F.);
#19995=ORIENTED_EDGE('',*,*,#14021,.T.);
#19996=ORIENTED_EDGE('',*,*,#14017,.T.);
#19997=ORIENTED_EDGE('',*,*,#14022,.T.);
#19998=ORIENTED_EDGE('',*,*,#14023,.F.);
#19999=ORIENTED_EDGE('',*,*,#14024,.T.);
#20000=ORIENTED_EDGE('',*,*,#14020,.T.);
#20001=ORIENTED_EDGE('',*,*,#14025,.T.);
#20002=ORIENTED_EDGE('',*,*,#14026,.F.);
#20003=ORIENTED_EDGE('',*,*,#14027,.T.);
#20004=ORIENTED_EDGE('',*,*,#14023,.T.);
#20005=ORIENTED_EDGE('',*,*,#14028,.T.);
#20006=ORIENTED_EDGE('',*,*,#14029,.F.);
#20007=ORIENTED_EDGE('',*,*,#14030,.T.);
#20008=ORIENTED_EDGE('',*,*,#14026,.T.);
#20009=ORIENTED_EDGE('',*,*,#14031,.T.);
#20010=ORIENTED_EDGE('',*,*,#14032,.F.);
#20011=ORIENTED_EDGE('',*,*,#14033,.T.);
#20012=ORIENTED_EDGE('',*,*,#14029,.T.);
#20013=ORIENTED_EDGE('',*,*,#14034,.T.);
#20014=ORIENTED_EDGE('',*,*,#14035,.F.);
#20015=ORIENTED_EDGE('',*,*,#14036,.F.);
#20016=ORIENTED_EDGE('',*,*,#14037,.T.);
#20017=ORIENTED_EDGE('',*,*,#14032,.T.);
#20018=ORIENTED_EDGE('',*,*,#14038,.T.);
#20019=ORIENTED_EDGE('',*,*,#14039,.F.);
#20020=ORIENTED_EDGE('',*,*,#14040,.T.);
#20021=ORIENTED_EDGE('',*,*,#14041,.F.);
#20022=ORIENTED_EDGE('',*,*,#14042,.F.);
#20023=ORIENTED_EDGE('',*,*,#14043,.F.);
#20024=ORIENTED_EDGE('',*,*,#14044,.T.);
#20025=ORIENTED_EDGE('',*,*,#14039,.T.);
#20026=ORIENTED_EDGE('',*,*,#14045,.F.);
#20027=ORIENTED_EDGE('',*,*,#14046,.F.);
#20028=ORIENTED_EDGE('',*,*,#14047,.T.);
#20029=ORIENTED_EDGE('',*,*,#14043,.T.);
#20030=ORIENTED_EDGE('',*,*,#14048,.F.);
#20031=ORIENTED_EDGE('',*,*,#14049,.F.);
#20032=ORIENTED_EDGE('',*,*,#14050,.T.);
#20033=ORIENTED_EDGE('',*,*,#14046,.T.);
#20034=ORIENTED_EDGE('',*,*,#14051,.F.);
#20035=ORIENTED_EDGE('',*,*,#14052,.F.);
#20036=ORIENTED_EDGE('',*,*,#14053,.T.);
#20037=ORIENTED_EDGE('',*,*,#14049,.T.);
#20038=ORIENTED_EDGE('',*,*,#14054,.F.);
#20039=ORIENTED_EDGE('',*,*,#14055,.F.);
#20040=ORIENTED_EDGE('',*,*,#14056,.T.);
#20041=ORIENTED_EDGE('',*,*,#14052,.T.);
#20042=ORIENTED_EDGE('',*,*,#14057,.F.);
#20043=ORIENTED_EDGE('',*,*,#14058,.F.);
#20044=ORIENTED_EDGE('',*,*,#14059,.T.);
#20045=ORIENTED_EDGE('',*,*,#14055,.T.);
#20046=ORIENTED_EDGE('',*,*,#14060,.F.);
#20047=ORIENTED_EDGE('',*,*,#14061,.F.);
#20048=ORIENTED_EDGE('',*,*,#14062,.T.);
#20049=ORIENTED_EDGE('',*,*,#14058,.T.);
#20050=ORIENTED_EDGE('',*,*,#14063,.F.);
#20051=ORIENTED_EDGE('',*,*,#14064,.F.);
#20052=ORIENTED_EDGE('',*,*,#14065,.T.);
#20053=ORIENTED_EDGE('',*,*,#14061,.T.);
#20054=ORIENTED_EDGE('',*,*,#14066,.F.);
#20055=ORIENTED_EDGE('',*,*,#14067,.F.);
#20056=ORIENTED_EDGE('',*,*,#14068,.T.);
#20057=ORIENTED_EDGE('',*,*,#14064,.T.);
#20058=ORIENTED_EDGE('',*,*,#14069,.F.);
#20059=ORIENTED_EDGE('',*,*,#14070,.F.);
#20060=ORIENTED_EDGE('',*,*,#14071,.T.);
#20061=ORIENTED_EDGE('',*,*,#14067,.T.);
#20062=ORIENTED_EDGE('',*,*,#14072,.F.);
#20063=ORIENTED_EDGE('',*,*,#14073,.F.);
#20064=ORIENTED_EDGE('',*,*,#14074,.T.);
#20065=ORIENTED_EDGE('',*,*,#14070,.T.);
#20066=ORIENTED_EDGE('',*,*,#14075,.F.);
#20067=ORIENTED_EDGE('',*,*,#14076,.F.);
#20068=ORIENTED_EDGE('',*,*,#14077,.T.);
#20069=ORIENTED_EDGE('',*,*,#14073,.T.);
#20070=ORIENTED_EDGE('',*,*,#14078,.F.);
#20071=ORIENTED_EDGE('',*,*,#14079,.F.);
#20072=ORIENTED_EDGE('',*,*,#14080,.T.);
#20073=ORIENTED_EDGE('',*,*,#14076,.T.);
#20074=ORIENTED_EDGE('',*,*,#14081,.F.);
#20075=ORIENTED_EDGE('',*,*,#14082,.F.);
#20076=ORIENTED_EDGE('',*,*,#14083,.T.);
#20077=ORIENTED_EDGE('',*,*,#14079,.T.);
#20078=ORIENTED_EDGE('',*,*,#14084,.F.);
#20079=ORIENTED_EDGE('',*,*,#14085,.F.);
#20080=ORIENTED_EDGE('',*,*,#14086,.T.);
#20081=ORIENTED_EDGE('',*,*,#14082,.T.);
#20082=ORIENTED_EDGE('',*,*,#14087,.F.);
#20083=ORIENTED_EDGE('',*,*,#14088,.F.);
#20084=ORIENTED_EDGE('',*,*,#14089,.T.);
#20085=ORIENTED_EDGE('',*,*,#14085,.T.);
#20086=ORIENTED_EDGE('',*,*,#14090,.F.);
#20087=ORIENTED_EDGE('',*,*,#14091,.F.);
#20088=ORIENTED_EDGE('',*,*,#14092,.T.);
#20089=ORIENTED_EDGE('',*,*,#14088,.T.);
#20090=ORIENTED_EDGE('',*,*,#14093,.F.);
#20091=ORIENTED_EDGE('',*,*,#14094,.F.);
#20092=ORIENTED_EDGE('',*,*,#14095,.T.);
#20093=ORIENTED_EDGE('',*,*,#14091,.T.);
#20094=ORIENTED_EDGE('',*,*,#14096,.F.);
#20095=ORIENTED_EDGE('',*,*,#14097,.F.);
#20096=ORIENTED_EDGE('',*,*,#14098,.T.);
#20097=ORIENTED_EDGE('',*,*,#14094,.T.);
#20098=ORIENTED_EDGE('',*,*,#14099,.F.);
#20099=ORIENTED_EDGE('',*,*,#14100,.F.);
#20100=ORIENTED_EDGE('',*,*,#14101,.T.);
#20101=ORIENTED_EDGE('',*,*,#14097,.T.);
#20102=ORIENTED_EDGE('',*,*,#14102,.F.);
#20103=ORIENTED_EDGE('',*,*,#14103,.F.);
#20104=ORIENTED_EDGE('',*,*,#14104,.T.);
#20105=ORIENTED_EDGE('',*,*,#14100,.T.);
#20106=ORIENTED_EDGE('',*,*,#14105,.F.);
#20107=ORIENTED_EDGE('',*,*,#14041,.T.);
#20108=ORIENTED_EDGE('',*,*,#14106,.T.);
#20109=ORIENTED_EDGE('',*,*,#14107,.F.);
#20110=ORIENTED_EDGE('',*,*,#14108,.T.);
#20111=ORIENTED_EDGE('',*,*,#14108,.F.);
#20112=ORIENTED_EDGE('',*,*,#14109,.F.);
#20113=ORIENTED_EDGE('',*,*,#14038,.F.);
#20114=ORIENTED_EDGE('',*,*,#14034,.F.);
#20115=ORIENTED_EDGE('',*,*,#14031,.F.);
#20116=ORIENTED_EDGE('',*,*,#14028,.F.);
#20117=ORIENTED_EDGE('',*,*,#14025,.F.);
#20118=ORIENTED_EDGE('',*,*,#14022,.F.);
#20119=ORIENTED_EDGE('',*,*,#14019,.F.);
#20120=ORIENTED_EDGE('',*,*,#14016,.F.);
#20121=ORIENTED_EDGE('',*,*,#14013,.F.);
#20122=ORIENTED_EDGE('',*,*,#14010,.F.);
#20123=ORIENTED_EDGE('',*,*,#14007,.F.);
#20124=ORIENTED_EDGE('',*,*,#14004,.F.);
#20125=ORIENTED_EDGE('',*,*,#14001,.F.);
#20126=ORIENTED_EDGE('',*,*,#13998,.F.);
#20127=ORIENTED_EDGE('',*,*,#13995,.F.);
#20128=ORIENTED_EDGE('',*,*,#13992,.F.);
#20129=ORIENTED_EDGE('',*,*,#13989,.F.);
#20130=ORIENTED_EDGE('',*,*,#13986,.F.);
#20131=ORIENTED_EDGE('',*,*,#13983,.F.);
#20132=ORIENTED_EDGE('',*,*,#13980,.F.);
#20133=ORIENTED_EDGE('',*,*,#13977,.F.);
#20134=ORIENTED_EDGE('',*,*,#13974,.F.);
#20135=ORIENTED_EDGE('',*,*,#13971,.F.);
#20136=ORIENTED_EDGE('',*,*,#14110,.F.);
#20137=ORIENTED_EDGE('',*,*,#14111,.T.);
#20138=ORIENTED_EDGE('',*,*,#14105,.T.);
#20139=ORIENTED_EDGE('',*,*,#14102,.T.);
#20140=ORIENTED_EDGE('',*,*,#14099,.T.);
#20141=ORIENTED_EDGE('',*,*,#14096,.T.);
#20142=ORIENTED_EDGE('',*,*,#14093,.T.);
#20143=ORIENTED_EDGE('',*,*,#14090,.T.);
#20144=ORIENTED_EDGE('',*,*,#14087,.T.);
#20145=ORIENTED_EDGE('',*,*,#14084,.T.);
#20146=ORIENTED_EDGE('',*,*,#14081,.T.);
#20147=ORIENTED_EDGE('',*,*,#14078,.T.);
#20148=ORIENTED_EDGE('',*,*,#14075,.T.);
#20149=ORIENTED_EDGE('',*,*,#14072,.T.);
#20150=ORIENTED_EDGE('',*,*,#14069,.T.);
#20151=ORIENTED_EDGE('',*,*,#14066,.T.);
#20152=ORIENTED_EDGE('',*,*,#14063,.T.);
#20153=ORIENTED_EDGE('',*,*,#14060,.T.);
#20154=ORIENTED_EDGE('',*,*,#14057,.T.);
#20155=ORIENTED_EDGE('',*,*,#14054,.T.);
#20156=ORIENTED_EDGE('',*,*,#14051,.T.);
#20157=ORIENTED_EDGE('',*,*,#14048,.T.);
#20158=ORIENTED_EDGE('',*,*,#14045,.T.);
#20159=ORIENTED_EDGE('',*,*,#14042,.T.);
#20160=ORIENTED_EDGE('',*,*,#13967,.F.);
#20161=ORIENTED_EDGE('',*,*,#14112,.T.);
#20162=ORIENTED_EDGE('',*,*,#14113,.T.);
#20163=ORIENTED_EDGE('',*,*,#14110,.T.);
#20164=ORIENTED_EDGE('',*,*,#13970,.F.);
#20165=ORIENTED_EDGE('',*,*,#14103,.T.);
#20166=ORIENTED_EDGE('',*,*,#14111,.F.);
#20167=ORIENTED_EDGE('',*,*,#14113,.F.);
#20168=ORIENTED_EDGE('',*,*,#14114,.T.);
#20169=ORIENTED_EDGE('',*,*,#14106,.F.);
#20170=ORIENTED_EDGE('',*,*,#14040,.F.);
#20171=ORIENTED_EDGE('',*,*,#14044,.F.);
#20172=ORIENTED_EDGE('',*,*,#14047,.F.);
#20173=ORIENTED_EDGE('',*,*,#14050,.F.);
#20174=ORIENTED_EDGE('',*,*,#14053,.F.);
#20175=ORIENTED_EDGE('',*,*,#14056,.F.);
#20176=ORIENTED_EDGE('',*,*,#14059,.F.);
#20177=ORIENTED_EDGE('',*,*,#14062,.F.);
#20178=ORIENTED_EDGE('',*,*,#14065,.F.);
#20179=ORIENTED_EDGE('',*,*,#14068,.F.);
#20180=ORIENTED_EDGE('',*,*,#14071,.F.);
#20181=ORIENTED_EDGE('',*,*,#14074,.F.);
#20182=ORIENTED_EDGE('',*,*,#14077,.F.);
#20183=ORIENTED_EDGE('',*,*,#14080,.F.);
#20184=ORIENTED_EDGE('',*,*,#14083,.F.);
#20185=ORIENTED_EDGE('',*,*,#14086,.F.);
#20186=ORIENTED_EDGE('',*,*,#14089,.F.);
#20187=ORIENTED_EDGE('',*,*,#14092,.F.);
#20188=ORIENTED_EDGE('',*,*,#14095,.F.);
#20189=ORIENTED_EDGE('',*,*,#14098,.F.);
#20190=ORIENTED_EDGE('',*,*,#14101,.F.);
#20191=ORIENTED_EDGE('',*,*,#14104,.F.);
#20192=ORIENTED_EDGE('',*,*,#14114,.F.);
#20193=ORIENTED_EDGE('',*,*,#14112,.F.);
#20194=ORIENTED_EDGE('',*,*,#13966,.F.);
#20195=ORIENTED_EDGE('',*,*,#13973,.F.);
#20196=ORIENTED_EDGE('',*,*,#13976,.F.);
#20197=ORIENTED_EDGE('',*,*,#13979,.F.);
#20198=ORIENTED_EDGE('',*,*,#13982,.F.);
#20199=ORIENTED_EDGE('',*,*,#13985,.F.);
#20200=ORIENTED_EDGE('',*,*,#13988,.F.);
#20201=ORIENTED_EDGE('',*,*,#13991,.F.);
#20202=ORIENTED_EDGE('',*,*,#13994,.F.);
#20203=ORIENTED_EDGE('',*,*,#13997,.F.);
#20204=ORIENTED_EDGE('',*,*,#14000,.F.);
#20205=ORIENTED_EDGE('',*,*,#14003,.F.);
#20206=ORIENTED_EDGE('',*,*,#14006,.F.);
#20207=ORIENTED_EDGE('',*,*,#14009,.F.);
#20208=ORIENTED_EDGE('',*,*,#14012,.F.);
#20209=ORIENTED_EDGE('',*,*,#14015,.F.);
#20210=ORIENTED_EDGE('',*,*,#14018,.F.);
#20211=ORIENTED_EDGE('',*,*,#14021,.F.);
#20212=ORIENTED_EDGE('',*,*,#14024,.F.);
#20213=ORIENTED_EDGE('',*,*,#14027,.F.);
#20214=ORIENTED_EDGE('',*,*,#14030,.F.);
#20215=ORIENTED_EDGE('',*,*,#14033,.F.);
#20216=ORIENTED_EDGE('',*,*,#14037,.F.);
#20217=ORIENTED_EDGE('',*,*,#14035,.T.);
#20218=ORIENTED_EDGE('',*,*,#14109,.T.);
#20219=ORIENTED_EDGE('',*,*,#14115,.F.);
#20220=ORIENTED_EDGE('',*,*,#14036,.T.);
#20221=ORIENTED_EDGE('',*,*,#14116,.T.);
#20222=ORIENTED_EDGE('',*,*,#14117,.T.);
#20223=ORIENTED_EDGE('',*,*,#14116,.F.);
#20224=ORIENTED_EDGE('',*,*,#14115,.T.);
#20225=ORIENTED_EDGE('',*,*,#14107,.T.);
#20226=ORIENTED_EDGE('',*,*,#14118,.F.);
#20227=ORIENTED_EDGE('',*,*,#14117,.F.);
#20228=ORIENTED_EDGE('',*,*,#14119,.T.);
#20229=ORIENTED_EDGE('',*,*,#14120,.F.);
#20230=ORIENTED_EDGE('',*,*,#14119,.F.);
#20231=ORIENTED_EDGE('',*,*,#14121,.F.);
#20232=ORIENTED_EDGE('',*,*,#14122,.T.);
#20233=ORIENTED_EDGE('',*,*,#14123,.T.);
#20234=ORIENTED_EDGE('',*,*,#14124,.F.);
#20235=ORIENTED_EDGE('',*,*,#14125,.F.);
#20236=ORIENTED_EDGE('',*,*,#14126,.T.);
#20237=ORIENTED_EDGE('',*,*,#14127,.T.);
#20238=ORIENTED_EDGE('',*,*,#14122,.F.);
#20239=ORIENTED_EDGE('',*,*,#14128,.F.);
#20240=ORIENTED_EDGE('',*,*,#14129,.T.);
#20241=ORIENTED_EDGE('',*,*,#14130,.T.);
#20242=ORIENTED_EDGE('',*,*,#14126,.F.);
#20243=ORIENTED_EDGE('',*,*,#14131,.F.);
#20244=ORIENTED_EDGE('',*,*,#14132,.T.);
#20245=ORIENTED_EDGE('',*,*,#14133,.T.);
#20246=ORIENTED_EDGE('',*,*,#14129,.F.);
#20247=ORIENTED_EDGE('',*,*,#14134,.F.);
#20248=ORIENTED_EDGE('',*,*,#14135,.T.);
#20249=ORIENTED_EDGE('',*,*,#14136,.T.);
#20250=ORIENTED_EDGE('',*,*,#14132,.F.);
#20251=ORIENTED_EDGE('',*,*,#14137,.F.);
#20252=ORIENTED_EDGE('',*,*,#14124,.T.);
#20253=ORIENTED_EDGE('',*,*,#14138,.T.);
#20254=ORIENTED_EDGE('',*,*,#14135,.F.);
#20255=ORIENTED_EDGE('',*,*,#14138,.F.);
#20256=ORIENTED_EDGE('',*,*,#14123,.F.);
#20257=ORIENTED_EDGE('',*,*,#14127,.F.);
#20258=ORIENTED_EDGE('',*,*,#14130,.F.);
#20259=ORIENTED_EDGE('',*,*,#14133,.F.);
#20260=ORIENTED_EDGE('',*,*,#14136,.F.);
#20261=ORIENTED_EDGE('',*,*,#14120,.T.);
#20262=ORIENTED_EDGE('',*,*,#14139,.F.);
#20263=ORIENTED_EDGE('',*,*,#14140,.T.);
#20264=ORIENTED_EDGE('',*,*,#14141,.F.);
#20265=ORIENTED_EDGE('',*,*,#14142,.F.);
#20266=ORIENTED_EDGE('',*,*,#14143,.F.);
#20267=ORIENTED_EDGE('',*,*,#14142,.T.);
#20268=ORIENTED_EDGE('',*,*,#14144,.T.);
#20269=ORIENTED_EDGE('',*,*,#14145,.F.);
#20270=ORIENTED_EDGE('',*,*,#14144,.F.);
#20271=ORIENTED_EDGE('',*,*,#14141,.T.);
#20272=ORIENTED_EDGE('',*,*,#14146,.T.);
#20273=ORIENTED_EDGE('',*,*,#14147,.F.);
#20274=ORIENTED_EDGE('',*,*,#14146,.F.);
#20275=ORIENTED_EDGE('',*,*,#14140,.F.);
#20276=ORIENTED_EDGE('',*,*,#14148,.F.);
#20277=ORIENTED_EDGE('',*,*,#14149,.T.);
#20278=ORIENTED_EDGE('',*,*,#14150,.F.);
#20279=ORIENTED_EDGE('',*,*,#14151,.F.);
#20280=ORIENTED_EDGE('',*,*,#14152,.F.);
#20281=ORIENTED_EDGE('',*,*,#14151,.T.);
#20282=ORIENTED_EDGE('',*,*,#14153,.T.);
#20283=ORIENTED_EDGE('',*,*,#14154,.F.);
#20284=ORIENTED_EDGE('',*,*,#14153,.F.);
#20285=ORIENTED_EDGE('',*,*,#14150,.T.);
#20286=ORIENTED_EDGE('',*,*,#14155,.T.);
#20287=ORIENTED_EDGE('',*,*,#14156,.F.);
#20288=ORIENTED_EDGE('',*,*,#14155,.F.);
#20289=ORIENTED_EDGE('',*,*,#14149,.F.);
#20290=ORIENTED_EDGE('',*,*,#14157,.F.);
#20291=ORIENTED_EDGE('',*,*,#14158,.T.);
#20292=ORIENTED_EDGE('',*,*,#14159,.F.);
#20293=ORIENTED_EDGE('',*,*,#14160,.F.);
#20294=ORIENTED_EDGE('',*,*,#14161,.F.);
#20295=ORIENTED_EDGE('',*,*,#14160,.T.);
#20296=ORIENTED_EDGE('',*,*,#14162,.T.);
#20297=ORIENTED_EDGE('',*,*,#14163,.F.);
#20298=ORIENTED_EDGE('',*,*,#14162,.F.);
#20299=ORIENTED_EDGE('',*,*,#14159,.T.);
#20300=ORIENTED_EDGE('',*,*,#14164,.T.);
#20301=ORIENTED_EDGE('',*,*,#14165,.F.);
#20302=ORIENTED_EDGE('',*,*,#14164,.F.);
#20303=ORIENTED_EDGE('',*,*,#14158,.F.);
#20304=ORIENTED_EDGE('',*,*,#14166,.F.);
#20305=ORIENTED_EDGE('',*,*,#14167,.T.);
#20306=ORIENTED_EDGE('',*,*,#14168,.F.);
#20307=ORIENTED_EDGE('',*,*,#14169,.F.);
#20308=ORIENTED_EDGE('',*,*,#14170,.F.);
#20309=ORIENTED_EDGE('',*,*,#14169,.T.);
#20310=ORIENTED_EDGE('',*,*,#14171,.T.);
#20311=ORIENTED_EDGE('',*,*,#14172,.F.);
#20312=ORIENTED_EDGE('',*,*,#14171,.F.);
#20313=ORIENTED_EDGE('',*,*,#14168,.T.);
#20314=ORIENTED_EDGE('',*,*,#14173,.T.);
#20315=ORIENTED_EDGE('',*,*,#14174,.F.);
#20316=ORIENTED_EDGE('',*,*,#14173,.F.);
#20317=ORIENTED_EDGE('',*,*,#14167,.F.);
#20318=ORIENTED_EDGE('',*,*,#14175,.F.);
#20319=ORIENTED_EDGE('',*,*,#14176,.T.);
#20320=ORIENTED_EDGE('',*,*,#14177,.F.);
#20321=ORIENTED_EDGE('',*,*,#14178,.F.);
#20322=ORIENTED_EDGE('',*,*,#14179,.F.);
#20323=ORIENTED_EDGE('',*,*,#14178,.T.);
#20324=ORIENTED_EDGE('',*,*,#14180,.T.);
#20325=ORIENTED_EDGE('',*,*,#14181,.F.);
#20326=ORIENTED_EDGE('',*,*,#14180,.F.);
#20327=ORIENTED_EDGE('',*,*,#14177,.T.);
#20328=ORIENTED_EDGE('',*,*,#14182,.T.);
#20329=ORIENTED_EDGE('',*,*,#14183,.F.);
#20330=ORIENTED_EDGE('',*,*,#14182,.F.);
#20331=ORIENTED_EDGE('',*,*,#14176,.F.);
#20332=ORIENTED_EDGE('',*,*,#14184,.F.);
#20333=ORIENTED_EDGE('',*,*,#14185,.T.);
#20334=ORIENTED_EDGE('',*,*,#14186,.F.);
#20335=ORIENTED_EDGE('',*,*,#14187,.F.);
#20336=ORIENTED_EDGE('',*,*,#14188,.F.);
#20337=ORIENTED_EDGE('',*,*,#14187,.T.);
#20338=ORIENTED_EDGE('',*,*,#14189,.T.);
#20339=ORIENTED_EDGE('',*,*,#14190,.F.);
#20340=ORIENTED_EDGE('',*,*,#14189,.F.);
#20341=ORIENTED_EDGE('',*,*,#14186,.T.);
#20342=ORIENTED_EDGE('',*,*,#14191,.T.);
#20343=ORIENTED_EDGE('',*,*,#14192,.F.);
#20344=ORIENTED_EDGE('',*,*,#14191,.F.);
#20345=ORIENTED_EDGE('',*,*,#14185,.F.);
#20346=ORIENTED_EDGE('',*,*,#14193,.F.);
#20347=ORIENTED_EDGE('',*,*,#14194,.T.);
#20348=ORIENTED_EDGE('',*,*,#14195,.F.);
#20349=ORIENTED_EDGE('',*,*,#14196,.F.);
#20350=ORIENTED_EDGE('',*,*,#14197,.F.);
#20351=ORIENTED_EDGE('',*,*,#14196,.T.);
#20352=ORIENTED_EDGE('',*,*,#14198,.T.);
#20353=ORIENTED_EDGE('',*,*,#14199,.F.);
#20354=ORIENTED_EDGE('',*,*,#14198,.F.);
#20355=ORIENTED_EDGE('',*,*,#14195,.T.);
#20356=ORIENTED_EDGE('',*,*,#14200,.T.);
#20357=ORIENTED_EDGE('',*,*,#14201,.F.);
#20358=ORIENTED_EDGE('',*,*,#14200,.F.);
#20359=ORIENTED_EDGE('',*,*,#14194,.F.);
#20360=ORIENTED_EDGE('',*,*,#14202,.F.);
#20361=ORIENTED_EDGE('',*,*,#14203,.T.);
#20362=ORIENTED_EDGE('',*,*,#14204,.F.);
#20363=ORIENTED_EDGE('',*,*,#14205,.F.);
#20364=ORIENTED_EDGE('',*,*,#14206,.F.);
#20365=ORIENTED_EDGE('',*,*,#14205,.T.);
#20366=ORIENTED_EDGE('',*,*,#14207,.T.);
#20367=ORIENTED_EDGE('',*,*,#14208,.F.);
#20368=ORIENTED_EDGE('',*,*,#14207,.F.);
#20369=ORIENTED_EDGE('',*,*,#14204,.T.);
#20370=ORIENTED_EDGE('',*,*,#14209,.T.);
#20371=ORIENTED_EDGE('',*,*,#14210,.F.);
#20372=ORIENTED_EDGE('',*,*,#14209,.F.);
#20373=ORIENTED_EDGE('',*,*,#14203,.F.);
#20374=ORIENTED_EDGE('',*,*,#14211,.F.);
#20375=ORIENTED_EDGE('',*,*,#14212,.T.);
#20376=ORIENTED_EDGE('',*,*,#14213,.F.);
#20377=ORIENTED_EDGE('',*,*,#14214,.F.);
#20378=ORIENTED_EDGE('',*,*,#14215,.F.);
#20379=ORIENTED_EDGE('',*,*,#14214,.T.);
#20380=ORIENTED_EDGE('',*,*,#14216,.T.);
#20381=ORIENTED_EDGE('',*,*,#14217,.F.);
#20382=ORIENTED_EDGE('',*,*,#14218,.F.);
#20383=ORIENTED_EDGE('',*,*,#14216,.F.);
#20384=ORIENTED_EDGE('',*,*,#14213,.T.);
#20385=ORIENTED_EDGE('',*,*,#14219,.T.);
#20386=ORIENTED_EDGE('',*,*,#14220,.F.);
#20387=ORIENTED_EDGE('',*,*,#14219,.F.);
#20388=ORIENTED_EDGE('',*,*,#14212,.F.);
#20389=ORIENTED_EDGE('',*,*,#14221,.F.);
#20390=ORIENTED_EDGE('',*,*,#14222,.F.);
#20391=ORIENTED_EDGE('',*,*,#14223,.T.);
#20392=ORIENTED_EDGE('',*,*,#14224,.F.);
#20393=ORIENTED_EDGE('',*,*,#14225,.F.);
#20394=ORIENTED_EDGE('',*,*,#14226,.F.);
#20395=ORIENTED_EDGE('',*,*,#14225,.T.);
#20396=ORIENTED_EDGE('',*,*,#14227,.T.);
#20397=ORIENTED_EDGE('',*,*,#14228,.F.);
#20398=ORIENTED_EDGE('',*,*,#14227,.F.);
#20399=ORIENTED_EDGE('',*,*,#14224,.T.);
#20400=ORIENTED_EDGE('',*,*,#14229,.T.);
#20401=ORIENTED_EDGE('',*,*,#14230,.F.);
#20402=ORIENTED_EDGE('',*,*,#14229,.F.);
#20403=ORIENTED_EDGE('',*,*,#14223,.F.);
#20404=ORIENTED_EDGE('',*,*,#14231,.F.);
#20405=ORIENTED_EDGE('',*,*,#14232,.T.);
#20406=ORIENTED_EDGE('',*,*,#14233,.F.);
#20407=ORIENTED_EDGE('',*,*,#14234,.F.);
#20408=ORIENTED_EDGE('',*,*,#14235,.F.);
#20409=ORIENTED_EDGE('',*,*,#14234,.T.);
#20410=ORIENTED_EDGE('',*,*,#14236,.T.);
#20411=ORIENTED_EDGE('',*,*,#14237,.F.);
#20412=ORIENTED_EDGE('',*,*,#14236,.F.);
#20413=ORIENTED_EDGE('',*,*,#14233,.T.);
#20414=ORIENTED_EDGE('',*,*,#14238,.T.);
#20415=ORIENTED_EDGE('',*,*,#14239,.F.);
#20416=ORIENTED_EDGE('',*,*,#14238,.F.);
#20417=ORIENTED_EDGE('',*,*,#14232,.F.);
#20418=ORIENTED_EDGE('',*,*,#14240,.F.);
#20419=ORIENTED_EDGE('',*,*,#14241,.T.);
#20420=ORIENTED_EDGE('',*,*,#14242,.F.);
#20421=ORIENTED_EDGE('',*,*,#14243,.F.);
#20422=ORIENTED_EDGE('',*,*,#14244,.F.);
#20423=ORIENTED_EDGE('',*,*,#14243,.T.);
#20424=ORIENTED_EDGE('',*,*,#14245,.T.);
#20425=ORIENTED_EDGE('',*,*,#14246,.F.);
#20426=ORIENTED_EDGE('',*,*,#14245,.F.);
#20427=ORIENTED_EDGE('',*,*,#14242,.T.);
#20428=ORIENTED_EDGE('',*,*,#14247,.T.);
#20429=ORIENTED_EDGE('',*,*,#14248,.F.);
#20430=ORIENTED_EDGE('',*,*,#14247,.F.);
#20431=ORIENTED_EDGE('',*,*,#14241,.F.);
#20432=ORIENTED_EDGE('',*,*,#14249,.F.);
#20433=ORIENTED_EDGE('',*,*,#14250,.T.);
#20434=ORIENTED_EDGE('',*,*,#14251,.F.);
#20435=ORIENTED_EDGE('',*,*,#14252,.F.);
#20436=ORIENTED_EDGE('',*,*,#14253,.F.);
#20437=ORIENTED_EDGE('',*,*,#14252,.T.);
#20438=ORIENTED_EDGE('',*,*,#14254,.T.);
#20439=ORIENTED_EDGE('',*,*,#14255,.F.);
#20440=ORIENTED_EDGE('',*,*,#14254,.F.);
#20441=ORIENTED_EDGE('',*,*,#14251,.T.);
#20442=ORIENTED_EDGE('',*,*,#14256,.T.);
#20443=ORIENTED_EDGE('',*,*,#14257,.F.);
#20444=ORIENTED_EDGE('',*,*,#14256,.F.);
#20445=ORIENTED_EDGE('',*,*,#14250,.F.);
#20446=ORIENTED_EDGE('',*,*,#14258,.F.);
#20447=ORIENTED_EDGE('',*,*,#14259,.T.);
#20448=ORIENTED_EDGE('',*,*,#14260,.F.);
#20449=ORIENTED_EDGE('',*,*,#14261,.F.);
#20450=ORIENTED_EDGE('',*,*,#14262,.F.);
#20451=ORIENTED_EDGE('',*,*,#14261,.T.);
#20452=ORIENTED_EDGE('',*,*,#14263,.T.);
#20453=ORIENTED_EDGE('',*,*,#14264,.F.);
#20454=ORIENTED_EDGE('',*,*,#14263,.F.);
#20455=ORIENTED_EDGE('',*,*,#14260,.T.);
#20456=ORIENTED_EDGE('',*,*,#14265,.T.);
#20457=ORIENTED_EDGE('',*,*,#14266,.F.);
#20458=ORIENTED_EDGE('',*,*,#14265,.F.);
#20459=ORIENTED_EDGE('',*,*,#14259,.F.);
#20460=ORIENTED_EDGE('',*,*,#14267,.F.);
#20461=ORIENTED_EDGE('',*,*,#14268,.T.);
#20462=ORIENTED_EDGE('',*,*,#14269,.F.);
#20463=ORIENTED_EDGE('',*,*,#14270,.F.);
#20464=ORIENTED_EDGE('',*,*,#14271,.F.);
#20465=ORIENTED_EDGE('',*,*,#14270,.T.);
#20466=ORIENTED_EDGE('',*,*,#14272,.T.);
#20467=ORIENTED_EDGE('',*,*,#14273,.F.);
#20468=ORIENTED_EDGE('',*,*,#14272,.F.);
#20469=ORIENTED_EDGE('',*,*,#14269,.T.);
#20470=ORIENTED_EDGE('',*,*,#14274,.T.);
#20471=ORIENTED_EDGE('',*,*,#14275,.F.);
#20472=ORIENTED_EDGE('',*,*,#14274,.F.);
#20473=ORIENTED_EDGE('',*,*,#14268,.F.);
#20474=ORIENTED_EDGE('',*,*,#14276,.F.);
#20475=ORIENTED_EDGE('',*,*,#14277,.T.);
#20476=ORIENTED_EDGE('',*,*,#14278,.F.);
#20477=ORIENTED_EDGE('',*,*,#14279,.F.);
#20478=ORIENTED_EDGE('',*,*,#14280,.F.);
#20479=ORIENTED_EDGE('',*,*,#14279,.T.);
#20480=ORIENTED_EDGE('',*,*,#14281,.T.);
#20481=ORIENTED_EDGE('',*,*,#14282,.F.);
#20482=ORIENTED_EDGE('',*,*,#14281,.F.);
#20483=ORIENTED_EDGE('',*,*,#14278,.T.);
#20484=ORIENTED_EDGE('',*,*,#14283,.T.);
#20485=ORIENTED_EDGE('',*,*,#14284,.F.);
#20486=ORIENTED_EDGE('',*,*,#14283,.F.);
#20487=ORIENTED_EDGE('',*,*,#14277,.F.);
#20488=ORIENTED_EDGE('',*,*,#14285,.F.);
#20489=ORIENTED_EDGE('',*,*,#14286,.T.);
#20490=ORIENTED_EDGE('',*,*,#14287,.F.);
#20491=ORIENTED_EDGE('',*,*,#14288,.F.);
#20492=ORIENTED_EDGE('',*,*,#14289,.F.);
#20493=ORIENTED_EDGE('',*,*,#14288,.T.);
#20494=ORIENTED_EDGE('',*,*,#14290,.T.);
#20495=ORIENTED_EDGE('',*,*,#14291,.F.);
#20496=ORIENTED_EDGE('',*,*,#14290,.F.);
#20497=ORIENTED_EDGE('',*,*,#14287,.T.);
#20498=ORIENTED_EDGE('',*,*,#14292,.T.);
#20499=ORIENTED_EDGE('',*,*,#14293,.F.);
#20500=ORIENTED_EDGE('',*,*,#14292,.F.);
#20501=ORIENTED_EDGE('',*,*,#14286,.F.);
#20502=ORIENTED_EDGE('',*,*,#14294,.F.);
#20503=ORIENTED_EDGE('',*,*,#14295,.T.);
#20504=ORIENTED_EDGE('',*,*,#14296,.F.);
#20505=ORIENTED_EDGE('',*,*,#14297,.F.);
#20506=ORIENTED_EDGE('',*,*,#14298,.F.);
#20507=ORIENTED_EDGE('',*,*,#14297,.T.);
#20508=ORIENTED_EDGE('',*,*,#14299,.T.);
#20509=ORIENTED_EDGE('',*,*,#14300,.F.);
#20510=ORIENTED_EDGE('',*,*,#14299,.F.);
#20511=ORIENTED_EDGE('',*,*,#14296,.T.);
#20512=ORIENTED_EDGE('',*,*,#14301,.T.);
#20513=ORIENTED_EDGE('',*,*,#14302,.F.);
#20514=ORIENTED_EDGE('',*,*,#14301,.F.);
#20515=ORIENTED_EDGE('',*,*,#14295,.F.);
#20516=ORIENTED_EDGE('',*,*,#14303,.F.);
#20517=ORIENTED_EDGE('',*,*,#14304,.T.);
#20518=ORIENTED_EDGE('',*,*,#14305,.F.);
#20519=ORIENTED_EDGE('',*,*,#14306,.F.);
#20520=ORIENTED_EDGE('',*,*,#14307,.F.);
#20521=ORIENTED_EDGE('',*,*,#14306,.T.);
#20522=ORIENTED_EDGE('',*,*,#14308,.T.);
#20523=ORIENTED_EDGE('',*,*,#14309,.F.);
#20524=ORIENTED_EDGE('',*,*,#14308,.F.);
#20525=ORIENTED_EDGE('',*,*,#14305,.T.);
#20526=ORIENTED_EDGE('',*,*,#14310,.T.);
#20527=ORIENTED_EDGE('',*,*,#14311,.F.);
#20528=ORIENTED_EDGE('',*,*,#14310,.F.);
#20529=ORIENTED_EDGE('',*,*,#14304,.F.);
#20530=ORIENTED_EDGE('',*,*,#14312,.F.);
#20531=ORIENTED_EDGE('',*,*,#14313,.T.);
#20532=ORIENTED_EDGE('',*,*,#14314,.F.);
#20533=ORIENTED_EDGE('',*,*,#14315,.F.);
#20534=ORIENTED_EDGE('',*,*,#14316,.F.);
#20535=ORIENTED_EDGE('',*,*,#14315,.T.);
#20536=ORIENTED_EDGE('',*,*,#14317,.T.);
#20537=ORIENTED_EDGE('',*,*,#14318,.F.);
#20538=ORIENTED_EDGE('',*,*,#14317,.F.);
#20539=ORIENTED_EDGE('',*,*,#14314,.T.);
#20540=ORIENTED_EDGE('',*,*,#14319,.T.);
#20541=ORIENTED_EDGE('',*,*,#14320,.F.);
#20542=ORIENTED_EDGE('',*,*,#14319,.F.);
#20543=ORIENTED_EDGE('',*,*,#14313,.F.);
#20544=ORIENTED_EDGE('',*,*,#14321,.F.);
#20545=ORIENTED_EDGE('',*,*,#14322,.T.);
#20546=ORIENTED_EDGE('',*,*,#14323,.F.);
#20547=ORIENTED_EDGE('',*,*,#14324,.F.);
#20548=ORIENTED_EDGE('',*,*,#14325,.F.);
#20549=ORIENTED_EDGE('',*,*,#14324,.T.);
#20550=ORIENTED_EDGE('',*,*,#14326,.T.);
#20551=ORIENTED_EDGE('',*,*,#14327,.F.);
#20552=ORIENTED_EDGE('',*,*,#14326,.F.);
#20553=ORIENTED_EDGE('',*,*,#14323,.T.);
#20554=ORIENTED_EDGE('',*,*,#14328,.T.);
#20555=ORIENTED_EDGE('',*,*,#14329,.F.);
#20556=ORIENTED_EDGE('',*,*,#14328,.F.);
#20557=ORIENTED_EDGE('',*,*,#14322,.F.);
#20558=ORIENTED_EDGE('',*,*,#14330,.F.);
#20559=ORIENTED_EDGE('',*,*,#14331,.T.);
#20560=ORIENTED_EDGE('',*,*,#14332,.F.);
#20561=ORIENTED_EDGE('',*,*,#14333,.F.);
#20562=ORIENTED_EDGE('',*,*,#14334,.F.);
#20563=ORIENTED_EDGE('',*,*,#14333,.T.);
#20564=ORIENTED_EDGE('',*,*,#14335,.T.);
#20565=ORIENTED_EDGE('',*,*,#14336,.F.);
#20566=ORIENTED_EDGE('',*,*,#14335,.F.);
#20567=ORIENTED_EDGE('',*,*,#14332,.T.);
#20568=ORIENTED_EDGE('',*,*,#14337,.T.);
#20569=ORIENTED_EDGE('',*,*,#14338,.F.);
#20570=ORIENTED_EDGE('',*,*,#14337,.F.);
#20571=ORIENTED_EDGE('',*,*,#14331,.F.);
#20572=ORIENTED_EDGE('',*,*,#14339,.F.);
#20573=ORIENTED_EDGE('',*,*,#14340,.T.);
#20574=ORIENTED_EDGE('',*,*,#14341,.F.);
#20575=ORIENTED_EDGE('',*,*,#14342,.F.);
#20576=ORIENTED_EDGE('',*,*,#14343,.F.);
#20577=ORIENTED_EDGE('',*,*,#14342,.T.);
#20578=ORIENTED_EDGE('',*,*,#14344,.T.);
#20579=ORIENTED_EDGE('',*,*,#14345,.F.);
#20580=ORIENTED_EDGE('',*,*,#14344,.F.);
#20581=ORIENTED_EDGE('',*,*,#14341,.T.);
#20582=ORIENTED_EDGE('',*,*,#14346,.T.);
#20583=ORIENTED_EDGE('',*,*,#14347,.F.);
#20584=ORIENTED_EDGE('',*,*,#14346,.F.);
#20585=ORIENTED_EDGE('',*,*,#14340,.F.);
#20586=ORIENTED_EDGE('',*,*,#14348,.F.);
#20587=ORIENTED_EDGE('',*,*,#14349,.T.);
#20588=ORIENTED_EDGE('',*,*,#14350,.F.);
#20589=ORIENTED_EDGE('',*,*,#14351,.F.);
#20590=ORIENTED_EDGE('',*,*,#14352,.F.);
#20591=ORIENTED_EDGE('',*,*,#14351,.T.);
#20592=ORIENTED_EDGE('',*,*,#14353,.T.);
#20593=ORIENTED_EDGE('',*,*,#14354,.F.);
#20594=ORIENTED_EDGE('',*,*,#14353,.F.);
#20595=ORIENTED_EDGE('',*,*,#14350,.T.);
#20596=ORIENTED_EDGE('',*,*,#14355,.T.);
#20597=ORIENTED_EDGE('',*,*,#14356,.F.);
#20598=ORIENTED_EDGE('',*,*,#14355,.F.);
#20599=ORIENTED_EDGE('',*,*,#14349,.F.);
#20600=ORIENTED_EDGE('',*,*,#14357,.F.);
#20601=ORIENTED_EDGE('',*,*,#14358,.T.);
#20602=ORIENTED_EDGE('',*,*,#14359,.F.);
#20603=ORIENTED_EDGE('',*,*,#14360,.F.);
#20604=ORIENTED_EDGE('',*,*,#14361,.F.);
#20605=ORIENTED_EDGE('',*,*,#14360,.T.);
#20606=ORIENTED_EDGE('',*,*,#14362,.T.);
#20607=ORIENTED_EDGE('',*,*,#14363,.F.);
#20608=ORIENTED_EDGE('',*,*,#14362,.F.);
#20609=ORIENTED_EDGE('',*,*,#14359,.T.);
#20610=ORIENTED_EDGE('',*,*,#14364,.T.);
#20611=ORIENTED_EDGE('',*,*,#14365,.F.);
#20612=ORIENTED_EDGE('',*,*,#14364,.F.);
#20613=ORIENTED_EDGE('',*,*,#14358,.F.);
#20614=ORIENTED_EDGE('',*,*,#14366,.F.);
#20615=ORIENTED_EDGE('',*,*,#14367,.T.);
#20616=ORIENTED_EDGE('',*,*,#14368,.F.);
#20617=ORIENTED_EDGE('',*,*,#14369,.F.);
#20618=ORIENTED_EDGE('',*,*,#14370,.F.);
#20619=ORIENTED_EDGE('',*,*,#14369,.T.);
#20620=ORIENTED_EDGE('',*,*,#14371,.T.);
#20621=ORIENTED_EDGE('',*,*,#14372,.F.);
#20622=ORIENTED_EDGE('',*,*,#14371,.F.);
#20623=ORIENTED_EDGE('',*,*,#14368,.T.);
#20624=ORIENTED_EDGE('',*,*,#14373,.T.);
#20625=ORIENTED_EDGE('',*,*,#14374,.F.);
#20626=ORIENTED_EDGE('',*,*,#14373,.F.);
#20627=ORIENTED_EDGE('',*,*,#14367,.F.);
#20628=ORIENTED_EDGE('',*,*,#14375,.F.);
#20629=ORIENTED_EDGE('',*,*,#14376,.T.);
#20630=ORIENTED_EDGE('',*,*,#14377,.T.);
#20631=ORIENTED_EDGE('',*,*,#14378,.F.);
#20632=ORIENTED_EDGE('',*,*,#14379,.T.);
#20633=ORIENTED_EDGE('',*,*,#14380,.F.);
#20634=ORIENTED_EDGE('',*,*,#14376,.F.);
#20635=ORIENTED_EDGE('',*,*,#14381,.F.);
#20636=ORIENTED_EDGE('',*,*,#14377,.F.);
#20637=ORIENTED_EDGE('',*,*,#14380,.T.);
#20638=ORIENTED_EDGE('',*,*,#14382,.T.);
#20639=ORIENTED_EDGE('',*,*,#14383,.F.);
#20640=ORIENTED_EDGE('',*,*,#14382,.F.);
#20641=ORIENTED_EDGE('',*,*,#14379,.F.);
#20642=ORIENTED_EDGE('',*,*,#14384,.F.);
#20643=ORIENTED_EDGE('',*,*,#14385,.T.);
#20644=ORIENTED_EDGE('',*,*,#14386,.F.);
#20645=ORIENTED_EDGE('',*,*,#14387,.F.);
#20646=ORIENTED_EDGE('',*,*,#14388,.F.);
#20647=ORIENTED_EDGE('',*,*,#14387,.T.);
#20648=ORIENTED_EDGE('',*,*,#14389,.T.);
#20649=ORIENTED_EDGE('',*,*,#14390,.F.);
#20650=ORIENTED_EDGE('',*,*,#14389,.F.);
#20651=ORIENTED_EDGE('',*,*,#14386,.T.);
#20652=ORIENTED_EDGE('',*,*,#14391,.T.);
#20653=ORIENTED_EDGE('',*,*,#14392,.F.);
#20654=ORIENTED_EDGE('',*,*,#14391,.F.);
#20655=ORIENTED_EDGE('',*,*,#14385,.F.);
#20656=ORIENTED_EDGE('',*,*,#14393,.F.);
#20657=ORIENTED_EDGE('',*,*,#14394,.T.);
#20658=ORIENTED_EDGE('',*,*,#14395,.F.);
#20659=ORIENTED_EDGE('',*,*,#14396,.F.);
#20660=ORIENTED_EDGE('',*,*,#14397,.F.);
#20661=ORIENTED_EDGE('',*,*,#14396,.T.);
#20662=ORIENTED_EDGE('',*,*,#14398,.T.);
#20663=ORIENTED_EDGE('',*,*,#14399,.F.);
#20664=ORIENTED_EDGE('',*,*,#14398,.F.);
#20665=ORIENTED_EDGE('',*,*,#14395,.T.);
#20666=ORIENTED_EDGE('',*,*,#14400,.T.);
#20667=ORIENTED_EDGE('',*,*,#14401,.F.);
#20668=ORIENTED_EDGE('',*,*,#14400,.F.);
#20669=ORIENTED_EDGE('',*,*,#14394,.F.);
#20670=ORIENTED_EDGE('',*,*,#14402,.F.);
#20671=ORIENTED_EDGE('',*,*,#14403,.T.);
#20672=ORIENTED_EDGE('',*,*,#14404,.F.);
#20673=ORIENTED_EDGE('',*,*,#14405,.F.);
#20674=ORIENTED_EDGE('',*,*,#14406,.F.);
#20675=ORIENTED_EDGE('',*,*,#14405,.T.);
#20676=ORIENTED_EDGE('',*,*,#14407,.T.);
#20677=ORIENTED_EDGE('',*,*,#14408,.F.);
#20678=ORIENTED_EDGE('',*,*,#14407,.F.);
#20679=ORIENTED_EDGE('',*,*,#14404,.T.);
#20680=ORIENTED_EDGE('',*,*,#14409,.T.);
#20681=ORIENTED_EDGE('',*,*,#14410,.F.);
#20682=ORIENTED_EDGE('',*,*,#14409,.F.);
#20683=ORIENTED_EDGE('',*,*,#14403,.F.);
#20684=ORIENTED_EDGE('',*,*,#14411,.F.);
#20685=ORIENTED_EDGE('',*,*,#14412,.T.);
#20686=ORIENTED_EDGE('',*,*,#14413,.F.);
#20687=ORIENTED_EDGE('',*,*,#14414,.F.);
#20688=ORIENTED_EDGE('',*,*,#14415,.F.);
#20689=ORIENTED_EDGE('',*,*,#14414,.T.);
#20690=ORIENTED_EDGE('',*,*,#14416,.T.);
#20691=ORIENTED_EDGE('',*,*,#14417,.F.);
#20692=ORIENTED_EDGE('',*,*,#14416,.F.);
#20693=ORIENTED_EDGE('',*,*,#14413,.T.);
#20694=ORIENTED_EDGE('',*,*,#14418,.T.);
#20695=ORIENTED_EDGE('',*,*,#14419,.F.);
#20696=ORIENTED_EDGE('',*,*,#14418,.F.);
#20697=ORIENTED_EDGE('',*,*,#14412,.F.);
#20698=ORIENTED_EDGE('',*,*,#14420,.F.);
#20699=ORIENTED_EDGE('',*,*,#14421,.T.);
#20700=ORIENTED_EDGE('',*,*,#14422,.F.);
#20701=ORIENTED_EDGE('',*,*,#14423,.F.);
#20702=ORIENTED_EDGE('',*,*,#14424,.F.);
#20703=ORIENTED_EDGE('',*,*,#14423,.T.);
#20704=ORIENTED_EDGE('',*,*,#14425,.T.);
#20705=ORIENTED_EDGE('',*,*,#14426,.F.);
#20706=ORIENTED_EDGE('',*,*,#14425,.F.);
#20707=ORIENTED_EDGE('',*,*,#14422,.T.);
#20708=ORIENTED_EDGE('',*,*,#14427,.T.);
#20709=ORIENTED_EDGE('',*,*,#14428,.F.);
#20710=ORIENTED_EDGE('',*,*,#14427,.F.);
#20711=ORIENTED_EDGE('',*,*,#14421,.F.);
#20712=ORIENTED_EDGE('',*,*,#14429,.F.);
#20713=ORIENTED_EDGE('',*,*,#14430,.T.);
#20714=ORIENTED_EDGE('',*,*,#14431,.F.);
#20715=ORIENTED_EDGE('',*,*,#14432,.F.);
#20716=ORIENTED_EDGE('',*,*,#14433,.F.);
#20717=ORIENTED_EDGE('',*,*,#14432,.T.);
#20718=ORIENTED_EDGE('',*,*,#14434,.T.);
#20719=ORIENTED_EDGE('',*,*,#14435,.F.);
#20720=ORIENTED_EDGE('',*,*,#14434,.F.);
#20721=ORIENTED_EDGE('',*,*,#14431,.T.);
#20722=ORIENTED_EDGE('',*,*,#14436,.T.);
#20723=ORIENTED_EDGE('',*,*,#14437,.F.);
#20724=ORIENTED_EDGE('',*,*,#14436,.F.);
#20725=ORIENTED_EDGE('',*,*,#14430,.F.);
#20726=ORIENTED_EDGE('',*,*,#14438,.F.);
#20727=ORIENTED_EDGE('',*,*,#14439,.T.);
#20728=ORIENTED_EDGE('',*,*,#14440,.F.);
#20729=ORIENTED_EDGE('',*,*,#14441,.F.);
#20730=ORIENTED_EDGE('',*,*,#14442,.F.);
#20731=ORIENTED_EDGE('',*,*,#14441,.T.);
#20732=ORIENTED_EDGE('',*,*,#14443,.T.);
#20733=ORIENTED_EDGE('',*,*,#14444,.F.);
#20734=ORIENTED_EDGE('',*,*,#14443,.F.);
#20735=ORIENTED_EDGE('',*,*,#14440,.T.);
#20736=ORIENTED_EDGE('',*,*,#14445,.T.);
#20737=ORIENTED_EDGE('',*,*,#14446,.F.);
#20738=ORIENTED_EDGE('',*,*,#14445,.F.);
#20739=ORIENTED_EDGE('',*,*,#14439,.F.);
#20740=ORIENTED_EDGE('',*,*,#14447,.F.);
#20741=ORIENTED_EDGE('',*,*,#14448,.T.);
#20742=ORIENTED_EDGE('',*,*,#14449,.F.);
#20743=ORIENTED_EDGE('',*,*,#14450,.F.);
#20744=ORIENTED_EDGE('',*,*,#14451,.F.);
#20745=ORIENTED_EDGE('',*,*,#14450,.T.);
#20746=ORIENTED_EDGE('',*,*,#14452,.T.);
#20747=ORIENTED_EDGE('',*,*,#14453,.F.);
#20748=ORIENTED_EDGE('',*,*,#14452,.F.);
#20749=ORIENTED_EDGE('',*,*,#14449,.T.);
#20750=ORIENTED_EDGE('',*,*,#14454,.T.);
#20751=ORIENTED_EDGE('',*,*,#14455,.F.);
#20752=ORIENTED_EDGE('',*,*,#14454,.F.);
#20753=ORIENTED_EDGE('',*,*,#14448,.F.);
#20754=ORIENTED_EDGE('',*,*,#14456,.F.);
#20755=ORIENTED_EDGE('',*,*,#14457,.T.);
#20756=ORIENTED_EDGE('',*,*,#14458,.F.);
#20757=ORIENTED_EDGE('',*,*,#14459,.F.);
#20758=ORIENTED_EDGE('',*,*,#14460,.F.);
#20759=ORIENTED_EDGE('',*,*,#14459,.T.);
#20760=ORIENTED_EDGE('',*,*,#14461,.T.);
#20761=ORIENTED_EDGE('',*,*,#14462,.F.);
#20762=ORIENTED_EDGE('',*,*,#14461,.F.);
#20763=ORIENTED_EDGE('',*,*,#14458,.T.);
#20764=ORIENTED_EDGE('',*,*,#14463,.T.);
#20765=ORIENTED_EDGE('',*,*,#14464,.F.);
#20766=ORIENTED_EDGE('',*,*,#14463,.F.);
#20767=ORIENTED_EDGE('',*,*,#14457,.F.);
#20768=ORIENTED_EDGE('',*,*,#14465,.F.);
#20769=ORIENTED_EDGE('',*,*,#13969,.F.);
#20770=ORIENTED_EDGE('',*,*,#14466,.T.);
#20771=ORIENTED_EDGE('',*,*,#14465,.T.);
#20772=ORIENTED_EDGE('',*,*,#14466,.F.);
#20773=ORIENTED_EDGE('',*,*,#14467,.F.);
#20774=ORIENTED_EDGE('',*,*,#14468,.T.);
#20775=ORIENTED_EDGE('',*,*,#14118,.T.);
#20776=ORIENTED_EDGE('',*,*,#14468,.F.);
#20777=ORIENTED_EDGE('',*,*,#14139,.T.);
#20778=ORIENTED_EDGE('',*,*,#14469,.F.);
#20779=ORIENTED_EDGE('',*,*,#14453,.T.);
#20780=ORIENTED_EDGE('',*,*,#14455,.T.);
#20781=ORIENTED_EDGE('',*,*,#14447,.T.);
#20782=ORIENTED_EDGE('',*,*,#14470,.F.);
#20783=ORIENTED_EDGE('',*,*,#14154,.T.);
#20784=ORIENTED_EDGE('',*,*,#14156,.T.);
#20785=ORIENTED_EDGE('',*,*,#14148,.T.);
#20786=ORIENTED_EDGE('',*,*,#14471,.F.);
#20787=ORIENTED_EDGE('',*,*,#14444,.T.);
#20788=ORIENTED_EDGE('',*,*,#14446,.T.);
#20789=ORIENTED_EDGE('',*,*,#14438,.T.);
#20790=ORIENTED_EDGE('',*,*,#14472,.F.);
#20791=ORIENTED_EDGE('',*,*,#14163,.T.);
#20792=ORIENTED_EDGE('',*,*,#14165,.T.);
#20793=ORIENTED_EDGE('',*,*,#14157,.T.);
#20794=ORIENTED_EDGE('',*,*,#14473,.F.);
#20795=ORIENTED_EDGE('',*,*,#14435,.T.);
#20796=ORIENTED_EDGE('',*,*,#14437,.T.);
#20797=ORIENTED_EDGE('',*,*,#14429,.T.);
#20798=ORIENTED_EDGE('',*,*,#14474,.F.);
#20799=ORIENTED_EDGE('',*,*,#14172,.T.);
#20800=ORIENTED_EDGE('',*,*,#14174,.T.);
#20801=ORIENTED_EDGE('',*,*,#14166,.T.);
#20802=ORIENTED_EDGE('',*,*,#14475,.F.);
#20803=ORIENTED_EDGE('',*,*,#14426,.T.);
#20804=ORIENTED_EDGE('',*,*,#14428,.T.);
#20805=ORIENTED_EDGE('',*,*,#14420,.T.);
#20806=ORIENTED_EDGE('',*,*,#14476,.F.);
#20807=ORIENTED_EDGE('',*,*,#14181,.T.);
#20808=ORIENTED_EDGE('',*,*,#14183,.T.);
#20809=ORIENTED_EDGE('',*,*,#14175,.T.);
#20810=ORIENTED_EDGE('',*,*,#14477,.F.);
#20811=ORIENTED_EDGE('',*,*,#14417,.T.);
#20812=ORIENTED_EDGE('',*,*,#14419,.T.);
#20813=ORIENTED_EDGE('',*,*,#14411,.T.);
#20814=ORIENTED_EDGE('',*,*,#14478,.F.);
#20815=ORIENTED_EDGE('',*,*,#14190,.T.);
#20816=ORIENTED_EDGE('',*,*,#14192,.T.);
#20817=ORIENTED_EDGE('',*,*,#14184,.T.);
#20818=ORIENTED_EDGE('',*,*,#14479,.F.);
#20819=ORIENTED_EDGE('',*,*,#14408,.T.);
#20820=ORIENTED_EDGE('',*,*,#14410,.T.);
#20821=ORIENTED_EDGE('',*,*,#14402,.T.);
#20822=ORIENTED_EDGE('',*,*,#14480,.F.);
#20823=ORIENTED_EDGE('',*,*,#14199,.T.);
#20824=ORIENTED_EDGE('',*,*,#14201,.T.);
#20825=ORIENTED_EDGE('',*,*,#14193,.T.);
#20826=ORIENTED_EDGE('',*,*,#14481,.F.);
#20827=ORIENTED_EDGE('',*,*,#14399,.T.);
#20828=ORIENTED_EDGE('',*,*,#14401,.T.);
#20829=ORIENTED_EDGE('',*,*,#14393,.T.);
#20830=ORIENTED_EDGE('',*,*,#14482,.F.);
#20831=ORIENTED_EDGE('',*,*,#14208,.T.);
#20832=ORIENTED_EDGE('',*,*,#14210,.T.);
#20833=ORIENTED_EDGE('',*,*,#14202,.T.);
#20834=ORIENTED_EDGE('',*,*,#14483,.F.);
#20835=ORIENTED_EDGE('',*,*,#14390,.T.);
#20836=ORIENTED_EDGE('',*,*,#14392,.T.);
#20837=ORIENTED_EDGE('',*,*,#14384,.T.);
#20838=ORIENTED_EDGE('',*,*,#14484,.F.);
#20839=ORIENTED_EDGE('',*,*,#14218,.T.);
#20840=ORIENTED_EDGE('',*,*,#14220,.T.);
#20841=ORIENTED_EDGE('',*,*,#14485,.T.);
#20842=ORIENTED_EDGE('',*,*,#14467,.T.);
#20843=ORIENTED_EDGE('',*,*,#14485,.F.);
#20844=ORIENTED_EDGE('',*,*,#14221,.T.);
#20845=ORIENTED_EDGE('',*,*,#14211,.T.);
#20846=ORIENTED_EDGE('',*,*,#14486,.F.);
#20847=ORIENTED_EDGE('',*,*,#14228,.T.);
#20848=ORIENTED_EDGE('',*,*,#14230,.T.);
#20849=ORIENTED_EDGE('',*,*,#14222,.T.);
#20850=ORIENTED_EDGE('',*,*,#14487,.F.);
#20851=ORIENTED_EDGE('',*,*,#14372,.T.);
#20852=ORIENTED_EDGE('',*,*,#14374,.T.);
#20853=ORIENTED_EDGE('',*,*,#14366,.T.);
#20854=ORIENTED_EDGE('',*,*,#14488,.F.);
#20855=ORIENTED_EDGE('',*,*,#14237,.T.);
#20856=ORIENTED_EDGE('',*,*,#14239,.T.);
#20857=ORIENTED_EDGE('',*,*,#14231,.T.);
#20858=ORIENTED_EDGE('',*,*,#14489,.F.);
#20859=ORIENTED_EDGE('',*,*,#14363,.T.);
#20860=ORIENTED_EDGE('',*,*,#14365,.T.);
#20861=ORIENTED_EDGE('',*,*,#14357,.T.);
#20862=ORIENTED_EDGE('',*,*,#14490,.F.);
#20863=ORIENTED_EDGE('',*,*,#14246,.T.);
#20864=ORIENTED_EDGE('',*,*,#14248,.T.);
#20865=ORIENTED_EDGE('',*,*,#14240,.T.);
#20866=ORIENTED_EDGE('',*,*,#14491,.F.);
#20867=ORIENTED_EDGE('',*,*,#14354,.T.);
#20868=ORIENTED_EDGE('',*,*,#14356,.T.);
#20869=ORIENTED_EDGE('',*,*,#14348,.T.);
#20870=ORIENTED_EDGE('',*,*,#14492,.F.);
#20871=ORIENTED_EDGE('',*,*,#14255,.T.);
#20872=ORIENTED_EDGE('',*,*,#14257,.T.);
#20873=ORIENTED_EDGE('',*,*,#14249,.T.);
#20874=ORIENTED_EDGE('',*,*,#14493,.F.);
#20875=ORIENTED_EDGE('',*,*,#14345,.T.);
#20876=ORIENTED_EDGE('',*,*,#14347,.T.);
#20877=ORIENTED_EDGE('',*,*,#14339,.T.);
#20878=ORIENTED_EDGE('',*,*,#14494,.F.);
#20879=ORIENTED_EDGE('',*,*,#14264,.T.);
#20880=ORIENTED_EDGE('',*,*,#14266,.T.);
#20881=ORIENTED_EDGE('',*,*,#14258,.T.);
#20882=ORIENTED_EDGE('',*,*,#14495,.F.);
#20883=ORIENTED_EDGE('',*,*,#14336,.T.);
#20884=ORIENTED_EDGE('',*,*,#14338,.T.);
#20885=ORIENTED_EDGE('',*,*,#14330,.T.);
#20886=ORIENTED_EDGE('',*,*,#14496,.F.);
#20887=ORIENTED_EDGE('',*,*,#14273,.T.);
#20888=ORIENTED_EDGE('',*,*,#14275,.T.);
#20889=ORIENTED_EDGE('',*,*,#14267,.T.);
#20890=ORIENTED_EDGE('',*,*,#14497,.F.);
#20891=ORIENTED_EDGE('',*,*,#14327,.T.);
#20892=ORIENTED_EDGE('',*,*,#14329,.T.);
#20893=ORIENTED_EDGE('',*,*,#14321,.T.);
#20894=ORIENTED_EDGE('',*,*,#14498,.F.);
#20895=ORIENTED_EDGE('',*,*,#14282,.T.);
#20896=ORIENTED_EDGE('',*,*,#14284,.T.);
#20897=ORIENTED_EDGE('',*,*,#14276,.T.);
#20898=ORIENTED_EDGE('',*,*,#14499,.F.);
#20899=ORIENTED_EDGE('',*,*,#14318,.T.);
#20900=ORIENTED_EDGE('',*,*,#14320,.T.);
#20901=ORIENTED_EDGE('',*,*,#14312,.T.);
#20902=ORIENTED_EDGE('',*,*,#14500,.F.);
#20903=ORIENTED_EDGE('',*,*,#14291,.T.);
#20904=ORIENTED_EDGE('',*,*,#14293,.T.);
#20905=ORIENTED_EDGE('',*,*,#14285,.T.);
#20906=ORIENTED_EDGE('',*,*,#14501,.F.);
#20907=ORIENTED_EDGE('',*,*,#14309,.T.);
#20908=ORIENTED_EDGE('',*,*,#14311,.T.);
#20909=ORIENTED_EDGE('',*,*,#14303,.T.);
#20910=ORIENTED_EDGE('',*,*,#14502,.F.);
#20911=ORIENTED_EDGE('',*,*,#14300,.T.);
#20912=ORIENTED_EDGE('',*,*,#14302,.T.);
#20913=ORIENTED_EDGE('',*,*,#14294,.T.);
#20914=ORIENTED_EDGE('',*,*,#14503,.F.);
#20915=ORIENTED_EDGE('',*,*,#14381,.T.);
#20916=ORIENTED_EDGE('',*,*,#14383,.T.);
#20917=ORIENTED_EDGE('',*,*,#14378,.T.);
#20918=ORIENTED_EDGE('',*,*,#14504,.F.);
#20919=ORIENTED_EDGE('',*,*,#14462,.T.);
#20920=ORIENTED_EDGE('',*,*,#14464,.T.);
#20921=ORIENTED_EDGE('',*,*,#14456,.T.);
#20922=ORIENTED_EDGE('',*,*,#14505,.F.);
#20923=ORIENTED_EDGE('',*,*,#14145,.T.);
#20924=ORIENTED_EDGE('',*,*,#14147,.T.);
#20925=ORIENTED_EDGE('',*,*,#14506,.F.);
#20926=ORIENTED_EDGE('',*,*,#14507,.T.);
#20927=ORIENTED_EDGE('',*,*,#14217,.T.);
#20928=ORIENTED_EDGE('',*,*,#14484,.T.);
#20929=ORIENTED_EDGE('',*,*,#14388,.T.);
#20930=ORIENTED_EDGE('',*,*,#14483,.T.);
#20931=ORIENTED_EDGE('',*,*,#14206,.T.);
#20932=ORIENTED_EDGE('',*,*,#14482,.T.);
#20933=ORIENTED_EDGE('',*,*,#14397,.T.);
#20934=ORIENTED_EDGE('',*,*,#14481,.T.);
#20935=ORIENTED_EDGE('',*,*,#14197,.T.);
#20936=ORIENTED_EDGE('',*,*,#14480,.T.);
#20937=ORIENTED_EDGE('',*,*,#14406,.T.);
#20938=ORIENTED_EDGE('',*,*,#14479,.T.);
#20939=ORIENTED_EDGE('',*,*,#14188,.T.);
#20940=ORIENTED_EDGE('',*,*,#14478,.T.);
#20941=ORIENTED_EDGE('',*,*,#14415,.T.);
#20942=ORIENTED_EDGE('',*,*,#14477,.T.);
#20943=ORIENTED_EDGE('',*,*,#14179,.T.);
#20944=ORIENTED_EDGE('',*,*,#14476,.T.);
#20945=ORIENTED_EDGE('',*,*,#14424,.T.);
#20946=ORIENTED_EDGE('',*,*,#14475,.T.);
#20947=ORIENTED_EDGE('',*,*,#14170,.T.);
#20948=ORIENTED_EDGE('',*,*,#14474,.T.);
#20949=ORIENTED_EDGE('',*,*,#14433,.T.);
#20950=ORIENTED_EDGE('',*,*,#14473,.T.);
#20951=ORIENTED_EDGE('',*,*,#14161,.T.);
#20952=ORIENTED_EDGE('',*,*,#14472,.T.);
#20953=ORIENTED_EDGE('',*,*,#14442,.T.);
#20954=ORIENTED_EDGE('',*,*,#14471,.T.);
#20955=ORIENTED_EDGE('',*,*,#14152,.T.);
#20956=ORIENTED_EDGE('',*,*,#14470,.T.);
#20957=ORIENTED_EDGE('',*,*,#14451,.T.);
#20958=ORIENTED_EDGE('',*,*,#14469,.T.);
#20959=ORIENTED_EDGE('',*,*,#14143,.T.);
#20960=ORIENTED_EDGE('',*,*,#14505,.T.);
#20961=ORIENTED_EDGE('',*,*,#14460,.T.);
#20962=ORIENTED_EDGE('',*,*,#14504,.T.);
#20963=ORIENTED_EDGE('',*,*,#14375,.T.);
#20964=ORIENTED_EDGE('',*,*,#14503,.T.);
#20965=ORIENTED_EDGE('',*,*,#14298,.T.);
#20966=ORIENTED_EDGE('',*,*,#14502,.T.);
#20967=ORIENTED_EDGE('',*,*,#14307,.T.);
#20968=ORIENTED_EDGE('',*,*,#14501,.T.);
#20969=ORIENTED_EDGE('',*,*,#14289,.T.);
#20970=ORIENTED_EDGE('',*,*,#14500,.T.);
#20971=ORIENTED_EDGE('',*,*,#14316,.T.);
#20972=ORIENTED_EDGE('',*,*,#14499,.T.);
#20973=ORIENTED_EDGE('',*,*,#14280,.T.);
#20974=ORIENTED_EDGE('',*,*,#14498,.T.);
#20975=ORIENTED_EDGE('',*,*,#14325,.T.);
#20976=ORIENTED_EDGE('',*,*,#14497,.T.);
#20977=ORIENTED_EDGE('',*,*,#14271,.T.);
#20978=ORIENTED_EDGE('',*,*,#14496,.T.);
#20979=ORIENTED_EDGE('',*,*,#14334,.T.);
#20980=ORIENTED_EDGE('',*,*,#14495,.T.);
#20981=ORIENTED_EDGE('',*,*,#14262,.T.);
#20982=ORIENTED_EDGE('',*,*,#14494,.T.);
#20983=ORIENTED_EDGE('',*,*,#14343,.T.);
#20984=ORIENTED_EDGE('',*,*,#14493,.T.);
#20985=ORIENTED_EDGE('',*,*,#14253,.T.);
#20986=ORIENTED_EDGE('',*,*,#14492,.T.);
#20987=ORIENTED_EDGE('',*,*,#14352,.T.);
#20988=ORIENTED_EDGE('',*,*,#14491,.T.);
#20989=ORIENTED_EDGE('',*,*,#14244,.T.);
#20990=ORIENTED_EDGE('',*,*,#14490,.T.);
#20991=ORIENTED_EDGE('',*,*,#14361,.T.);
#20992=ORIENTED_EDGE('',*,*,#14489,.T.);
#20993=ORIENTED_EDGE('',*,*,#14235,.T.);
#20994=ORIENTED_EDGE('',*,*,#14488,.T.);
#20995=ORIENTED_EDGE('',*,*,#14370,.T.);
#20996=ORIENTED_EDGE('',*,*,#14487,.T.);
#20997=ORIENTED_EDGE('',*,*,#14226,.T.);
#20998=ORIENTED_EDGE('',*,*,#14486,.T.);
#20999=ORIENTED_EDGE('',*,*,#14215,.T.);
#21000=ORIENTED_EDGE('',*,*,#14507,.F.);
#21001=ORIENTED_EDGE('',*,*,#14506,.T.);
#21002=ORIENTED_EDGE('',*,*,#14121,.T.);
#21003=ORIENTED_EDGE('',*,*,#14137,.T.);
#21004=ORIENTED_EDGE('',*,*,#14134,.T.);
#21005=ORIENTED_EDGE('',*,*,#14131,.T.);
#21006=ORIENTED_EDGE('',*,*,#14128,.T.);
#21007=ORIENTED_EDGE('',*,*,#14125,.T.);
#21490=CONICAL_SURFACE('',#24724,0.149995599935465,1.0303638848789);
#21491=CONICAL_SURFACE('',#24953,0.37,0.785398163397445);
#21492=CONICAL_SURFACE('',#24954,0.63,0.785398163397449);
#21493=CONICAL_SURFACE('',#24993,0.62,0.785398163397447);
#22533=ADVANCED_FACE('',(#3703),#2589,.T.);
#22534=ADVANCED_FACE('',(#3704),#2590,.T.);
#22535=ADVANCED_FACE('',(#3705),#2591,.T.);
#22536=ADVANCED_FACE('',(#3706),#2592,.T.);
#22537=ADVANCED_FACE('',(#3707),#2593,.T.);
#22538=ADVANCED_FACE('',(#3708),#2594,.T.);
#22539=ADVANCED_FACE('',(#3709),#2595,.T.);
#22540=ADVANCED_FACE('',(#3710),#2596,.T.);
#22541=ADVANCED_FACE('',(#3711),#2597,.T.);
#22542=ADVANCED_FACE('',(#3712),#2598,.T.);
#22543=ADVANCED_FACE('',(#3713),#2599,.T.);
#22544=ADVANCED_FACE('',(#3714),#2600,.T.);
#22545=ADVANCED_FACE('',(#3715),#2601,.T.);
#22546=ADVANCED_FACE('',(#3716),#2602,.T.);
#22547=ADVANCED_FACE('',(#3717),#2603,.T.);
#22548=ADVANCED_FACE('',(#3718),#2604,.T.);
#22549=ADVANCED_FACE('',(#3719),#2605,.T.);
#22550=ADVANCED_FACE('',(#3720),#2606,.T.);
#22551=ADVANCED_FACE('',(#3721),#2607,.T.);
#22552=ADVANCED_FACE('',(#3722),#2608,.T.);
#22553=ADVANCED_FACE('',(#3723),#2609,.T.);
#22554=ADVANCED_FACE('',(#3724),#2610,.T.);
#22555=ADVANCED_FACE('',(#3725),#2611,.T.);
#22556=ADVANCED_FACE('',(#3726),#2612,.T.);
#22557=ADVANCED_FACE('',(#3727),#2613,.T.);
#22558=ADVANCED_FACE('',(#3728),#2614,.T.);
#22559=ADVANCED_FACE('',(#3729),#2615,.T.);
#22560=ADVANCED_FACE('',(#3730),#2616,.T.);
#22561=ADVANCED_FACE('',(#3731),#2617,.T.);
#22562=ADVANCED_FACE('',(#3732),#2618,.T.);
#22563=ADVANCED_FACE('',(#3733),#2619,.T.);
#22564=ADVANCED_FACE('',(#3734),#2620,.T.);
#22565=ADVANCED_FACE('',(#3735),#2621,.T.);
#22566=ADVANCED_FACE('',(#3736),#2622,.T.);
#22567=ADVANCED_FACE('',(#3737),#2623,.T.);
#22568=ADVANCED_FACE('',(#3738),#2624,.T.);
#22569=ADVANCED_FACE('',(#3739),#2625,.T.);
#22570=ADVANCED_FACE('',(#3740),#2626,.T.);
#22571=ADVANCED_FACE('',(#3741),#2627,.T.);
#22572=ADVANCED_FACE('',(#3742),#2628,.T.);
#22573=ADVANCED_FACE('',(#3743),#2629,.T.);
#22574=ADVANCED_FACE('',(#3744),#2630,.T.);
#22575=ADVANCED_FACE('',(#3745),#2631,.T.);
#22576=ADVANCED_FACE('',(#3746),#2632,.T.);
#22577=ADVANCED_FACE('',(#3747),#2633,.T.);
#22578=ADVANCED_FACE('',(#3748),#2238,.F.);
#22579=ADVANCED_FACE('',(#3749),#559,.F.);
#22580=ADVANCED_FACE('',(#3750),#2239,.T.);
#22581=ADVANCED_FACE('',(#3751),#2634,.T.);
#22582=ADVANCED_FACE('',(#3752),#560,.F.);
#22583=ADVANCED_FACE('',(#3753),#2635,.T.);
#22584=ADVANCED_FACE('',(#3754),#313,.F.);
#22585=ADVANCED_FACE('',(#3755,#1802),#2240,.T.);
#22586=ADVANCED_FACE('',(#3756),#21490,.F.);
#22587=ADVANCED_FACE('',(#3757),#2241,.F.);
#22588=ADVANCED_FACE('',(#3758),#2242,.F.);
#22589=ADVANCED_FACE('',(#3759),#2243,.F.);
#22590=ADVANCED_FACE('',(#3760),#2244,.F.);
#22591=ADVANCED_FACE('',(#3761),#2245,.F.);
#22592=ADVANCED_FACE('',(#3762),#2246,.F.);
#22593=ADVANCED_FACE('',(#3763,#1803),#2247,.F.);
#22594=ADVANCED_FACE('',(#3764),#2248,.F.);
#22595=ADVANCED_FACE('',(#3765),#2249,.F.);
#22596=ADVANCED_FACE('',(#3766),#2250,.F.);
#22597=ADVANCED_FACE('',(#3767),#2251,.F.);
#22598=ADVANCED_FACE('',(#3768),#2252,.F.);
#22599=ADVANCED_FACE('',(#3769),#2253,.F.);
#22600=ADVANCED_FACE('',(#3770),#2254,.F.);
#22601=ADVANCED_FACE('',(#3771),#2255,.F.);
#22602=ADVANCED_FACE('',(#3772),#2256,.F.);
#22603=ADVANCED_FACE('',(#3773),#2257,.F.);
#22604=ADVANCED_FACE('',(#3774),#2258,.F.);
#22605=ADVANCED_FACE('',(#3775),#2259,.F.);
#22606=ADVANCED_FACE('',(#3776),#2260,.F.);
#22607=ADVANCED_FACE('',(#3777),#2261,.F.);
#22608=ADVANCED_FACE('',(#3778),#2262,.F.);
#22609=ADVANCED_FACE('',(#3779),#2263,.F.);
#22610=ADVANCED_FACE('',(#3780),#2264,.F.);
#22611=ADVANCED_FACE('',(#3781),#2265,.F.);
#22612=ADVANCED_FACE('',(#3782),#2266,.F.);
#22613=ADVANCED_FACE('',(#3783),#2267,.F.);
#22614=ADVANCED_FACE('',(#3784),#2268,.F.);
#22615=ADVANCED_FACE('',(#3785),#2269,.F.);
#22616=ADVANCED_FACE('',(#3786),#2270,.F.);
#22617=ADVANCED_FACE('',(#3787),#2271,.F.);
#22618=ADVANCED_FACE('',(#3788),#2272,.F.);
#22619=ADVANCED_FACE('',(#3789),#2273,.F.);
#22620=ADVANCED_FACE('',(#3790),#2274,.F.);
#22621=ADVANCED_FACE('',(#3791),#2275,.F.);
#22622=ADVANCED_FACE('',(#3792),#2276,.F.);
#22623=ADVANCED_FACE('',(#3793),#2277,.F.);
#22624=ADVANCED_FACE('',(#3794),#2278,.F.);
#22625=ADVANCED_FACE('',(#3795),#2279,.F.);
#22626=ADVANCED_FACE('',(#3796),#2280,.F.);
#22627=ADVANCED_FACE('',(#3797),#2281,.F.);
#22628=ADVANCED_FACE('',(#3798),#2282,.F.);
#22629=ADVANCED_FACE('',(#3799),#2283,.F.);
#22630=ADVANCED_FACE('',(#3800),#2284,.F.);
#22631=ADVANCED_FACE('',(#3801),#2285,.F.);
#22632=ADVANCED_FACE('',(#3802),#2286,.F.);
#22633=ADVANCED_FACE('',(#3803),#2287,.F.);
#22634=ADVANCED_FACE('',(#3804),#2288,.F.);
#22635=ADVANCED_FACE('',(#3805),#2289,.F.);
#22636=ADVANCED_FACE('',(#3806),#2290,.F.);
#22637=ADVANCED_FACE('',(#3807),#2291,.F.);
#22638=ADVANCED_FACE('',(#3808),#2292,.F.);
#22639=ADVANCED_FACE('',(#3809),#2293,.F.);
#22640=ADVANCED_FACE('',(#3810),#2294,.F.);
#22641=ADVANCED_FACE('',(#3811),#2295,.F.);
#22642=ADVANCED_FACE('',(#3812),#2296,.F.);
#22643=ADVANCED_FACE('',(#3813),#2297,.F.);
#22644=ADVANCED_FACE('',(#3814),#2298,.F.);
#22645=ADVANCED_FACE('',(#3815),#2299,.F.);
#22646=ADVANCED_FACE('',(#3816),#2300,.F.);
#22647=ADVANCED_FACE('',(#3817),#2301,.F.);
#22648=ADVANCED_FACE('',(#3818),#2302,.F.);
#22649=ADVANCED_FACE('',(#3819),#2303,.F.);
#22650=ADVANCED_FACE('',(#3820),#2304,.F.);
#22651=ADVANCED_FACE('',(#3821),#2305,.F.);
#22652=ADVANCED_FACE('',(#3822),#2306,.F.);
#22653=ADVANCED_FACE('',(#3823),#2307,.F.);
#22654=ADVANCED_FACE('',(#3824),#2308,.F.);
#22655=ADVANCED_FACE('',(#3825),#2309,.F.);
#22656=ADVANCED_FACE('',(#3826),#2310,.F.);
#22657=ADVANCED_FACE('',(#3827),#2311,.F.);
#22658=ADVANCED_FACE('',(#3828),#2312,.F.);
#22659=ADVANCED_FACE('',(#3829),#2313,.F.);
#22660=ADVANCED_FACE('',(#3830),#2314,.F.);
#22661=ADVANCED_FACE('',(#3831),#2315,.F.);
#22662=ADVANCED_FACE('',(#3832),#2316,.F.);
#22663=ADVANCED_FACE('',(#3833),#2317,.F.);
#22664=ADVANCED_FACE('',(#3834),#2318,.F.);
#22665=ADVANCED_FACE('',(#3835),#2319,.F.);
#22666=ADVANCED_FACE('',(#3836),#2320,.F.);
#22667=ADVANCED_FACE('',(#3837),#2321,.F.);
#22668=ADVANCED_FACE('',(#3838),#2322,.F.);
#22669=ADVANCED_FACE('',(#3839),#2323,.F.);
#22670=ADVANCED_FACE('',(#3840),#2324,.F.);
#22671=ADVANCED_FACE('',(#3841),#2325,.F.);
#22672=ADVANCED_FACE('',(#3842),#2326,.F.);
#22673=ADVANCED_FACE('',(#3843),#2327,.F.);
#22674=ADVANCED_FACE('',(#3844),#2328,.F.);
#22675=ADVANCED_FACE('',(#3845),#2329,.F.);
#22676=ADVANCED_FACE('',(#3846),#2330,.F.);
#22677=ADVANCED_FACE('',(#3847),#2331,.F.);
#22678=ADVANCED_FACE('',(#3848),#2332,.F.);
#22679=ADVANCED_FACE('',(#3849),#2333,.F.);
#22680=ADVANCED_FACE('',(#3850),#2334,.F.);
#22681=ADVANCED_FACE('',(#3851),#2335,.F.);
#22682=ADVANCED_FACE('',(#3852),#2336,.F.);
#22683=ADVANCED_FACE('',(#3853),#2337,.F.);
#22684=ADVANCED_FACE('',(#3854),#2338,.F.);
#22685=ADVANCED_FACE('',(#3855),#2339,.F.);
#22686=ADVANCED_FACE('',(#3856),#2340,.F.);
#22687=ADVANCED_FACE('',(#3857),#2341,.F.);
#22688=ADVANCED_FACE('',(#3858),#2342,.F.);
#22689=ADVANCED_FACE('',(#3859),#2343,.F.);
#22690=ADVANCED_FACE('',(#3860),#2344,.F.);
#22691=ADVANCED_FACE('',(#3861),#2345,.F.);
#22692=ADVANCED_FACE('',(#3862),#2346,.F.);
#22693=ADVANCED_FACE('',(#3863),#2347,.F.);
#22694=ADVANCED_FACE('',(#3864),#2348,.F.);
#22695=ADVANCED_FACE('',(#3865),#2349,.F.);
#22696=ADVANCED_FACE('',(#3866),#2350,.F.);
#22697=ADVANCED_FACE('',(#3867),#2351,.F.);
#22698=ADVANCED_FACE('',(#3868),#2352,.F.);
#22699=ADVANCED_FACE('',(#3869),#2353,.F.);
#22700=ADVANCED_FACE('',(#3870),#2354,.F.);
#22701=ADVANCED_FACE('',(#3871),#2355,.F.);
#22702=ADVANCED_FACE('',(#3872),#2356,.F.);
#22703=ADVANCED_FACE('',(#3873),#2357,.F.);
#22704=ADVANCED_FACE('',(#3874),#2358,.F.);
#22705=ADVANCED_FACE('',(#3875),#2359,.F.);
#22706=ADVANCED_FACE('',(#3876),#2360,.F.);
#22707=ADVANCED_FACE('',(#3877),#2361,.F.);
#22708=ADVANCED_FACE('',(#3878),#2362,.F.);
#22709=ADVANCED_FACE('',(#3879),#2363,.F.);
#22710=ADVANCED_FACE('',(#3880),#2364,.F.);
#22711=ADVANCED_FACE('',(#3881),#2365,.F.);
#22712=ADVANCED_FACE('',(#3882),#2366,.F.);
#22713=ADVANCED_FACE('',(#3883),#2367,.F.);
#22714=ADVANCED_FACE('',(#3884),#2368,.F.);
#22715=ADVANCED_FACE('',(#3885),#2369,.F.);
#22716=ADVANCED_FACE('',(#3886),#2370,.F.);
#22717=ADVANCED_FACE('',(#3887),#2371,.F.);
#22718=ADVANCED_FACE('',(#3888),#2372,.F.);
#22719=ADVANCED_FACE('',(#3889),#2373,.F.);
#22720=ADVANCED_FACE('',(#3890),#2374,.F.);
#22721=ADVANCED_FACE('',(#3891),#2375,.F.);
#22722=ADVANCED_FACE('',(#3892),#2376,.F.);
#22723=ADVANCED_FACE('',(#3893),#2377,.F.);
#22724=ADVANCED_FACE('',(#3894),#2378,.F.);
#22725=ADVANCED_FACE('',(#3895),#2379,.F.);
#22726=ADVANCED_FACE('',(#3896),#2380,.F.);
#22727=ADVANCED_FACE('',(#3897),#2381,.F.);
#22728=ADVANCED_FACE('',(#3898),#2382,.F.);
#22729=ADVANCED_FACE('',(#3899),#2383,.F.);
#22730=ADVANCED_FACE('',(#3900),#2384,.F.);
#22731=ADVANCED_FACE('',(#3901),#2385,.F.);
#22732=ADVANCED_FACE('',(#3902),#2386,.F.);
#22733=ADVANCED_FACE('',(#3903),#2387,.F.);
#22734=ADVANCED_FACE('',(#3904),#2388,.F.);
#22735=ADVANCED_FACE('',(#3905),#2389,.F.);
#22736=ADVANCED_FACE('',(#3906),#2390,.F.);
#22737=ADVANCED_FACE('',(#3907),#2391,.F.);
#22738=ADVANCED_FACE('',(#3908),#2392,.T.);
#22739=ADVANCED_FACE('',(#3909),#21491,.T.);
#22740=ADVANCED_FACE('',(#3910),#21492,.T.);
#22741=ADVANCED_FACE('',(#3911),#2636,.T.);
#22742=ADVANCED_FACE('',(#3912),#21493,.T.);
#22743=ADVANCED_FACE('',(#3913,#1804),#2393,.T.);
#22822=CLOSED_SHELL('',(#22533,#22534,#22535,#22536,#22537,#22538,#22539,
#22540,#22541,#22542,#22543,#22544,#22545,#22546,#22547,#22548,#22549,#22550,
#22551,#22552,#22553,#22554,#22555,#22556,#22557,#22558,#22559,#22560,#22561,
#22562,#22563,#22564,#22565,#22566,#22567,#22568,#22569,#22570,#22571,#22572,
#22573,#22574,#22575,#22576,#22577,#22578,#22579,#22580,#22581,#22582,#22583,
#22584,#22585,#22586,#22587,#22588,#22589,#22590,#22591,#22592,#22593,#22594,
#22595,#22596,#22597,#22598,#22599,#22600,#22601,#22602,#22603,#22604,#22605,
#22606,#22607,#22608,#22609,#22610,#22611,#22612,#22613,#22614,#22615,#22616,
#22617,#22618,#22619,#22620,#22621,#22622,#22623,#22624,#22625,#22626,#22627,
#22628,#22629,#22630,#22631,#22632,#22633,#22634,#22635,#22636,#22637,#22638,
#22639,#22640,#22641,#22642,#22643,#22644,#22645,#22646,#22647,#22648,#22649,
#22650,#22651,#22652,#22653,#22654,#22655,#22656,#22657,#22658,#22659,#22660,
#22661,#22662,#22663,#22664,#22665,#22666,#22667,#22668,#22669,#22670,#22671,
#22672,#22673,#22674,#22675,#22676,#22677,#22678,#22679,#22680,#22681,#22682,
#22683,#22684,#22685,#22686,#22687,#22688,#22689,#22690,#22691,#22692,#22693,
#22694,#22695,#22696,#22697,#22698,#22699,#22700,#22701,#22702,#22703,#22704,
#22705,#22706,#22707,#22708,#22709,#22710,#22711,#22712,#22713,#22714,#22715,
#22716,#22717,#22718,#22719,#22720,#22721,#22722,#22723,#22724,#22725,#22726,
#22727,#22728,#22729,#22730,#22731,#22732,#22733,#22734,#22735,#22736,#22737,
#22738,#22739,#22740,#22741,#22742,#22743));
#24661=AXIS2_PLACEMENT_3D('',#48573,#29420,#29421);
#24662=AXIS2_PLACEMENT_3D('',#48574,#29422,#29423);
#24663=AXIS2_PLACEMENT_3D('',#48593,#29425,#29426);
#24664=AXIS2_PLACEMENT_3D('',#48596,#29428,#29429);
#24665=AXIS2_PLACEMENT_3D('',#48598,#29430,#29431);
#24666=AXIS2_PLACEMENT_3D('',#48609,#29432,#29433);
#24667=AXIS2_PLACEMENT_3D('',#48657,#29435,#29436);
#24668=AXIS2_PLACEMENT_3D('',#48705,#29438,#29439);
#24669=AXIS2_PLACEMENT_3D('',#48753,#29441,#29442);
#24670=AXIS2_PLACEMENT_3D('',#48807,#29444,#29445);
#24671=AXIS2_PLACEMENT_3D('',#48855,#29447,#29448);
#24672=AXIS2_PLACEMENT_3D('',#48903,#29450,#29451);
#24673=AXIS2_PLACEMENT_3D('',#48957,#29453,#29454);
#24674=AXIS2_PLACEMENT_3D('',#49005,#29456,#29457);
#24675=AXIS2_PLACEMENT_3D('',#49053,#29459,#29460);
#24676=AXIS2_PLACEMENT_3D('',#49101,#29462,#29463);
#24677=AXIS2_PLACEMENT_3D('',#49155,#29465,#29466);
#24678=AXIS2_PLACEMENT_3D('',#49203,#29468,#29469);
#24679=AXIS2_PLACEMENT_3D('',#49251,#29471,#29472);
#24680=AXIS2_PLACEMENT_3D('',#49305,#29474,#29475);
#24681=AXIS2_PLACEMENT_3D('',#49353,#29477,#29478);
#24682=AXIS2_PLACEMENT_3D('',#49401,#29480,#29481);
#24683=AXIS2_PLACEMENT_3D('',#49449,#29483,#29484);
#24684=AXIS2_PLACEMENT_3D('',#49503,#29486,#29487);
#24685=AXIS2_PLACEMENT_3D('',#49551,#29489,#29490);
#24686=AXIS2_PLACEMENT_3D('',#49599,#29492,#29493);
#24687=AXIS2_PLACEMENT_3D('',#49653,#29495,#29496);
#24688=AXIS2_PLACEMENT_3D('',#49658,#29498,#29499);
#24689=AXIS2_PLACEMENT_3D('',#49700,#29500,#29501);
#24690=AXIS2_PLACEMENT_3D('',#49713,#29503,#29504);
#24691=AXIS2_PLACEMENT_3D('',#49720,#29505,#29506);
#24692=AXIS2_PLACEMENT_3D('',#49745,#29508,#29509);
#24693=AXIS2_PLACEMENT_3D('',#49770,#29511,#29512);
#24694=AXIS2_PLACEMENT_3D('',#49794,#29514,#29515);
#24695=AXIS2_PLACEMENT_3D('',#49819,#29517,#29518);
#24696=AXIS2_PLACEMENT_3D('',#49844,#29520,#29521);
#24697=AXIS2_PLACEMENT_3D('',#49868,#29523,#29524);
#24698=AXIS2_PLACEMENT_3D('',#49892,#29526,#29527);
#24699=AXIS2_PLACEMENT_3D('',#49917,#29529,#29530);
#24700=AXIS2_PLACEMENT_3D('',#49942,#29532,#29533);
#24701=AXIS2_PLACEMENT_3D('',#49966,#29535,#29536);
#24702=AXIS2_PLACEMENT_3D('',#49991,#29538,#29539);
#24703=AXIS2_PLACEMENT_3D('',#50016,#29541,#29542);
#24704=AXIS2_PLACEMENT_3D('',#50040,#29544,#29545);
#24705=AXIS2_PLACEMENT_3D('',#50064,#29547,#29548);
#24706=AXIS2_PLACEMENT_3D('',#50089,#29550,#29551);
#24707=AXIS2_PLACEMENT_3D('',#50114,#29553,#29554);
#24708=AXIS2_PLACEMENT_3D('',#50138,#29556,#29557);
#24709=AXIS2_PLACEMENT_3D('',#50163,#29559,#29560);
#24710=AXIS2_PLACEMENT_3D('',#50188,#29562,#29563);
#24711=AXIS2_PLACEMENT_3D('',#50212,#29565,#29566);
#24712=AXIS2_PLACEMENT_3D('',#50236,#29568,#29569);
#24713=AXIS2_PLACEMENT_3D('',#50305,#29570,#29571);
#24714=AXIS2_PLACEMENT_3D('',#51033,#29572,#29573);
#24715=AXIS2_PLACEMENT_3D('',#51096,#29574,#29575);
#24716=AXIS2_PLACEMENT_3D('',#51097,#29576,#29577);
#24717=AXIS2_PLACEMENT_3D('',#51691,#29578,#29579);
#24718=AXIS2_PLACEMENT_3D('',#51692,#29580,#29581);
#24719=AXIS2_PLACEMENT_3D('',#51693,#29582,#29583);
#24720=AXIS2_PLACEMENT_3D('',#51695,#29584,#29585);
#24721=AXIS2_PLACEMENT_3D('',#51696,#29586,#29587);
#24722=AXIS2_PLACEMENT_3D('',#51697,#29588,#29589);
#24723=AXIS2_PLACEMENT_3D('',#51699,#29590,#29591);
#24724=AXIS2_PLACEMENT_3D('',#51700,#29592,#29593);
#24725=AXIS2_PLACEMENT_3D('',#51704,#29595,#29596);
#24726=AXIS2_PLACEMENT_3D('',#51705,#29597,#29598);
#24727=AXIS2_PLACEMENT_3D('',#51714,#29603,#29604);
#24728=AXIS2_PLACEMENT_3D('',#51720,#29608,#29609);
#24729=AXIS2_PLACEMENT_3D('',#51726,#29613,#29614);
#24730=AXIS2_PLACEMENT_3D('',#51732,#29618,#29619);
#24731=AXIS2_PLACEMENT_3D('',#51738,#29623,#29624);
#24732=AXIS2_PLACEMENT_3D('',#51741,#29627,#29628);
#24733=AXIS2_PLACEMENT_3D('',#51742,#29629,#29630);
#24734=AXIS2_PLACEMENT_3D('',#51751,#29635,#29636);
#24735=AXIS2_PLACEMENT_3D('',#51753,#29637,#29638);
#24736=AXIS2_PLACEMENT_3D('',#51755,#29640,#29641);
#24737=AXIS2_PLACEMENT_3D('',#51759,#29644,#29645);
#24738=AXIS2_PLACEMENT_3D('',#51760,#29646,#29647);
#24739=AXIS2_PLACEMENT_3D('',#51761,#29648,#29649);
#24740=AXIS2_PLACEMENT_3D('',#51770,#29654,#29655);
#24741=AXIS2_PLACEMENT_3D('',#51772,#29656,#29657);
#24742=AXIS2_PLACEMENT_3D('',#51774,#29659,#29660);
#24743=AXIS2_PLACEMENT_3D('',#51778,#29663,#29664);
#24744=AXIS2_PLACEMENT_3D('',#51779,#29665,#29666);
#24745=AXIS2_PLACEMENT_3D('',#51780,#29667,#29668);
#24746=AXIS2_PLACEMENT_3D('',#51789,#29673,#29674);
#24747=AXIS2_PLACEMENT_3D('',#51791,#29675,#29676);
#24748=AXIS2_PLACEMENT_3D('',#51793,#29678,#29679);
#24749=AXIS2_PLACEMENT_3D('',#51797,#29682,#29683);
#24750=AXIS2_PLACEMENT_3D('',#51798,#29684,#29685);
#24751=AXIS2_PLACEMENT_3D('',#51799,#29686,#29687);
#24752=AXIS2_PLACEMENT_3D('',#51808,#29692,#29693);
#24753=AXIS2_PLACEMENT_3D('',#51810,#29694,#29695);
#24754=AXIS2_PLACEMENT_3D('',#51812,#29697,#29698);
#24755=AXIS2_PLACEMENT_3D('',#51816,#29701,#29702);
#24756=AXIS2_PLACEMENT_3D('',#51817,#29703,#29704);
#24757=AXIS2_PLACEMENT_3D('',#51818,#29705,#29706);
#24758=AXIS2_PLACEMENT_3D('',#51827,#29711,#29712);
#24759=AXIS2_PLACEMENT_3D('',#51829,#29713,#29714);
#24760=AXIS2_PLACEMENT_3D('',#51831,#29716,#29717);
#24761=AXIS2_PLACEMENT_3D('',#51835,#29720,#29721);
#24762=AXIS2_PLACEMENT_3D('',#51836,#29722,#29723);
#24763=AXIS2_PLACEMENT_3D('',#51837,#29724,#29725);
#24764=AXIS2_PLACEMENT_3D('',#51846,#29730,#29731);
#24765=AXIS2_PLACEMENT_3D('',#51848,#29732,#29733);
#24766=AXIS2_PLACEMENT_3D('',#51850,#29735,#29736);
#24767=AXIS2_PLACEMENT_3D('',#51854,#29739,#29740);
#24768=AXIS2_PLACEMENT_3D('',#51855,#29741,#29742);
#24769=AXIS2_PLACEMENT_3D('',#51856,#29743,#29744);
#24770=AXIS2_PLACEMENT_3D('',#51865,#29749,#29750);
#24771=AXIS2_PLACEMENT_3D('',#51867,#29751,#29752);
#24772=AXIS2_PLACEMENT_3D('',#51869,#29754,#29755);
#24773=AXIS2_PLACEMENT_3D('',#51873,#29758,#29759);
#24774=AXIS2_PLACEMENT_3D('',#51874,#29760,#29761);
#24775=AXIS2_PLACEMENT_3D('',#51875,#29762,#29763);
#24776=AXIS2_PLACEMENT_3D('',#51884,#29768,#29769);
#24777=AXIS2_PLACEMENT_3D('',#51886,#29770,#29771);
#24778=AXIS2_PLACEMENT_3D('',#51888,#29773,#29774);
#24779=AXIS2_PLACEMENT_3D('',#51892,#29777,#29778);
#24780=AXIS2_PLACEMENT_3D('',#51893,#29779,#29780);
#24781=AXIS2_PLACEMENT_3D('',#51894,#29781,#29782);
#24782=AXIS2_PLACEMENT_3D('',#51903,#29787,#29788);
#24783=AXIS2_PLACEMENT_3D('',#51905,#29789,#29790);
#24784=AXIS2_PLACEMENT_3D('',#51908,#29792,#29793);
#24785=AXIS2_PLACEMENT_3D('',#51909,#29794,#29795);
#24786=AXIS2_PLACEMENT_3D('',#51913,#29798,#29799);
#24787=AXIS2_PLACEMENT_3D('',#51915,#29800,#29801);
#24788=AXIS2_PLACEMENT_3D('',#51916,#29802,#29803);
#24789=AXIS2_PLACEMENT_3D('',#51917,#29804,#29805);
#24790=AXIS2_PLACEMENT_3D('',#51926,#29810,#29811);
#24791=AXIS2_PLACEMENT_3D('',#51928,#29812,#29813);
#24792=AXIS2_PLACEMENT_3D('',#51930,#29815,#29816);
#24793=AXIS2_PLACEMENT_3D('',#51934,#29819,#29820);
#24794=AXIS2_PLACEMENT_3D('',#51935,#29821,#29822);
#24795=AXIS2_PLACEMENT_3D('',#51936,#29823,#29824);
#24796=AXIS2_PLACEMENT_3D('',#51945,#29829,#29830);
#24797=AXIS2_PLACEMENT_3D('',#51947,#29831,#29832);
#24798=AXIS2_PLACEMENT_3D('',#51949,#29834,#29835);
#24799=AXIS2_PLACEMENT_3D('',#51953,#29838,#29839);
#24800=AXIS2_PLACEMENT_3D('',#51954,#29840,#29841);
#24801=AXIS2_PLACEMENT_3D('',#51955,#29842,#29843);
#24802=AXIS2_PLACEMENT_3D('',#51964,#29848,#29849);
#24803=AXIS2_PLACEMENT_3D('',#51966,#29850,#29851);
#24804=AXIS2_PLACEMENT_3D('',#51968,#29853,#29854);
#24805=AXIS2_PLACEMENT_3D('',#51972,#29857,#29858);
#24806=AXIS2_PLACEMENT_3D('',#51973,#29859,#29860);
#24807=AXIS2_PLACEMENT_3D('',#51974,#29861,#29862);
#24808=AXIS2_PLACEMENT_3D('',#51983,#29867,#29868);
#24809=AXIS2_PLACEMENT_3D('',#51985,#29869,#29870);
#24810=AXIS2_PLACEMENT_3D('',#51987,#29872,#29873);
#24811=AXIS2_PLACEMENT_3D('',#51991,#29876,#29877);
#24812=AXIS2_PLACEMENT_3D('',#51992,#29878,#29879);
#24813=AXIS2_PLACEMENT_3D('',#51993,#29880,#29881);
#24814=AXIS2_PLACEMENT_3D('',#52002,#29886,#29887);
#24815=AXIS2_PLACEMENT_3D('',#52004,#29888,#29889);
#24816=AXIS2_PLACEMENT_3D('',#52006,#29891,#29892);
#24817=AXIS2_PLACEMENT_3D('',#52010,#29895,#29896);
#24818=AXIS2_PLACEMENT_3D('',#52011,#29897,#29898);
#24819=AXIS2_PLACEMENT_3D('',#52012,#29899,#29900);
#24820=AXIS2_PLACEMENT_3D('',#52021,#29905,#29906);
#24821=AXIS2_PLACEMENT_3D('',#52023,#29907,#29908);
#24822=AXIS2_PLACEMENT_3D('',#52025,#29910,#29911);
#24823=AXIS2_PLACEMENT_3D('',#52029,#29914,#29915);
#24824=AXIS2_PLACEMENT_3D('',#52030,#29916,#29917);
#24825=AXIS2_PLACEMENT_3D('',#52031,#29918,#29919);
#24826=AXIS2_PLACEMENT_3D('',#52040,#29924,#29925);
#24827=AXIS2_PLACEMENT_3D('',#52042,#29926,#29927);
#24828=AXIS2_PLACEMENT_3D('',#52044,#29929,#29930);
#24829=AXIS2_PLACEMENT_3D('',#52048,#29933,#29934);
#24830=AXIS2_PLACEMENT_3D('',#52049,#29935,#29936);
#24831=AXIS2_PLACEMENT_3D('',#52050,#29937,#29938);
#24832=AXIS2_PLACEMENT_3D('',#52059,#29943,#29944);
#24833=AXIS2_PLACEMENT_3D('',#52061,#29945,#29946);
#24834=AXIS2_PLACEMENT_3D('',#52063,#29948,#29949);
#24835=AXIS2_PLACEMENT_3D('',#52067,#29952,#29953);
#24836=AXIS2_PLACEMENT_3D('',#52068,#29954,#29955);
#24837=AXIS2_PLACEMENT_3D('',#52069,#29956,#29957);
#24838=AXIS2_PLACEMENT_3D('',#52078,#29962,#29963);
#24839=AXIS2_PLACEMENT_3D('',#52080,#29964,#29965);
#24840=AXIS2_PLACEMENT_3D('',#52082,#29967,#29968);
#24841=AXIS2_PLACEMENT_3D('',#52086,#29971,#29972);
#24842=AXIS2_PLACEMENT_3D('',#52087,#29973,#29974);
#24843=AXIS2_PLACEMENT_3D('',#52088,#29975,#29976);
#24844=AXIS2_PLACEMENT_3D('',#52097,#29981,#29982);
#24845=AXIS2_PLACEMENT_3D('',#52099,#29983,#29984);
#24846=AXIS2_PLACEMENT_3D('',#52101,#29986,#29987);
#24847=AXIS2_PLACEMENT_3D('',#52105,#29990,#29991);
#24848=AXIS2_PLACEMENT_3D('',#52106,#29992,#29993);
#24849=AXIS2_PLACEMENT_3D('',#52107,#29994,#29995);
#24850=AXIS2_PLACEMENT_3D('',#52116,#30000,#30001);
#24851=AXIS2_PLACEMENT_3D('',#52118,#30002,#30003);
#24852=AXIS2_PLACEMENT_3D('',#52120,#30005,#30006);
#24853=AXIS2_PLACEMENT_3D('',#52124,#30009,#30010);
#24854=AXIS2_PLACEMENT_3D('',#52125,#30011,#30012);
#24855=AXIS2_PLACEMENT_3D('',#52126,#30013,#30014);
#24856=AXIS2_PLACEMENT_3D('',#52135,#30019,#30020);
#24857=AXIS2_PLACEMENT_3D('',#52137,#30021,#30022);
#24858=AXIS2_PLACEMENT_3D('',#52139,#30024,#30025);
#24859=AXIS2_PLACEMENT_3D('',#52143,#30028,#30029);
#24860=AXIS2_PLACEMENT_3D('',#52144,#30030,#30031);
#24861=AXIS2_PLACEMENT_3D('',#52145,#30032,#30033);
#24862=AXIS2_PLACEMENT_3D('',#52154,#30038,#30039);
#24863=AXIS2_PLACEMENT_3D('',#52156,#30040,#30041);
#24864=AXIS2_PLACEMENT_3D('',#52158,#30043,#30044);
#24865=AXIS2_PLACEMENT_3D('',#52162,#30047,#30048);
#24866=AXIS2_PLACEMENT_3D('',#52163,#30049,#30050);
#24867=AXIS2_PLACEMENT_3D('',#52164,#30051,#30052);
#24868=AXIS2_PLACEMENT_3D('',#52173,#30057,#30058);
#24869=AXIS2_PLACEMENT_3D('',#52175,#30059,#30060);
#24870=AXIS2_PLACEMENT_3D('',#52177,#30062,#30063);
#24871=AXIS2_PLACEMENT_3D('',#52181,#30066,#30067);
#24872=AXIS2_PLACEMENT_3D('',#52182,#30068,#30069);
#24873=AXIS2_PLACEMENT_3D('',#52183,#30070,#30071);
#24874=AXIS2_PLACEMENT_3D('',#52192,#30076,#30077);
#24875=AXIS2_PLACEMENT_3D('',#52194,#30078,#30079);
#24876=AXIS2_PLACEMENT_3D('',#52196,#30081,#30082);
#24877=AXIS2_PLACEMENT_3D('',#52200,#30085,#30086);
#24878=AXIS2_PLACEMENT_3D('',#52201,#30087,#30088);
#24879=AXIS2_PLACEMENT_3D('',#52202,#30089,#30090);
#24880=AXIS2_PLACEMENT_3D('',#52211,#30095,#30096);
#24881=AXIS2_PLACEMENT_3D('',#52213,#30097,#30098);
#24882=AXIS2_PLACEMENT_3D('',#52215,#30100,#30101);
#24883=AXIS2_PLACEMENT_3D('',#52219,#30104,#30105);
#24884=AXIS2_PLACEMENT_3D('',#52220,#30106,#30107);
#24885=AXIS2_PLACEMENT_3D('',#52221,#30108,#30109);
#24886=AXIS2_PLACEMENT_3D('',#52230,#30114,#30115);
#24887=AXIS2_PLACEMENT_3D('',#52232,#30116,#30117);
#24888=AXIS2_PLACEMENT_3D('',#52234,#30119,#30120);
#24889=AXIS2_PLACEMENT_3D('',#52238,#30123,#30124);
#24890=AXIS2_PLACEMENT_3D('',#52239,#30125,#30126);
#24891=AXIS2_PLACEMENT_3D('',#52240,#30127,#30128);
#24892=AXIS2_PLACEMENT_3D('',#52243,#30129,#30130);
#24893=AXIS2_PLACEMENT_3D('',#52247,#30133,#30134);
#24894=AXIS2_PLACEMENT_3D('',#52253,#30138,#30139);
#24895=AXIS2_PLACEMENT_3D('',#52257,#30142,#30143);
#24896=AXIS2_PLACEMENT_3D('',#52258,#30144,#30145);
#24897=AXIS2_PLACEMENT_3D('',#52259,#30146,#30147);
#24898=AXIS2_PLACEMENT_3D('',#52268,#30152,#30153);
#24899=AXIS2_PLACEMENT_3D('',#52270,#30154,#30155);
#24900=AXIS2_PLACEMENT_3D('',#52272,#30157,#30158);
#24901=AXIS2_PLACEMENT_3D('',#52276,#30161,#30162);
#24902=AXIS2_PLACEMENT_3D('',#52277,#30163,#30164);
#24903=AXIS2_PLACEMENT_3D('',#52278,#30165,#30166);
#24904=AXIS2_PLACEMENT_3D('',#52287,#30171,#30172);
#24905=AXIS2_PLACEMENT_3D('',#52289,#30173,#30174);
#24906=AXIS2_PLACEMENT_3D('',#52291,#30176,#30177);
#24907=AXIS2_PLACEMENT_3D('',#52295,#30180,#30181);
#24908=AXIS2_PLACEMENT_3D('',#52296,#30182,#30183);
#24909=AXIS2_PLACEMENT_3D('',#52297,#30184,#30185);
#24910=AXIS2_PLACEMENT_3D('',#52306,#30190,#30191);
#24911=AXIS2_PLACEMENT_3D('',#52308,#30192,#30193);
#24912=AXIS2_PLACEMENT_3D('',#52310,#30195,#30196);
#24913=AXIS2_PLACEMENT_3D('',#52314,#30199,#30200);
#24914=AXIS2_PLACEMENT_3D('',#52315,#30201,#30202);
#24915=AXIS2_PLACEMENT_3D('',#52316,#30203,#30204);
#24916=AXIS2_PLACEMENT_3D('',#52325,#30209,#30210);
#24917=AXIS2_PLACEMENT_3D('',#52327,#30211,#30212);
#24918=AXIS2_PLACEMENT_3D('',#52329,#30214,#30215);
#24919=AXIS2_PLACEMENT_3D('',#52333,#30218,#30219);
#24920=AXIS2_PLACEMENT_3D('',#52334,#30220,#30221);
#24921=AXIS2_PLACEMENT_3D('',#52335,#30222,#30223);
#24922=AXIS2_PLACEMENT_3D('',#52344,#30228,#30229);
#24923=AXIS2_PLACEMENT_3D('',#52346,#30230,#30231);
#24924=AXIS2_PLACEMENT_3D('',#52348,#30233,#30234);
#24925=AXIS2_PLACEMENT_3D('',#52352,#30237,#30238);
#24926=AXIS2_PLACEMENT_3D('',#52353,#30239,#30240);
#24927=AXIS2_PLACEMENT_3D('',#52354,#30241,#30242);
#24928=AXIS2_PLACEMENT_3D('',#52363,#30247,#30248);
#24929=AXIS2_PLACEMENT_3D('',#52365,#30249,#30250);
#24930=AXIS2_PLACEMENT_3D('',#52367,#30252,#30253);
#24931=AXIS2_PLACEMENT_3D('',#52371,#30256,#30257);
#24932=AXIS2_PLACEMENT_3D('',#52372,#30258,#30259);
#24933=AXIS2_PLACEMENT_3D('',#52373,#30260,#30261);
#24934=AXIS2_PLACEMENT_3D('',#52382,#30266,#30267);
#24935=AXIS2_PLACEMENT_3D('',#52384,#30268,#30269);
#24936=AXIS2_PLACEMENT_3D('',#52386,#30271,#30272);
#24937=AXIS2_PLACEMENT_3D('',#52390,#30275,#30276);
#24938=AXIS2_PLACEMENT_3D('',#52391,#30277,#30278);
#24939=AXIS2_PLACEMENT_3D('',#52392,#30279,#30280);
#24940=AXIS2_PLACEMENT_3D('',#52401,#30285,#30286);
#24941=AXIS2_PLACEMENT_3D('',#52403,#30287,#30288);
#24942=AXIS2_PLACEMENT_3D('',#52405,#30290,#30291);
#24943=AXIS2_PLACEMENT_3D('',#52409,#30294,#30295);
#24944=AXIS2_PLACEMENT_3D('',#52410,#30296,#30297);
#24945=AXIS2_PLACEMENT_3D('',#52411,#30298,#30299);
#24946=AXIS2_PLACEMENT_3D('',#52420,#30304,#30305);
#24947=AXIS2_PLACEMENT_3D('',#52422,#30306,#30307);
#24948=AXIS2_PLACEMENT_3D('',#52424,#30309,#30310);
#24949=AXIS2_PLACEMENT_3D('',#52428,#30313,#30314);
#24950=AXIS2_PLACEMENT_3D('',#52429,#30315,#30316);
#24951=AXIS2_PLACEMENT_3D('',#52430,#30317,#30318);
#24952=AXIS2_PLACEMENT_3D('',#52432,#30319,#30320);
#24953=AXIS2_PLACEMENT_3D('',#52433,#30321,#30322);
#24954=AXIS2_PLACEMENT_3D('',#52435,#30324,#30325);
#24955=AXIS2_PLACEMENT_3D('',#52437,#30326,#30327);
#24956=AXIS2_PLACEMENT_3D('',#52439,#30329,#30330);
#24957=AXIS2_PLACEMENT_3D('',#52440,#30331,#30332);
#24958=AXIS2_PLACEMENT_3D('',#52441,#30333,#30334);
#24959=AXIS2_PLACEMENT_3D('',#52442,#30335,#30336);
#24960=AXIS2_PLACEMENT_3D('',#52443,#30337,#30338);
#24961=AXIS2_PLACEMENT_3D('',#52444,#30339,#30340);
#24962=AXIS2_PLACEMENT_3D('',#52445,#30341,#30342);
#24963=AXIS2_PLACEMENT_3D('',#52446,#30343,#30344);
#24964=AXIS2_PLACEMENT_3D('',#52447,#30345,#30346);
#24965=AXIS2_PLACEMENT_3D('',#52448,#30347,#30348);
#24966=AXIS2_PLACEMENT_3D('',#52449,#30349,#30350);
#24967=AXIS2_PLACEMENT_3D('',#52450,#30351,#30352);
#24968=AXIS2_PLACEMENT_3D('',#52451,#30353,#30354);
#24969=AXIS2_PLACEMENT_3D('',#52452,#30355,#30356);
#24970=AXIS2_PLACEMENT_3D('',#52453,#30357,#30358);
#24971=AXIS2_PLACEMENT_3D('',#52454,#30359,#30360);
#24972=AXIS2_PLACEMENT_3D('',#52455,#30361,#30362);
#24973=AXIS2_PLACEMENT_3D('',#52457,#30364,#30365);
#24974=AXIS2_PLACEMENT_3D('',#52458,#30366,#30367);
#24975=AXIS2_PLACEMENT_3D('',#52459,#30368,#30369);
#24976=AXIS2_PLACEMENT_3D('',#52460,#30370,#30371);
#24977=AXIS2_PLACEMENT_3D('',#52461,#30372,#30373);
#24978=AXIS2_PLACEMENT_3D('',#52462,#30374,#30375);
#24979=AXIS2_PLACEMENT_3D('',#52463,#30376,#30377);
#24980=AXIS2_PLACEMENT_3D('',#52464,#30378,#30379);
#24981=AXIS2_PLACEMENT_3D('',#52465,#30380,#30381);
#24982=AXIS2_PLACEMENT_3D('',#52466,#30382,#30383);
#24983=AXIS2_PLACEMENT_3D('',#52467,#30384,#30385);
#24984=AXIS2_PLACEMENT_3D('',#52468,#30386,#30387);
#24985=AXIS2_PLACEMENT_3D('',#52469,#30388,#30389);
#24986=AXIS2_PLACEMENT_3D('',#52470,#30390,#30391);
#24987=AXIS2_PLACEMENT_3D('',#52471,#30392,#30393);
#24988=AXIS2_PLACEMENT_3D('',#52472,#30394,#30395);
#24989=AXIS2_PLACEMENT_3D('',#52473,#30396,#30397);
#24990=AXIS2_PLACEMENT_3D('',#52474,#30398,#30399);
#24991=AXIS2_PLACEMENT_3D('',#52475,#30400,#30401);
#24992=AXIS2_PLACEMENT_3D('',#52476,#30402,#30403);
#24993=AXIS2_PLACEMENT_3D('',#52477,#30404,#30405);
#24994=AXIS2_PLACEMENT_3D('',#52479,#30406,#30407);
#24995=AXIS2_PLACEMENT_3D('',#52481,#30409,#30410);
#29420=DIRECTION('axis',(0.,0.,1.));
#29421=DIRECTION('refdir',(1.,0.,0.));
#29422=DIRECTION('center_axis',(0.,0.,1.));
#29423=DIRECTION('ref_axis',(1.,0.,0.));
#29424=DIRECTION('',(0.,0.,-1.));
#29425=DIRECTION('center_axis',(0.,0.,-1.));
#29426=DIRECTION('ref_axis',(1.,0.,0.));
#29427=DIRECTION('',(0.,0.,-1.));
#29428=DIRECTION('center_axis',(0.,0.,1.));
#29429=DIRECTION('ref_axis',(1.,0.,0.));
#29430=DIRECTION('center_axis',(0.,0.,-1.));
#29431=DIRECTION('ref_axis',(1.,0.,0.));
#29432=DIRECTION('center_axis',(0.,0.,1.));
#29433=DIRECTION('ref_axis',(1.,0.,0.));
#29434=DIRECTION('',(0.,0.,-1.));
#29435=DIRECTION('center_axis',(0.,0.,1.));
#29436=DIRECTION('ref_axis',(1.,0.,0.));
#29437=DIRECTION('',(0.,0.,-1.));
#29438=DIRECTION('center_axis',(0.,0.,1.));
#29439=DIRECTION('ref_axis',(1.,0.,0.));
#29440=DIRECTION('',(0.,0.,-1.));
#29441=DIRECTION('center_axis',(0.,0.,1.));
#29442=DIRECTION('ref_axis',(1.,0.,0.));
#29443=DIRECTION('',(0.,0.,-1.));
#29444=DIRECTION('center_axis',(0.,0.,1.));
#29445=DIRECTION('ref_axis',(1.,0.,0.));
#29446=DIRECTION('',(0.,0.,-1.));
#29447=DIRECTION('center_axis',(0.,0.,1.));
#29448=DIRECTION('ref_axis',(1.,0.,0.));
#29449=DIRECTION('',(0.,0.,-1.));
#29450=DIRECTION('center_axis',(0.,0.,1.));
#29451=DIRECTION('ref_axis',(1.,0.,0.));
#29452=DIRECTION('',(0.,0.,-1.));
#29453=DIRECTION('center_axis',(0.,0.,1.));
#29454=DIRECTION('ref_axis',(1.,0.,0.));
#29455=DIRECTION('',(0.,0.,-1.));
#29456=DIRECTION('center_axis',(0.,0.,1.));
#29457=DIRECTION('ref_axis',(1.,0.,0.));
#29458=DIRECTION('',(0.,0.,-1.));
#29459=DIRECTION('center_axis',(0.,0.,1.));
#29460=DIRECTION('ref_axis',(1.,0.,0.));
#29461=DIRECTION('',(0.,0.,-1.));
#29462=DIRECTION('center_axis',(0.,0.,1.));
#29463=DIRECTION('ref_axis',(1.,0.,0.));
#29464=DIRECTION('',(0.,0.,-1.));
#29465=DIRECTION('center_axis',(0.,0.,1.));
#29466=DIRECTION('ref_axis',(1.,0.,0.));
#29467=DIRECTION('',(0.,0.,-1.));
#29468=DIRECTION('center_axis',(0.,0.,1.));
#29469=DIRECTION('ref_axis',(1.,0.,0.));
#29470=DIRECTION('',(0.,0.,-1.));
#29471=DIRECTION('center_axis',(0.,0.,1.));
#29472=DIRECTION('ref_axis',(1.,0.,0.));
#29473=DIRECTION('',(0.,0.,-1.));
#29474=DIRECTION('center_axis',(0.,0.,1.));
#29475=DIRECTION('ref_axis',(1.,0.,0.));
#29476=DIRECTION('',(0.,0.,-1.));
#29477=DIRECTION('center_axis',(0.,0.,1.));
#29478=DIRECTION('ref_axis',(1.,0.,0.));
#29479=DIRECTION('',(0.,0.,-1.));
#29480=DIRECTION('center_axis',(0.,0.,1.));
#29481=DIRECTION('ref_axis',(1.,0.,0.));
#29482=DIRECTION('',(0.,0.,-1.));
#29483=DIRECTION('center_axis',(0.,0.,1.));
#29484=DIRECTION('ref_axis',(1.,0.,0.));
#29485=DIRECTION('',(0.,0.,-1.));
#29486=DIRECTION('center_axis',(0.,0.,1.));
#29487=DIRECTION('ref_axis',(1.,0.,0.));
#29488=DIRECTION('',(0.,0.,-1.));
#29489=DIRECTION('center_axis',(0.,0.,1.));
#29490=DIRECTION('ref_axis',(1.,0.,0.));
#29491=DIRECTION('',(0.,0.,-1.));
#29492=DIRECTION('center_axis',(0.,0.,1.));
#29493=DIRECTION('ref_axis',(1.,0.,0.));
#29494=DIRECTION('',(0.,0.,-1.));
#29495=DIRECTION('center_axis',(0.,0.,1.));
#29496=DIRECTION('ref_axis',(1.,0.,0.));
#29497=DIRECTION('',(0.,0.,-1.));
#29498=DIRECTION('center_axis',(0.,0.,1.));
#29499=DIRECTION('ref_axis',(1.,0.,0.));
#29500=DIRECTION('center_axis',(0.,0.,1.));
#29501=DIRECTION('ref_axis',(0.315430408607799,-0.948948711641213,0.));
#29502=DIRECTION('',(0.,0.,1.));
#29503=DIRECTION('center_axis',(0.,0.,1.));
#29504=DIRECTION('ref_axis',(1.,4.63459159752748E-15,0.));
#29505=DIRECTION('center_axis',(0.,0.,1.));
#29506=DIRECTION('ref_axis',(1.,4.63459159752748E-15,0.));
#29507=DIRECTION('',(0.,0.,1.));
#29508=DIRECTION('center_axis',(0.,0.,1.));
#29509=DIRECTION('ref_axis',(1.,4.63459159752748E-15,0.));
#29510=DIRECTION('',(0.,0.,1.));
#29511=DIRECTION('center_axis',(0.,0.,1.));
#29512=DIRECTION('ref_axis',(1.,4.63459159752748E-15,0.));
#29513=DIRECTION('',(0.,0.,1.));
#29514=DIRECTION('center_axis',(0.,0.,1.));
#29515=DIRECTION('ref_axis',(1.,4.63459159752748E-15,0.));
#29516=DIRECTION('',(0.,0.,1.));
#29517=DIRECTION('center_axis',(0.,0.,1.));
#29518=DIRECTION('ref_axis',(1.,4.63459159752748E-15,0.));
#29519=DIRECTION('',(0.,0.,1.));
#29520=DIRECTION('center_axis',(0.,0.,1.));
#29521=DIRECTION('ref_axis',(1.,4.63459159752748E-15,0.));
#29522=DIRECTION('',(0.,0.,1.));
#29523=DIRECTION('center_axis',(0.,0.,1.));
#29524=DIRECTION('ref_axis',(1.,4.63459159752748E-15,0.));
#29525=DIRECTION('',(0.,0.,1.));
#29526=DIRECTION('center_axis',(0.,0.,1.));
#29527=DIRECTION('ref_axis',(1.,4.63459159752748E-15,0.));
#29528=DIRECTION('',(0.,0.,1.));
#29529=DIRECTION('center_axis',(0.,0.,1.));
#29530=DIRECTION('ref_axis',(1.,4.63459159752748E-15,0.));
#29531=DIRECTION('',(0.,0.,1.));
#29532=DIRECTION('center_axis',(0.,0.,1.));
#29533=DIRECTION('ref_axis',(1.,4.63459159752748E-15,0.));
#29534=DIRECTION('',(0.,0.,1.));
#29535=DIRECTION('center_axis',(0.,0.,1.));
#29536=DIRECTION('ref_axis',(1.,4.63459159752748E-15,0.));
#29537=DIRECTION('',(0.,0.,1.));
#29538=DIRECTION('center_axis',(0.,0.,1.));
#29539=DIRECTION('ref_axis',(1.,4.63459159752748E-15,0.));
#29540=DIRECTION('',(0.,0.,1.));
#29541=DIRECTION('center_axis',(0.,0.,1.));
#29542=DIRECTION('ref_axis',(1.,4.63459159752748E-15,0.));
#29543=DIRECTION('',(0.,0.,1.));
#29544=DIRECTION('center_axis',(0.,0.,1.));
#29545=DIRECTION('ref_axis',(1.,4.63459159752748E-15,0.));
#29546=DIRECTION('',(0.,0.,1.));
#29547=DIRECTION('center_axis',(0.,0.,1.));
#29548=DIRECTION('ref_axis',(1.,4.63459159752748E-15,0.));
#29549=DIRECTION('',(0.,0.,1.));
#29550=DIRECTION('center_axis',(0.,0.,1.));
#29551=DIRECTION('ref_axis',(1.,4.63459159752748E-15,0.));
#29552=DIRECTION('',(0.,0.,1.));
#29553=DIRECTION('center_axis',(0.,0.,1.));
#29554=DIRECTION('ref_axis',(1.,4.63459159752748E-15,0.));
#29555=DIRECTION('',(0.,0.,1.));
#29556=DIRECTION('center_axis',(0.,0.,1.));
#29557=DIRECTION('ref_axis',(1.,4.63459159752748E-15,0.));
#29558=DIRECTION('',(0.,0.,1.));
#29559=DIRECTION('center_axis',(0.,0.,1.));
#29560=DIRECTION('ref_axis',(1.,4.63459159752748E-15,0.));
#29561=DIRECTION('',(0.,0.,1.));
#29562=DIRECTION('center_axis',(0.,0.,1.));
#29563=DIRECTION('ref_axis',(1.,4.63459159752748E-15,0.));
#29564=DIRECTION('',(0.,0.,1.));
#29565=DIRECTION('center_axis',(0.,0.,1.));
#29566=DIRECTION('ref_axis',(1.,4.63459159752748E-15,0.));
#29567=DIRECTION('',(0.,0.,1.));
#29568=DIRECTION('center_axis',(0.,0.,1.));
#29569=DIRECTION('ref_axis',(1.,0.,0.));
#29570=DIRECTION('center_axis',(0.,0.,1.));
#29571=DIRECTION('ref_axis',(1.,0.,0.));
#29572=DIRECTION('center_axis',(0.,0.,1.));
#29573=DIRECTION('ref_axis',(1.,0.,0.));
#29574=DIRECTION('center_axis',(0.,0.,-1.));
#29575=DIRECTION('ref_axis',(1.,4.63459159752748E-15,0.));
#29576=DIRECTION('center_axis',(0.,0.,1.));
#29577=DIRECTION('ref_axis',(1.,4.63459159752748E-15,0.));
#29578=DIRECTION('center_axis',(0.,0.,1.));
#29579=DIRECTION('ref_axis',(-0.970925317856845,-0.239382595742849,0.));
#29580=DIRECTION('center_axis',(0.,0.,1.));
#29581=DIRECTION('ref_axis',(1.,0.,0.));
#29582=DIRECTION('center_axis',(0.,0.,1.));
#29583=DIRECTION('ref_axis',(1.,0.,0.));
#29584=DIRECTION('center_axis',(1.22464679914735E-16,-1.,0.));
#29585=DIRECTION('ref_axis',(-1.,-1.22464679914735E-16,0.));
#29586=DIRECTION('center_axis',(0.,0.,-1.));
#29587=DIRECTION('ref_axis',(1.,0.,0.));
#29588=DIRECTION('center_axis',(0.,0.,-1.));
#29589=DIRECTION('ref_axis',(-1.,0.,0.));
#29590=DIRECTION('center_axis',(0.,0.,1.));
#29591=DIRECTION('ref_axis',(1.,0.,0.));
#29592=DIRECTION('center_axis',(0.,0.,1.));
#29593=DIRECTION('ref_axis',(1.,0.,0.));
#29594=DIRECTION('',(-0.8574862672191,-1.05011781246268E-16,0.514506852753833));
#29595=DIRECTION('center_axis',(0.,0.,-1.));
#29596=DIRECTION('ref_axis',(1.,0.,0.));
#29597=DIRECTION('center_axis',(0.866025403784439,0.5,0.));
#29598=DIRECTION('ref_axis',(0.5,-0.866025403784439,0.));
#29599=DIRECTION('',(0.5,-0.866025403784439,0.));
#29600=DIRECTION('',(0.,0.,-1.));
#29601=DIRECTION('',(0.5,-0.866025403784439,0.));
#29602=DIRECTION('',(0.,0.,-1.));
#29603=DIRECTION('center_axis',(1.60246890531964E-16,1.,0.));
#29604=DIRECTION('ref_axis',(1.,-1.60246890531964E-16,0.));
#29605=DIRECTION('',(1.,-1.60246890531964E-16,0.));
#29606=DIRECTION('',(0.,0.,-1.));
#29607=DIRECTION('',(1.,-1.60246890531964E-16,0.));
#29608=DIRECTION('center_axis',(-0.866025403784439,0.5,0.));
#29609=DIRECTION('ref_axis',(0.5,0.866025403784439,0.));
#29610=DIRECTION('',(0.5,0.866025403784439,0.));
#29611=DIRECTION('',(0.,0.,-1.));
#29612=DIRECTION('',(0.5,0.866025403784439,0.));
#29613=DIRECTION('center_axis',(-0.866025403784439,-0.5,0.));
#29614=DIRECTION('ref_axis',(-0.5,0.866025403784439,0.));
#29615=DIRECTION('',(-0.5,0.866025403784439,0.));
#29616=DIRECTION('',(0.,0.,-1.));
#29617=DIRECTION('',(-0.5,0.866025403784439,0.));
#29618=DIRECTION('center_axis',(-1.60246890531964E-16,-1.,0.));
#29619=DIRECTION('ref_axis',(-1.,1.60246890531964E-16,0.));
#29620=DIRECTION('',(-1.,1.60246890531964E-16,0.));
#29621=DIRECTION('',(0.,0.,-1.));
#29622=DIRECTION('',(-1.,1.60246890531964E-16,0.));
#29623=DIRECTION('center_axis',(0.866025403784439,-0.5,0.));
#29624=DIRECTION('ref_axis',(-0.5,-0.866025403784439,0.));
#29625=DIRECTION('',(-0.5,-0.866025403784439,0.));
#29626=DIRECTION('',(-0.5,-0.866025403784439,0.));
#29627=DIRECTION('center_axis',(0.,0.,-1.));
#29628=DIRECTION('ref_axis',(-1.,0.,0.));
#29629=DIRECTION('center_axis',(-0.738540092256147,-0.674209560989966,0.));
#29630=DIRECTION('ref_axis',(-0.674209560989966,0.738540092256147,0.));
#29631=DIRECTION('',(0.,0.,1.));
#29632=DIRECTION('',(-0.674209560989966,0.738540092256147,0.));
#29633=DIRECTION('',(0.,0.,-1.));
#29634=DIRECTION('',(-0.674209560989966,0.738540092256147,0.));
#29635=DIRECTION('center_axis',(0.,0.,1.));
#29636=DIRECTION('ref_axis',(1.,0.,0.));
#29637=DIRECTION('center_axis',(0.,0.,1.));
#29638=DIRECTION('ref_axis',(1.,0.,0.));
#29639=DIRECTION('',(0.991198908253055,0.132380981556841,0.));
#29640=DIRECTION('center_axis',(-0.132380981556841,0.991198908253055,0.));
#29641=DIRECTION('ref_axis',(0.991198908253055,0.132380981556841,0.));
#29642=DIRECTION('',(0.,0.,-1.));
#29643=DIRECTION('',(0.991198908253055,0.132380981556841,0.));
#29644=DIRECTION('center_axis',(0.,0.,-1.));
#29645=DIRECTION('ref_axis',(-1.,0.,0.));
#29646=DIRECTION('center_axis',(0.,0.,-1.));
#29647=DIRECTION('ref_axis',(1.,0.,0.));
#29648=DIRECTION('center_axis',(-0.924593925528967,-0.380954161120384,0.));
#29649=DIRECTION('ref_axis',(-0.380954161120384,0.924593925528967,0.));
#29650=DIRECTION('',(0.,0.,1.));
#29651=DIRECTION('',(-0.380954161120384,0.924593925528967,0.));
#29652=DIRECTION('',(0.,0.,-1.));
#29653=DIRECTION('',(-0.380954161120384,0.924593925528967,0.));
#29654=DIRECTION('center_axis',(0.,0.,1.));
#29655=DIRECTION('ref_axis',(1.,0.,0.));
#29656=DIRECTION('center_axis',(0.,0.,1.));
#29657=DIRECTION('ref_axis',(1.,0.,0.));
#29658=DIRECTION('',(0.976699262102109,-0.214612561163589,0.));
#29659=DIRECTION('center_axis',(0.214612561163589,0.976699262102109,0.));
#29660=DIRECTION('ref_axis',(0.976699262102109,-0.214612561163589,0.));
#29661=DIRECTION('',(0.,0.,-1.));
#29662=DIRECTION('',(0.976699262102109,-0.214612561163589,0.));
#29663=DIRECTION('center_axis',(0.,0.,-1.));
#29664=DIRECTION('ref_axis',(-1.,0.,0.));
#29665=DIRECTION('center_axis',(0.,0.,-1.));
#29666=DIRECTION('ref_axis',(1.,0.,0.));
#29667=DIRECTION('center_axis',(-0.99912808582995,-0.0417500671350421,0.));
#29668=DIRECTION('ref_axis',(-0.0417500671350421,0.99912808582995,0.));
#29669=DIRECTION('',(0.,0.,1.));
#29670=DIRECTION('',(-0.0417500671350421,0.99912808582995,0.));
#29671=DIRECTION('',(0.,0.,-1.));
#29672=DIRECTION('',(-0.0417500671350421,0.99912808582995,0.));
#29673=DIRECTION('center_axis',(0.,0.,1.));
#29674=DIRECTION('ref_axis',(1.,0.,0.));
#29675=DIRECTION('center_axis',(0.,0.,1.));
#29676=DIRECTION('ref_axis',(1.,0.,0.));
#29677=DIRECTION('',(0.84439527039573,-0.535720661663634,0.));
#29678=DIRECTION('center_axis',(0.535720661663634,0.84439527039573,0.));
#29679=DIRECTION('ref_axis',(0.84439527039573,-0.535720661663634,0.));
#29680=DIRECTION('',(0.,0.,-1.));
#29681=DIRECTION('',(0.84439527039573,-0.535720661663634,0.));
#29682=DIRECTION('center_axis',(0.,0.,-1.));
#29683=DIRECTION('ref_axis',(-1.,0.,0.));
#29684=DIRECTION('center_axis',(0.,0.,-1.));
#29685=DIRECTION('ref_axis',(1.,0.,0.));
#29686=DIRECTION('center_axis',(-0.953152653419739,0.302489701112138,0.));
#29687=DIRECTION('ref_axis',(0.302489701112138,0.953152653419739,0.));
#29688=DIRECTION('',(0.,0.,1.));
#29689=DIRECTION('',(0.302489701112138,0.953152653419739,0.));
#29690=DIRECTION('',(0.,0.,-1.));
#29691=DIRECTION('',(0.302489701112138,0.953152653419739,0.));
#29692=DIRECTION('center_axis',(0.,0.,1.));
#29693=DIRECTION('ref_axis',(1.,0.,0.));
#29694=DIRECTION('center_axis',(0.,0.,1.));
#29695=DIRECTION('ref_axis',(1.,0.,0.));
#29696=DIRECTION('',(0.610244747132677,-0.792212943972121,0.));
#29697=DIRECTION('center_axis',(0.792212943972121,0.610244747132677,0.));
#29698=DIRECTION('ref_axis',(0.610244747132677,-0.792212943972121,0.));
#29699=DIRECTION('',(0.,0.,-1.));
#29700=DIRECTION('',(0.610244747132677,-0.792212943972121,0.));
#29701=DIRECTION('center_axis',(0.,0.,-1.));
#29702=DIRECTION('ref_axis',(-1.,0.,0.));
#29703=DIRECTION('center_axis',(0.,0.,-1.));
#29704=DIRECTION('ref_axis',(1.,0.,0.));
#29705=DIRECTION('center_axis',(-0.792212943972121,0.610244747132677,0.));
#29706=DIRECTION('ref_axis',(0.610244747132677,0.792212943972121,0.));
#29707=DIRECTION('',(0.,0.,1.));
#29708=DIRECTION('',(0.610244747132677,0.792212943972121,0.));
#29709=DIRECTION('',(0.,0.,-1.));
#29710=DIRECTION('',(0.610244747132677,0.792212943972121,0.));
#29711=DIRECTION('center_axis',(0.,0.,1.));
#29712=DIRECTION('ref_axis',(1.,0.,0.));
#29713=DIRECTION('center_axis',(0.,0.,1.));
#29714=DIRECTION('ref_axis',(1.,0.,0.));
#29715=DIRECTION('',(0.302489701112144,-0.953152653419737,0.));
#29716=DIRECTION('center_axis',(0.953152653419737,0.302489701112144,0.));
#29717=DIRECTION('ref_axis',(0.302489701112144,-0.953152653419737,0.));
#29718=DIRECTION('',(0.,0.,-1.));
#29719=DIRECTION('',(0.302489701112144,-0.953152653419737,0.));
#29720=DIRECTION('center_axis',(0.,0.,-1.));
#29721=DIRECTION('ref_axis',(-1.,0.,0.));
#29722=DIRECTION('center_axis',(0.,0.,-1.));
#29723=DIRECTION('ref_axis',(1.,0.,0.));
#29724=DIRECTION('center_axis',(-0.535720661663633,0.844395270395731,0.));
#29725=DIRECTION('ref_axis',(0.844395270395731,0.535720661663633,0.));
#29726=DIRECTION('',(0.,0.,1.));
#29727=DIRECTION('',(0.844395270395731,0.535720661663633,0.));
#29728=DIRECTION('',(0.,0.,-1.));
#29729=DIRECTION('',(0.844395270395731,0.535720661663633,0.));
#29730=DIRECTION('center_axis',(0.,0.,1.));
#29731=DIRECTION('ref_axis',(1.,0.,0.));
#29732=DIRECTION('center_axis',(0.,0.,1.));
#29733=DIRECTION('ref_axis',(1.,0.,0.));
#29734=DIRECTION('',(-0.0417500671350428,-0.99912808582995,0.));
#29735=DIRECTION('center_axis',(0.99912808582995,-0.0417500671350428,0.));
#29736=DIRECTION('ref_axis',(-0.0417500671350428,-0.99912808582995,0.));
#29737=DIRECTION('',(0.,0.,-1.));
#29738=DIRECTION('',(-0.0417500671350428,-0.99912808582995,0.));
#29739=DIRECTION('center_axis',(0.,0.,-1.));
#29740=DIRECTION('ref_axis',(-1.,0.,0.));
#29741=DIRECTION('center_axis',(0.,0.,-1.));
#29742=DIRECTION('ref_axis',(1.,0.,0.));
#29743=DIRECTION('center_axis',(-0.214612561163593,0.976699262102108,0.));
#29744=DIRECTION('ref_axis',(0.976699262102108,0.214612561163593,0.));
#29745=DIRECTION('',(0.,0.,1.));
#29746=DIRECTION('',(0.976699262102108,0.214612561163593,0.));
#29747=DIRECTION('',(0.,0.,-1.));
#29748=DIRECTION('',(0.976699262102108,0.214612561163593,0.));
#29749=DIRECTION('center_axis',(0.,0.,1.));
#29750=DIRECTION('ref_axis',(1.,0.,0.));
#29751=DIRECTION('center_axis',(0.,0.,1.));
#29752=DIRECTION('ref_axis',(1.,0.,0.));
#29753=DIRECTION('',(-0.38095416112038,-0.924593925528968,0.));
#29754=DIRECTION('center_axis',(0.924593925528968,-0.38095416112038,0.));
#29755=DIRECTION('ref_axis',(-0.38095416112038,-0.924593925528968,0.));
#29756=DIRECTION('',(0.,0.,-1.));
#29757=DIRECTION('',(-0.38095416112038,-0.924593925528968,0.));
#29758=DIRECTION('center_axis',(0.,0.,-1.));
#29759=DIRECTION('ref_axis',(-1.,0.,0.));
#29760=DIRECTION('center_axis',(0.,0.,-1.));
#29761=DIRECTION('ref_axis',(1.,0.,0.));
#29762=DIRECTION('center_axis',(0.132380981556845,0.991198908253054,0.));
#29763=DIRECTION('ref_axis',(0.991198908253054,-0.132380981556845,0.));
#29764=DIRECTION('',(0.,0.,1.));
#29765=DIRECTION('',(0.991198908253054,-0.132380981556845,0.));
#29766=DIRECTION('',(0.,0.,-1.));
#29767=DIRECTION('',(0.991198908253054,-0.132380981556845,0.));
#29768=DIRECTION('center_axis',(0.,0.,1.));
#29769=DIRECTION('ref_axis',(1.,0.,0.));
#29770=DIRECTION('center_axis',(0.,0.,1.));
#29771=DIRECTION('ref_axis',(1.,0.,0.));
#29772=DIRECTION('',(-0.674209560989967,-0.738540092256145,0.));
#29773=DIRECTION('center_axis',(0.738540092256145,-0.674209560989967,0.));
#29774=DIRECTION('ref_axis',(-0.674209560989967,-0.738540092256145,0.));
#29775=DIRECTION('',(0.,0.,-1.));
#29776=DIRECTION('',(-0.674209560989967,-0.738540092256145,0.));
#29777=DIRECTION('center_axis',(0.,0.,-1.));
#29778=DIRECTION('ref_axis',(-1.,0.,0.));
#29779=DIRECTION('center_axis',(0.,0.,-1.));
#29780=DIRECTION('ref_axis',(1.,0.,0.));
#29781=DIRECTION('center_axis',(0.463407424166319,0.886145337530779,0.));
#29782=DIRECTION('ref_axis',(0.886145337530779,-0.463407424166319,0.));
#29783=DIRECTION('',(0.,0.,1.));
#29784=DIRECTION('',(0.886145337530779,-0.463407424166319,0.));
#29785=DIRECTION('',(0.,0.,-1.));
#29786=DIRECTION('',(0.886145337530779,-0.463407424166319,0.));
#29787=DIRECTION('center_axis',(0.,0.,1.));
#29788=DIRECTION('ref_axis',(1.,0.,0.));
#29789=DIRECTION('center_axis',(0.,0.,1.));
#29790=DIRECTION('ref_axis',(1.,0.,0.));
#29791=DIRECTION('',(-0.886145337530779,-0.463407424166319,0.));
#29792=DIRECTION('center_axis',(0.,0.,1.));
#29793=DIRECTION('ref_axis',(1.,0.,0.));
#29794=DIRECTION('center_axis',(0.463407424166319,-0.886145337530779,0.));
#29795=DIRECTION('ref_axis',(-0.886145337530779,-0.463407424166319,0.));
#29796=DIRECTION('',(0.,0.,-1.));
#29797=DIRECTION('',(-0.886145337530779,-0.463407424166319,0.));
#29798=DIRECTION('center_axis',(0.,0.,-1.));
#29799=DIRECTION('ref_axis',(-1.,0.,0.));
#29800=DIRECTION('center_axis',(0.,0.,-1.));
#29801=DIRECTION('ref_axis',(1.,0.,0.));
#29802=DIRECTION('center_axis',(0.,0.,-1.));
#29803=DIRECTION('ref_axis',(1.,0.,0.));
#29804=DIRECTION('center_axis',(0.610244747132677,0.792212943972121,0.));
#29805=DIRECTION('ref_axis',(0.792212943972121,-0.610244747132677,0.));
#29806=DIRECTION('',(0.,0.,1.));
#29807=DIRECTION('',(0.792212943972121,-0.610244747132677,0.));
#29808=DIRECTION('',(0.,0.,-1.));
#29809=DIRECTION('',(0.792212943972121,-0.610244747132677,0.));
#29810=DIRECTION('center_axis',(0.,0.,1.));
#29811=DIRECTION('ref_axis',(1.,0.,0.));
#29812=DIRECTION('center_axis',(0.,0.,1.));
#29813=DIRECTION('ref_axis',(1.,0.,0.));
#29814=DIRECTION('',(-0.953152653419738,-0.302489701112141,0.));
#29815=DIRECTION('center_axis',(0.302489701112141,-0.953152653419738,0.));
#29816=DIRECTION('ref_axis',(-0.953152653419738,-0.302489701112141,0.));
#29817=DIRECTION('',(0.,0.,-1.));
#29818=DIRECTION('',(-0.953152653419738,-0.302489701112141,0.));
#29819=DIRECTION('center_axis',(0.,0.,-1.));
#29820=DIRECTION('ref_axis',(-1.,0.,0.));
#29821=DIRECTION('center_axis',(0.,0.,-1.));
#29822=DIRECTION('ref_axis',(1.,0.,0.));
#29823=DIRECTION('center_axis',(0.844395270395734,0.535720661663628,0.));
#29824=DIRECTION('ref_axis',(0.535720661663628,-0.844395270395734,0.));
#29825=DIRECTION('',(0.,0.,1.));
#29826=DIRECTION('',(0.535720661663628,-0.844395270395734,0.));
#29827=DIRECTION('',(0.,0.,-1.));
#29828=DIRECTION('',(0.535720661663628,-0.844395270395734,0.));
#29829=DIRECTION('center_axis',(0.,0.,1.));
#29830=DIRECTION('ref_axis',(1.,0.,0.));
#29831=DIRECTION('center_axis',(0.,0.,1.));
#29832=DIRECTION('ref_axis',(1.,0.,0.));
#29833=DIRECTION('',(-0.99912808582995,0.0417500671350472,0.));
#29834=DIRECTION('center_axis',(-0.0417500671350472,-0.99912808582995,0.));
#29835=DIRECTION('ref_axis',(-0.99912808582995,0.0417500671350472,0.));
#29836=DIRECTION('',(0.,0.,-1.));
#29837=DIRECTION('',(-0.99912808582995,0.0417500671350472,0.));
#29838=DIRECTION('center_axis',(0.,0.,-1.));
#29839=DIRECTION('ref_axis',(-1.,0.,0.));
#29840=DIRECTION('center_axis',(0.,0.,-1.));
#29841=DIRECTION('ref_axis',(1.,0.,0.));
#29842=DIRECTION('center_axis',(0.976699262102109,0.214612561163593,0.));
#29843=DIRECTION('ref_axis',(0.214612561163593,-0.976699262102109,0.));
#29844=DIRECTION('',(0.,0.,1.));
#29845=DIRECTION('',(0.214612561163593,-0.976699262102109,0.));
#29846=DIRECTION('',(0.,0.,-1.));
#29847=DIRECTION('',(0.214612561163593,-0.976699262102109,0.));
#29848=DIRECTION('center_axis',(0.,0.,1.));
#29849=DIRECTION('ref_axis',(1.,0.,0.));
#29850=DIRECTION('center_axis',(0.,0.,1.));
#29851=DIRECTION('ref_axis',(1.,0.,0.));
#29852=DIRECTION('',(-0.924593925528968,0.38095416112038,0.));
#29853=DIRECTION('center_axis',(-0.38095416112038,-0.924593925528968,0.));
#29854=DIRECTION('ref_axis',(-0.924593925528968,0.38095416112038,0.));
#29855=DIRECTION('',(0.,0.,-1.));
#29856=DIRECTION('',(-0.924593925528968,0.38095416112038,0.));
#29857=DIRECTION('center_axis',(0.,0.,-1.));
#29858=DIRECTION('ref_axis',(-1.,0.,0.));
#29859=DIRECTION('center_axis',(0.,0.,-1.));
#29860=DIRECTION('ref_axis',(1.,0.,0.));
#29861=DIRECTION('center_axis',(0.991198908253054,-0.132380981556846,0.));
#29862=DIRECTION('ref_axis',(-0.132380981556846,-0.991198908253054,0.));
#29863=DIRECTION('',(0.,0.,1.));
#29864=DIRECTION('',(-0.132380981556846,-0.991198908253054,0.));
#29865=DIRECTION('',(0.,0.,-1.));
#29866=DIRECTION('',(-0.132380981556846,-0.991198908253054,0.));
#29867=DIRECTION('center_axis',(0.,0.,1.));
#29868=DIRECTION('ref_axis',(1.,0.,0.));
#29869=DIRECTION('center_axis',(0.,0.,1.));
#29870=DIRECTION('ref_axis',(1.,0.,0.));
#29871=DIRECTION('',(-0.738540092256146,0.674209560989966,0.));
#29872=DIRECTION('center_axis',(-0.674209560989966,-0.738540092256146,0.));
#29873=DIRECTION('ref_axis',(-0.738540092256146,0.674209560989966,0.));
#29874=DIRECTION('',(0.,0.,-1.));
#29875=DIRECTION('',(-0.738540092256146,0.674209560989966,0.));
#29876=DIRECTION('center_axis',(0.,0.,-1.));
#29877=DIRECTION('ref_axis',(-1.,0.,0.));
#29878=DIRECTION('center_axis',(0.,0.,-1.));
#29879=DIRECTION('ref_axis',(1.,0.,0.));
#29880=DIRECTION('center_axis',(0.886145337530778,-0.46340742416632,0.));
#29881=DIRECTION('ref_axis',(-0.46340742416632,-0.886145337530778,0.));
#29882=DIRECTION('',(0.,0.,1.));
#29883=DIRECTION('',(-0.46340742416632,-0.886145337530778,0.));
#29884=DIRECTION('',(0.,0.,-1.));
#29885=DIRECTION('',(-0.46340742416632,-0.886145337530778,0.));
#29886=DIRECTION('center_axis',(0.,0.,1.));
#29887=DIRECTION('ref_axis',(1.,0.,0.));
#29888=DIRECTION('center_axis',(0.,0.,1.));
#29889=DIRECTION('ref_axis',(1.,0.,0.));
#29890=DIRECTION('',(-0.46340742416632,0.886145337530778,0.));
#29891=DIRECTION('center_axis',(-0.886145337530778,-0.46340742416632,0.));
#29892=DIRECTION('ref_axis',(-0.46340742416632,0.886145337530778,0.));
#29893=DIRECTION('',(0.,0.,-1.));
#29894=DIRECTION('',(-0.46340742416632,0.886145337530778,0.));
#29895=DIRECTION('center_axis',(0.,0.,-1.));
#29896=DIRECTION('ref_axis',(-1.,0.,0.));
#29897=DIRECTION('center_axis',(0.,0.,-1.));
#29898=DIRECTION('ref_axis',(1.,0.,0.));
#29899=DIRECTION('center_axis',(0.674209560989967,-0.738540092256145,0.));
#29900=DIRECTION('ref_axis',(-0.738540092256145,-0.674209560989967,0.));
#29901=DIRECTION('',(0.,0.,1.));
#29902=DIRECTION('',(-0.738540092256145,-0.674209560989967,0.));
#29903=DIRECTION('',(0.,0.,-1.));
#29904=DIRECTION('',(-0.738540092256145,-0.674209560989967,0.));
#29905=DIRECTION('center_axis',(0.,0.,1.));
#29906=DIRECTION('ref_axis',(1.,0.,0.));
#29907=DIRECTION('center_axis',(0.,0.,1.));
#29908=DIRECTION('ref_axis',(1.,0.,0.));
#29909=DIRECTION('',(-0.132380981556847,0.991198908253054,0.));
#29910=DIRECTION('center_axis',(-0.991198908253054,-0.132380981556847,0.));
#29911=DIRECTION('ref_axis',(-0.132380981556847,0.991198908253054,0.));
#29912=DIRECTION('',(0.,0.,-1.));
#29913=DIRECTION('',(-0.132380981556847,0.991198908253054,0.));
#29914=DIRECTION('center_axis',(0.,0.,-1.));
#29915=DIRECTION('ref_axis',(-1.,0.,0.));
#29916=DIRECTION('center_axis',(0.,0.,-1.));
#29917=DIRECTION('ref_axis',(1.,0.,0.));
#29918=DIRECTION('center_axis',(0.380954161120379,-0.924593925528969,0.));
#29919=DIRECTION('ref_axis',(-0.924593925528969,-0.380954161120379,0.));
#29920=DIRECTION('',(0.,0.,1.));
#29921=DIRECTION('',(-0.924593925528969,-0.380954161120379,0.));
#29922=DIRECTION('',(0.,0.,-1.));
#29923=DIRECTION('',(-0.924593925528969,-0.380954161120379,0.));
#29924=DIRECTION('center_axis',(0.,0.,1.));
#29925=DIRECTION('ref_axis',(1.,0.,0.));
#29926=DIRECTION('center_axis',(0.,0.,1.));
#29927=DIRECTION('ref_axis',(1.,0.,0.));
#29928=DIRECTION('',(0.214612561163592,0.976699262102109,0.));
#29929=DIRECTION('center_axis',(-0.976699262102109,0.214612561163592,0.));
#29930=DIRECTION('ref_axis',(0.214612561163592,0.976699262102109,0.));
#29931=DIRECTION('',(0.,0.,-1.));
#29932=DIRECTION('',(0.214612561163592,0.976699262102109,0.));
#29933=DIRECTION('center_axis',(0.,0.,-1.));
#29934=DIRECTION('ref_axis',(-1.,0.,0.));
#29935=DIRECTION('center_axis',(0.,0.,-1.));
#29936=DIRECTION('ref_axis',(1.,0.,0.));
#29937=DIRECTION('center_axis',(0.0417500671350458,-0.99912808582995,0.));
#29938=DIRECTION('ref_axis',(-0.99912808582995,-0.0417500671350458,0.));
#29939=DIRECTION('',(0.,0.,1.));
#29940=DIRECTION('',(-0.99912808582995,-0.0417500671350458,0.));
#29941=DIRECTION('',(0.,0.,-1.));
#29942=DIRECTION('',(-0.99912808582995,-0.0417500671350458,0.));
#29943=DIRECTION('center_axis',(0.,0.,1.));
#29944=DIRECTION('ref_axis',(1.,0.,0.));
#29945=DIRECTION('center_axis',(0.,0.,1.));
#29946=DIRECTION('ref_axis',(1.,0.,0.));
#29947=DIRECTION('',(0.535720661663629,0.844395270395733,0.));
#29948=DIRECTION('center_axis',(-0.844395270395733,0.535720661663629,0.));
#29949=DIRECTION('ref_axis',(0.535720661663629,0.844395270395733,0.));
#29950=DIRECTION('',(0.,0.,-1.));
#29951=DIRECTION('',(0.535720661663629,0.844395270395733,0.));
#29952=DIRECTION('center_axis',(0.,0.,-1.));
#29953=DIRECTION('ref_axis',(-1.,0.,0.));
#29954=DIRECTION('center_axis',(0.,0.,-1.));
#29955=DIRECTION('ref_axis',(1.,0.,0.));
#29956=DIRECTION('center_axis',(-0.302489701112142,-0.953152653419738,0.));
#29957=DIRECTION('ref_axis',(-0.953152653419738,0.302489701112142,0.));
#29958=DIRECTION('',(0.,0.,1.));
#29959=DIRECTION('',(-0.953152653419738,0.302489701112142,0.));
#29960=DIRECTION('',(0.,0.,-1.));
#29961=DIRECTION('',(-0.953152653419738,0.302489701112142,0.));
#29962=DIRECTION('center_axis',(0.,0.,1.));
#29963=DIRECTION('ref_axis',(1.,0.,0.));
#29964=DIRECTION('center_axis',(0.,0.,1.));
#29965=DIRECTION('ref_axis',(1.,0.,0.));
#29966=DIRECTION('',(0.792212943972123,0.610244747132675,0.));
#29967=DIRECTION('center_axis',(-0.610244747132675,0.792212943972123,0.));
#29968=DIRECTION('ref_axis',(0.792212943972123,0.610244747132675,0.));
#29969=DIRECTION('',(0.,0.,-1.));
#29970=DIRECTION('',(0.792212943972123,0.610244747132675,0.));
#29971=DIRECTION('center_axis',(0.,0.,-1.));
#29972=DIRECTION('ref_axis',(-1.,0.,0.));
#29973=DIRECTION('center_axis',(0.,0.,-1.));
#29974=DIRECTION('ref_axis',(1.,0.,0.));
#29975=DIRECTION('center_axis',(-0.132380981556845,-0.991198908253054,0.));
#29976=DIRECTION('ref_axis',(-0.991198908253054,0.132380981556845,0.));
#29977=DIRECTION('',(0.,0.,1.));
#29978=DIRECTION('',(-0.991198908253054,0.132380981556845,0.));
#29979=DIRECTION('',(0.,0.,-1.));
#29980=DIRECTION('',(-0.991198908253054,0.132380981556845,0.));
#29981=DIRECTION('center_axis',(0.,0.,1.));
#29982=DIRECTION('ref_axis',(1.,0.,0.));
#29983=DIRECTION('center_axis',(0.,0.,1.));
#29984=DIRECTION('ref_axis',(1.,0.,0.));
#29985=DIRECTION('',(0.674209560989966,0.738540092256146,0.));
#29986=DIRECTION('center_axis',(-0.738540092256146,0.674209560989966,0.));
#29987=DIRECTION('ref_axis',(0.674209560989966,0.738540092256146,0.));
#29988=DIRECTION('',(0.,0.,-1.));
#29989=DIRECTION('',(0.674209560989966,0.738540092256146,0.));
#29990=DIRECTION('center_axis',(0.,0.,-1.));
#29991=DIRECTION('ref_axis',(-1.,0.,0.));
#29992=DIRECTION('center_axis',(0.,0.,-1.));
#29993=DIRECTION('ref_axis',(1.,0.,0.));
#29994=DIRECTION('center_axis',(0.214612561163592,-0.976699262102109,0.));
#29995=DIRECTION('ref_axis',(-0.976699262102109,-0.214612561163592,0.));
#29996=DIRECTION('',(0.,0.,1.));
#29997=DIRECTION('',(-0.976699262102109,-0.214612561163592,0.));
#29998=DIRECTION('',(0.,0.,-1.));
#29999=DIRECTION('',(-0.976699262102109,-0.214612561163592,0.));
#30000=DIRECTION('center_axis',(0.,0.,1.));
#30001=DIRECTION('ref_axis',(1.,0.,0.));
#30002=DIRECTION('center_axis',(0.,0.,1.));
#30003=DIRECTION('ref_axis',(1.,0.,0.));
#30004=DIRECTION('',(0.380954161120378,0.924593925528969,0.));
#30005=DIRECTION('center_axis',(-0.924593925528969,0.380954161120378,0.));
#30006=DIRECTION('ref_axis',(0.380954161120378,0.924593925528969,0.));
#30007=DIRECTION('',(0.,0.,-1.));
#30008=DIRECTION('',(0.380954161120378,0.924593925528969,0.));
#30009=DIRECTION('center_axis',(0.,0.,-1.));
#30010=DIRECTION('ref_axis',(-1.,0.,0.));
#30011=DIRECTION('center_axis',(0.,0.,-1.));
#30012=DIRECTION('ref_axis',(1.,0.,0.));
#30013=DIRECTION('center_axis',(0.53572066166363,-0.844395270395733,0.));
#30014=DIRECTION('ref_axis',(-0.844395270395733,-0.53572066166363,0.));
#30015=DIRECTION('',(0.,0.,1.));
#30016=DIRECTION('',(-0.844395270395733,-0.53572066166363,0.));
#30017=DIRECTION('',(0.,0.,-1.));
#30018=DIRECTION('',(-0.844395270395733,-0.53572066166363,0.));
#30019=DIRECTION('center_axis',(0.,0.,1.));
#30020=DIRECTION('ref_axis',(1.,0.,0.));
#30021=DIRECTION('center_axis',(0.,0.,1.));
#30022=DIRECTION('ref_axis',(1.,0.,0.));
#30023=DIRECTION('',(0.0417500671350451,0.99912808582995,0.));
#30024=DIRECTION('center_axis',(-0.99912808582995,0.0417500671350451,0.));
#30025=DIRECTION('ref_axis',(0.0417500671350451,0.99912808582995,0.));
#30026=DIRECTION('',(0.,0.,-1.));
#30027=DIRECTION('',(0.0417500671350451,0.99912808582995,0.));
#30028=DIRECTION('center_axis',(0.,0.,-1.));
#30029=DIRECTION('ref_axis',(-1.,0.,0.));
#30030=DIRECTION('center_axis',(0.,0.,-1.));
#30031=DIRECTION('ref_axis',(1.,0.,0.));
#30032=DIRECTION('center_axis',(0.792212943972124,-0.610244747132674,0.));
#30033=DIRECTION('ref_axis',(-0.610244747132674,-0.792212943972124,0.));
#30034=DIRECTION('',(0.,0.,1.));
#30035=DIRECTION('',(-0.610244747132674,-0.792212943972124,0.));
#30036=DIRECTION('',(0.,0.,-1.));
#30037=DIRECTION('',(-0.610244747132674,-0.792212943972124,0.));
#30038=DIRECTION('center_axis',(0.,0.,1.));
#30039=DIRECTION('ref_axis',(1.,0.,0.));
#30040=DIRECTION('center_axis',(0.,0.,1.));
#30041=DIRECTION('ref_axis',(1.,0.,0.));
#30042=DIRECTION('',(-0.302489701112143,0.953152653419738,0.));
#30043=DIRECTION('center_axis',(-0.953152653419738,-0.302489701112143,0.));
#30044=DIRECTION('ref_axis',(-0.302489701112143,0.953152653419738,0.));
#30045=DIRECTION('',(0.,0.,-1.));
#30046=DIRECTION('',(-0.302489701112143,0.953152653419738,0.));
#30047=DIRECTION('center_axis',(0.,0.,-1.));
#30048=DIRECTION('ref_axis',(-1.,0.,0.));
#30049=DIRECTION('center_axis',(0.,0.,-1.));
#30050=DIRECTION('ref_axis',(1.,0.,0.));
#30051=DIRECTION('center_axis',(0.953152653419738,-0.302489701112143,0.));
#30052=DIRECTION('ref_axis',(-0.302489701112143,-0.953152653419738,0.));
#30053=DIRECTION('',(0.,0.,1.));
#30054=DIRECTION('',(-0.302489701112143,-0.953152653419738,0.));
#30055=DIRECTION('',(0.,0.,-1.));
#30056=DIRECTION('',(-0.302489701112143,-0.953152653419738,0.));
#30057=DIRECTION('center_axis',(0.,0.,1.));
#30058=DIRECTION('ref_axis',(1.,0.,0.));
#30059=DIRECTION('center_axis',(0.,0.,1.));
#30060=DIRECTION('ref_axis',(1.,0.,0.));
#30061=DIRECTION('',(-0.610244747132675,0.792212943972123,0.));
#30062=DIRECTION('center_axis',(-0.792212943972123,-0.610244747132675,0.));
#30063=DIRECTION('ref_axis',(-0.610244747132675,0.792212943972123,0.));
#30064=DIRECTION('',(0.,0.,-1.));
#30065=DIRECTION('',(-0.610244747132675,0.792212943972123,0.));
#30066=DIRECTION('center_axis',(0.,0.,-1.));
#30067=DIRECTION('ref_axis',(-1.,0.,0.));
#30068=DIRECTION('center_axis',(0.,0.,-1.));
#30069=DIRECTION('ref_axis',(1.,0.,0.));
#30070=DIRECTION('center_axis',(0.99912808582995,0.0417500671350458,0.));
#30071=DIRECTION('ref_axis',(0.0417500671350458,-0.99912808582995,0.));
#30072=DIRECTION('',(0.,0.,1.));
#30073=DIRECTION('',(0.0417500671350458,-0.99912808582995,0.));
#30074=DIRECTION('',(0.,0.,-1.));
#30075=DIRECTION('',(0.0417500671350458,-0.99912808582995,0.));
#30076=DIRECTION('center_axis',(0.,0.,1.));
#30077=DIRECTION('ref_axis',(1.,0.,0.));
#30078=DIRECTION('center_axis',(0.,0.,1.));
#30079=DIRECTION('ref_axis',(1.,0.,0.));
#30080=DIRECTION('',(-0.844395270395734,0.535720661663629,0.));
#30081=DIRECTION('center_axis',(-0.535720661663629,-0.844395270395734,0.));
#30082=DIRECTION('ref_axis',(-0.844395270395734,0.535720661663629,0.));
#30083=DIRECTION('',(0.,0.,-1.));
#30084=DIRECTION('',(-0.844395270395734,0.535720661663629,0.));
#30085=DIRECTION('center_axis',(0.,0.,-1.));
#30086=DIRECTION('ref_axis',(-1.,0.,0.));
#30087=DIRECTION('center_axis',(0.,0.,-1.));
#30088=DIRECTION('ref_axis',(1.,0.,0.));
#30089=DIRECTION('center_axis',(0.924593925528969,0.380954161120379,0.));
#30090=DIRECTION('ref_axis',(0.380954161120379,-0.924593925528969,0.));
#30091=DIRECTION('',(0.,0.,1.));
#30092=DIRECTION('',(0.380954161120379,-0.924593925528969,0.));
#30093=DIRECTION('',(0.,0.,-1.));
#30094=DIRECTION('',(0.380954161120379,-0.924593925528969,0.));
#30095=DIRECTION('center_axis',(0.,0.,1.));
#30096=DIRECTION('ref_axis',(1.,0.,0.));
#30097=DIRECTION('center_axis',(0.,0.,1.));
#30098=DIRECTION('ref_axis',(1.,0.,0.));
#30099=DIRECTION('',(-0.976699262102109,0.214612561163589,0.));
#30100=DIRECTION('center_axis',(-0.214612561163589,-0.976699262102109,0.));
#30101=DIRECTION('ref_axis',(-0.976699262102109,0.214612561163589,0.));
#30102=DIRECTION('',(0.,0.,-1.));
#30103=DIRECTION('',(-0.976699262102109,0.214612561163589,0.));
#30104=DIRECTION('center_axis',(0.,0.,-1.));
#30105=DIRECTION('ref_axis',(-1.,0.,0.));
#30106=DIRECTION('center_axis',(0.,0.,-1.));
#30107=DIRECTION('ref_axis',(1.,0.,0.));
#30108=DIRECTION('center_axis',(0.738540092256146,0.674209560989967,0.));
#30109=DIRECTION('ref_axis',(0.674209560989967,-0.738540092256146,0.));
#30110=DIRECTION('',(0.,0.,1.));
#30111=DIRECTION('',(0.674209560989967,-0.738540092256146,0.));
#30112=DIRECTION('',(0.,0.,-1.));
#30113=DIRECTION('',(0.674209560989967,-0.738540092256146,0.));
#30114=DIRECTION('center_axis',(0.,0.,1.));
#30115=DIRECTION('ref_axis',(1.,0.,0.));
#30116=DIRECTION('center_axis',(0.,0.,1.));
#30117=DIRECTION('ref_axis',(1.,0.,0.));
#30118=DIRECTION('',(-0.991198908253054,-0.132380981556849,0.));
#30119=DIRECTION('center_axis',(0.132380981556849,-0.991198908253054,0.));
#30120=DIRECTION('ref_axis',(-0.991198908253054,-0.132380981556849,0.));
#30121=DIRECTION('',(0.,0.,-1.));
#30122=DIRECTION('',(-0.991198908253054,-0.132380981556849,0.));
#30123=DIRECTION('center_axis',(0.,0.,-1.));
#30124=DIRECTION('ref_axis',(-1.,0.,0.));
#30125=DIRECTION('center_axis',(0.,0.,-1.));
#30126=DIRECTION('ref_axis',(1.,0.,0.));
#30127=DIRECTION('center_axis',(0.,0.,1.));
#30128=DIRECTION('ref_axis',(1.,0.,0.));
#30129=DIRECTION('center_axis',(0.,0.,1.));
#30130=DIRECTION('ref_axis',(1.,0.,0.));
#30131=DIRECTION('',(-0.886145337530778,0.46340742416632,0.));
#30132=DIRECTION('',(0.886145337530778,0.46340742416632,0.));
#30133=DIRECTION('center_axis',(-0.46340742416632,-0.886145337530778,0.));
#30134=DIRECTION('ref_axis',(-0.886145337530778,0.46340742416632,0.));
#30135=DIRECTION('',(0.,0.,1.));
#30136=DIRECTION('',(-0.886145337530778,0.46340742416632,0.));
#30137=DIRECTION('',(0.,0.,-1.));
#30138=DIRECTION('center_axis',(-0.46340742416632,0.886145337530778,0.));
#30139=DIRECTION('ref_axis',(0.886145337530778,0.46340742416632,0.));
#30140=DIRECTION('',(0.,0.,-1.));
#30141=DIRECTION('',(0.886145337530778,0.46340742416632,0.));
#30142=DIRECTION('center_axis',(0.,0.,-1.));
#30143=DIRECTION('ref_axis',(-1.,0.,0.));
#30144=DIRECTION('center_axis',(0.,0.,-1.));
#30145=DIRECTION('ref_axis',(1.,0.,0.));
#30146=DIRECTION('center_axis',(0.302489701112144,0.953152653419737,0.));
#30147=DIRECTION('ref_axis',(0.953152653419737,-0.302489701112144,0.));
#30148=DIRECTION('',(0.,0.,1.));
#30149=DIRECTION('',(0.953152653419737,-0.302489701112144,0.));
#30150=DIRECTION('',(0.,0.,-1.));
#30151=DIRECTION('',(0.953152653419737,-0.302489701112144,0.));
#30152=DIRECTION('center_axis',(0.,0.,1.));
#30153=DIRECTION('ref_axis',(1.,0.,0.));
#30154=DIRECTION('center_axis',(0.,0.,1.));
#30155=DIRECTION('ref_axis',(1.,0.,0.));
#30156=DIRECTION('',(-0.792212943972123,-0.610244747132674,0.));
#30157=DIRECTION('center_axis',(0.610244747132674,-0.792212943972123,0.));
#30158=DIRECTION('ref_axis',(-0.792212943972123,-0.610244747132674,0.));
#30159=DIRECTION('',(0.,0.,-1.));
#30160=DIRECTION('',(-0.792212943972123,-0.610244747132674,0.));
#30161=DIRECTION('center_axis',(0.,0.,-1.));
#30162=DIRECTION('ref_axis',(-1.,0.,0.));
#30163=DIRECTION('center_axis',(0.,0.,-1.));
#30164=DIRECTION('ref_axis',(1.,0.,0.));
#30165=DIRECTION('center_axis',(-0.0417500671350422,0.99912808582995,0.));
#30166=DIRECTION('ref_axis',(0.99912808582995,0.0417500671350422,0.));
#30167=DIRECTION('',(0.,0.,1.));
#30168=DIRECTION('',(0.99912808582995,0.0417500671350422,0.));
#30169=DIRECTION('',(0.,0.,-1.));
#30170=DIRECTION('',(0.99912808582995,0.0417500671350422,0.));
#30171=DIRECTION('center_axis',(0.,0.,1.));
#30172=DIRECTION('ref_axis',(1.,0.,0.));
#30173=DIRECTION('center_axis',(0.,0.,1.));
#30174=DIRECTION('ref_axis',(1.,0.,0.));
#30175=DIRECTION('',(-0.53572066166363,-0.844395270395733,0.));
#30176=DIRECTION('center_axis',(0.844395270395733,-0.53572066166363,0.));
#30177=DIRECTION('ref_axis',(-0.53572066166363,-0.844395270395733,0.));
#30178=DIRECTION('',(0.,0.,-1.));
#30179=DIRECTION('',(-0.53572066166363,-0.844395270395733,0.));
#30180=DIRECTION('center_axis',(0.,0.,-1.));
#30181=DIRECTION('ref_axis',(-1.,0.,0.));
#30182=DIRECTION('center_axis',(0.,0.,-1.));
#30183=DIRECTION('ref_axis',(1.,0.,0.));
#30184=DIRECTION('center_axis',(-0.380954161120378,0.924593925528969,0.));
#30185=DIRECTION('ref_axis',(0.924593925528969,0.380954161120378,0.));
#30186=DIRECTION('',(0.,0.,1.));
#30187=DIRECTION('',(0.924593925528969,0.380954161120378,0.));
#30188=DIRECTION('',(0.,0.,-1.));
#30189=DIRECTION('',(0.924593925528969,0.380954161120378,0.));
#30190=DIRECTION('center_axis',(0.,0.,1.));
#30191=DIRECTION('ref_axis',(1.,0.,0.));
#30192=DIRECTION('center_axis',(0.,0.,1.));
#30193=DIRECTION('ref_axis',(1.,0.,0.));
#30194=DIRECTION('',(-0.214612561163591,-0.976699262102109,0.));
#30195=DIRECTION('center_axis',(0.976699262102109,-0.214612561163591,0.));
#30196=DIRECTION('ref_axis',(-0.214612561163591,-0.976699262102109,0.));
#30197=DIRECTION('',(0.,0.,-1.));
#30198=DIRECTION('',(-0.214612561163591,-0.976699262102109,0.));
#30199=DIRECTION('center_axis',(0.,0.,-1.));
#30200=DIRECTION('ref_axis',(-1.,0.,0.));
#30201=DIRECTION('center_axis',(0.,0.,-1.));
#30202=DIRECTION('ref_axis',(1.,0.,0.));
#30203=DIRECTION('center_axis',(-0.674209560989966,0.738540092256147,0.));
#30204=DIRECTION('ref_axis',(0.738540092256147,0.674209560989966,0.));
#30205=DIRECTION('',(0.,0.,1.));
#30206=DIRECTION('',(0.738540092256147,0.674209560989966,0.));
#30207=DIRECTION('',(0.,0.,-1.));
#30208=DIRECTION('',(0.738540092256147,0.674209560989966,0.));
#30209=DIRECTION('center_axis',(0.,0.,1.));
#30210=DIRECTION('ref_axis',(1.,0.,0.));
#30211=DIRECTION('center_axis',(0.,0.,1.));
#30212=DIRECTION('ref_axis',(1.,0.,0.));
#30213=DIRECTION('',(0.132380981556841,-0.991198908253055,0.));
#30214=DIRECTION('center_axis',(0.991198908253055,0.132380981556841,0.));
#30215=DIRECTION('ref_axis',(0.132380981556841,-0.991198908253055,0.));
#30216=DIRECTION('',(0.,0.,-1.));
#30217=DIRECTION('',(0.132380981556841,-0.991198908253055,0.));
#30218=DIRECTION('center_axis',(0.,0.,-1.));
#30219=DIRECTION('ref_axis',(-1.,0.,0.));
#30220=DIRECTION('center_axis',(0.,0.,-1.));
#30221=DIRECTION('ref_axis',(1.,0.,0.));
#30222=DIRECTION('center_axis',(-0.886145337530777,0.463407424166322,0.));
#30223=DIRECTION('ref_axis',(0.463407424166322,0.886145337530777,0.));
#30224=DIRECTION('',(0.,0.,1.));
#30225=DIRECTION('',(0.463407424166322,0.886145337530777,0.));
#30226=DIRECTION('',(0.,0.,-1.));
#30227=DIRECTION('',(0.463407424166322,0.886145337530777,0.));
#30228=DIRECTION('center_axis',(0.,0.,1.));
#30229=DIRECTION('ref_axis',(1.,0.,0.));
#30230=DIRECTION('center_axis',(0.,0.,1.));
#30231=DIRECTION('ref_axis',(1.,0.,0.));
#30232=DIRECTION('',(0.463407424166322,-0.886145337530777,0.));
#30233=DIRECTION('center_axis',(0.886145337530777,0.463407424166322,0.));
#30234=DIRECTION('ref_axis',(0.463407424166322,-0.886145337530777,0.));
#30235=DIRECTION('',(0.,0.,-1.));
#30236=DIRECTION('',(0.463407424166322,-0.886145337530777,0.));
#30237=DIRECTION('center_axis',(0.,0.,-1.));
#30238=DIRECTION('ref_axis',(-1.,0.,0.));
#30239=DIRECTION('center_axis',(0.,0.,-1.));
#30240=DIRECTION('ref_axis',(1.,0.,0.));
#30241=DIRECTION('center_axis',(-0.991198908253054,0.132380981556848,0.));
#30242=DIRECTION('ref_axis',(0.132380981556848,0.991198908253054,0.));
#30243=DIRECTION('',(0.,0.,1.));
#30244=DIRECTION('',(0.132380981556848,0.991198908253054,0.));
#30245=DIRECTION('',(0.,0.,-1.));
#30246=DIRECTION('',(0.132380981556848,0.991198908253054,0.));
#30247=DIRECTION('center_axis',(0.,0.,1.));
#30248=DIRECTION('ref_axis',(1.,0.,0.));
#30249=DIRECTION('center_axis',(0.,0.,1.));
#30250=DIRECTION('ref_axis',(1.,0.,0.));
#30251=DIRECTION('',(0.738540092256143,-0.67420956098997,0.));
#30252=DIRECTION('center_axis',(0.67420956098997,0.738540092256143,0.));
#30253=DIRECTION('ref_axis',(0.738540092256143,-0.67420956098997,0.));
#30254=DIRECTION('',(0.,0.,-1.));
#30255=DIRECTION('',(0.738540092256143,-0.67420956098997,0.));
#30256=DIRECTION('center_axis',(0.,0.,-1.));
#30257=DIRECTION('ref_axis',(-1.,0.,0.));
#30258=DIRECTION('center_axis',(0.,0.,-1.));
#30259=DIRECTION('ref_axis',(1.,0.,0.));
#30260=DIRECTION('center_axis',(-0.976699262102109,-0.214612561163589,0.));
#30261=DIRECTION('ref_axis',(-0.214612561163589,0.976699262102109,0.));
#30262=DIRECTION('',(0.,0.,1.));
#30263=DIRECTION('',(-0.214612561163589,0.976699262102109,0.));
#30264=DIRECTION('',(0.,0.,-1.));
#30265=DIRECTION('',(-0.214612561163589,0.976699262102109,0.));
#30266=DIRECTION('center_axis',(0.,0.,1.));
#30267=DIRECTION('ref_axis',(1.,0.,0.));
#30268=DIRECTION('center_axis',(0.,0.,1.));
#30269=DIRECTION('ref_axis',(1.,0.,0.));
#30270=DIRECTION('',(0.92459392552897,-0.380954161120377,0.));
#30271=DIRECTION('center_axis',(0.380954161120377,0.92459392552897,0.));
#30272=DIRECTION('ref_axis',(0.92459392552897,-0.380954161120377,0.));
#30273=DIRECTION('',(0.,0.,-1.));
#30274=DIRECTION('',(0.92459392552897,-0.380954161120377,0.));
#30275=DIRECTION('center_axis',(0.,0.,-1.));
#30276=DIRECTION('ref_axis',(-1.,0.,0.));
#30277=DIRECTION('center_axis',(0.,0.,-1.));
#30278=DIRECTION('ref_axis',(1.,0.,0.));
#30279=DIRECTION('center_axis',(-0.844395270395731,-0.535720661663633,0.));
#30280=DIRECTION('ref_axis',(-0.535720661663633,0.844395270395731,0.));
#30281=DIRECTION('',(0.,0.,1.));
#30282=DIRECTION('',(-0.535720661663633,0.844395270395731,0.));
#30283=DIRECTION('',(0.,0.,-1.));
#30284=DIRECTION('',(-0.535720661663633,0.844395270395731,0.));
#30285=DIRECTION('center_axis',(0.,0.,1.));
#30286=DIRECTION('ref_axis',(1.,0.,0.));
#30287=DIRECTION('center_axis',(0.,0.,1.));
#30288=DIRECTION('ref_axis',(1.,0.,0.));
#30289=DIRECTION('',(0.99912808582995,-0.0417500671350428,0.));
#30290=DIRECTION('center_axis',(0.0417500671350428,0.99912808582995,0.));
#30291=DIRECTION('ref_axis',(0.99912808582995,-0.0417500671350428,0.));
#30292=DIRECTION('',(0.,0.,-1.));
#30293=DIRECTION('',(0.99912808582995,-0.0417500671350428,0.));
#30294=DIRECTION('center_axis',(0.,0.,-1.));
#30295=DIRECTION('ref_axis',(-1.,0.,0.));
#30296=DIRECTION('center_axis',(0.,0.,-1.));
#30297=DIRECTION('ref_axis',(1.,0.,0.));
#30298=DIRECTION('center_axis',(-0.610244747132677,-0.792212943972121,0.));
#30299=DIRECTION('ref_axis',(-0.792212943972121,0.610244747132677,0.));
#30300=DIRECTION('',(0.,0.,1.));
#30301=DIRECTION('',(-0.792212943972121,0.610244747132677,0.));
#30302=DIRECTION('',(0.,0.,-1.));
#30303=DIRECTION('',(-0.792212943972121,0.610244747132677,0.));
#30304=DIRECTION('center_axis',(0.,0.,1.));
#30305=DIRECTION('ref_axis',(1.,0.,0.));
#30306=DIRECTION('center_axis',(0.,0.,1.));
#30307=DIRECTION('ref_axis',(1.,0.,0.));
#30308=DIRECTION('',(0.953152653419737,0.302489701112144,0.));
#30309=DIRECTION('center_axis',(-0.302489701112144,0.953152653419737,0.));
#30310=DIRECTION('ref_axis',(0.953152653419737,0.302489701112144,0.));
#30311=DIRECTION('',(0.,0.,-1.));
#30312=DIRECTION('',(0.953152653419737,0.302489701112144,0.));
#30313=DIRECTION('center_axis',(0.,0.,-1.));
#30314=DIRECTION('ref_axis',(-1.,0.,0.));
#30315=DIRECTION('center_axis',(0.,0.,-1.));
#30316=DIRECTION('ref_axis',(1.,0.,0.));
#30317=DIRECTION('center_axis',(0.,0.,-1.));
#30318=DIRECTION('ref_axis',(-1.,0.,0.));
#30319=DIRECTION('center_axis',(0.,0.,1.));
#30320=DIRECTION('ref_axis',(1.,0.,0.));
#30321=DIRECTION('center_axis',(0.,0.,1.));
#30322=DIRECTION('ref_axis',(1.,0.,0.));
#30323=DIRECTION('',(0.707106781186545,8.6595605623549E-17,-0.70710678118655));
#30324=DIRECTION('center_axis',(0.,0.,1.));
#30325=DIRECTION('ref_axis',(1.,0.,0.));
#30326=DIRECTION('center_axis',(0.,0.,1.));
#30327=DIRECTION('ref_axis',(1.,0.,0.));
#30328=DIRECTION('',(0.707106781186548,8.65956056235494E-17,-0.707106781186547));
#30329=DIRECTION('center_axis',(0.,0.,1.));
#30330=DIRECTION('ref_axis',(1.,0.,0.));
#30331=DIRECTION('center_axis',(0.,0.,1.));
#30332=DIRECTION('ref_axis',(1.,0.,0.));
#30333=DIRECTION('center_axis',(0.,0.,1.));
#30334=DIRECTION('ref_axis',(1.,0.,0.));
#30335=DIRECTION('center_axis',(0.,0.,1.));
#30336=DIRECTION('ref_axis',(1.,0.,0.));
#30337=DIRECTION('center_axis',(0.,0.,1.));
#30338=DIRECTION('ref_axis',(1.,0.,0.));
#30339=DIRECTION('center_axis',(0.,0.,1.));
#30340=DIRECTION('ref_axis',(1.,0.,0.));
#30341=DIRECTION('center_axis',(0.,0.,1.));
#30342=DIRECTION('ref_axis',(1.,0.,0.));
#30343=DIRECTION('center_axis',(0.,0.,1.));
#30344=DIRECTION('ref_axis',(1.,0.,0.));
#30345=DIRECTION('center_axis',(0.,0.,1.));
#30346=DIRECTION('ref_axis',(1.,0.,0.));
#30347=DIRECTION('center_axis',(0.,0.,1.));
#30348=DIRECTION('ref_axis',(1.,0.,0.));
#30349=DIRECTION('center_axis',(0.,0.,1.));
#30350=DIRECTION('ref_axis',(1.,0.,0.));
#30351=DIRECTION('center_axis',(0.,0.,1.));
#30352=DIRECTION('ref_axis',(1.,0.,0.));
#30353=DIRECTION('center_axis',(0.,0.,1.));
#30354=DIRECTION('ref_axis',(1.,0.,0.));
#30355=DIRECTION('center_axis',(0.,0.,1.));
#30356=DIRECTION('ref_axis',(1.,0.,0.));
#30357=DIRECTION('center_axis',(0.,0.,1.));
#30358=DIRECTION('ref_axis',(1.,0.,0.));
#30359=DIRECTION('center_axis',(0.,0.,1.));
#30360=DIRECTION('ref_axis',(1.,0.,0.));
#30361=DIRECTION('center_axis',(0.,0.,1.));
#30362=DIRECTION('ref_axis',(1.,0.,0.));
#30363=DIRECTION('',(0.,0.,-1.));
#30364=DIRECTION('center_axis',(0.,0.,1.));
#30365=DIRECTION('ref_axis',(1.,0.,0.));
#30366=DIRECTION('center_axis',(0.,0.,1.));
#30367=DIRECTION('ref_axis',(1.,0.,0.));
#30368=DIRECTION('center_axis',(0.,0.,1.));
#30369=DIRECTION('ref_axis',(1.,0.,0.));
#30370=DIRECTION('center_axis',(0.,0.,1.));
#30371=DIRECTION('ref_axis',(1.,0.,0.));
#30372=DIRECTION('center_axis',(0.,0.,1.));
#30373=DIRECTION('ref_axis',(1.,0.,0.));
#30374=DIRECTION('center_axis',(0.,0.,1.));
#30375=DIRECTION('ref_axis',(1.,0.,0.));
#30376=DIRECTION('center_axis',(0.,0.,1.));
#30377=DIRECTION('ref_axis',(1.,0.,0.));
#30378=DIRECTION('center_axis',(0.,0.,1.));
#30379=DIRECTION('ref_axis',(1.,0.,0.));
#30380=DIRECTION('center_axis',(0.,0.,1.));
#30381=DIRECTION('ref_axis',(1.,0.,0.));
#30382=DIRECTION('center_axis',(0.,0.,1.));
#30383=DIRECTION('ref_axis',(1.,0.,0.));
#30384=DIRECTION('center_axis',(0.,0.,1.));
#30385=DIRECTION('ref_axis',(1.,0.,0.));
#30386=DIRECTION('center_axis',(0.,0.,1.));
#30387=DIRECTION('ref_axis',(1.,0.,0.));
#30388=DIRECTION('center_axis',(0.,0.,1.));
#30389=DIRECTION('ref_axis',(1.,0.,0.));
#30390=DIRECTION('center_axis',(0.,0.,1.));
#30391=DIRECTION('ref_axis',(1.,0.,0.));
#30392=DIRECTION('center_axis',(0.,0.,1.));
#30393=DIRECTION('ref_axis',(1.,0.,0.));
#30394=DIRECTION('center_axis',(0.,0.,1.));
#30395=DIRECTION('ref_axis',(1.,0.,0.));
#30396=DIRECTION('center_axis',(0.,0.,1.));
#30397=DIRECTION('ref_axis',(1.,0.,0.));
#30398=DIRECTION('center_axis',(0.,0.,1.));
#30399=DIRECTION('ref_axis',(1.,0.,0.));
#30400=DIRECTION('center_axis',(0.,0.,1.));
#30401=DIRECTION('ref_axis',(1.,0.,0.));
#30402=DIRECTION('center_axis',(0.,0.,1.));
#30403=DIRECTION('ref_axis',(1.,0.,0.));
#30404=DIRECTION('center_axis',(0.,0.,-1.));
#30405=DIRECTION('ref_axis',(1.,0.,0.));
#30406=DIRECTION('center_axis',(0.,0.,1.));
#30407=DIRECTION('ref_axis',(1.,0.,0.));
#30408=DIRECTION('',(-0.707106781186547,-8.65956056235493E-17,-0.707106781186548));
#30409=DIRECTION('center_axis',(0.,0.,1.));
#30410=DIRECTION('ref_axis',(1.,0.,0.));
#48573=CARTESIAN_POINT('',(0.,0.,0.));
#48574=CARTESIAN_POINT('Origin',(0.,0.,-2.22));
#48575=CARTESIAN_POINT('',(-0.393952734404645,4.1940781306567E-5,-2.7812836477965));
#48576=CARTESIAN_POINT('',(-0.394010867405998,5.4694194531556E-5,-2.7996163522035));
#48577=CARTESIAN_POINT('',(-0.3933,-4.81653586104654E-17,-2.22));
#48578=CARTESIAN_POINT('',(0.386880458087545,0.0743511284475749,-2.84));
#48579=CARTESIAN_POINT('Ctrl Pts',(-0.393952734404645,4.1940781306567E-5,
-2.7812836477965));
#48580=CARTESIAN_POINT('Ctrl Pts',(-0.393956887618347,0.00257921210189992,
-2.78141257124883));
#48581=CARTESIAN_POINT('Ctrl Pts',(-0.39393432800773,0.00511641073810632,
-2.78154149470116));
#48582=CARTESIAN_POINT('Ctrl Pts',(-0.393884823371554,0.00765309135505756,
-2.78167041815349));
#48583=CARTESIAN_POINT('Ctrl Pts',(-0.391341925890778,0.137954397427497,
-2.78829281046787));
#48584=CARTESIAN_POINT('Ctrl Pts',(-0.317703128330192,0.266888881816179,
-2.79491520278225));
#48585=CARTESIAN_POINT('Ctrl Pts',(-0.206805076321773,0.335299228187672,
-2.80153759509663));
#48586=CARTESIAN_POINT('Ctrl Pts',(-0.0959070243133527,0.403709574559165,
-2.80815998741101));
#48587=CARTESIAN_POINT('Ctrl Pts',(0.0522502821429009,0.411595782913467,
-2.81478237972539));
#48588=CARTESIAN_POINT('Ctrl Pts',(0.169863896558048,0.355408659714183,
-2.82140477203977));
#48589=CARTESIAN_POINT('Ctrl Pts',(0.279947577673663,0.302818784096202,
-2.82760318135985));
#48590=CARTESIAN_POINT('Ctrl Pts',(0.363273346469767,0.194097233714658,
-2.83380159067992));
#48591=CARTESIAN_POINT('Ctrl Pts',(0.386886490162192,0.0743511351644956,
-2.84));
#48592=CARTESIAN_POINT('',(-0.3933,-4.81653586104654E-17,-2.84));
#48593=CARTESIAN_POINT('Origin',(0.,0.,-2.84));
#48594=CARTESIAN_POINT('',(-0.3933,-4.81653586104654E-17,-4.4467));
#48595=CARTESIAN_POINT('',(-0.3933,-4.81653586104654E-17,-2.22));
#48596=CARTESIAN_POINT('Origin',(0.,0.,-4.4467));
#48597=CARTESIAN_POINT('',(0.174290087240704,0.352573191677455,-2.84));
#48598=CARTESIAN_POINT('Origin',(0.,0.,-2.84));
#48599=CARTESIAN_POINT('Ctrl Pts',(0.174290087240704,0.352573191677456,
-2.84));
#48600=CARTESIAN_POINT('Ctrl Pts',(0.0569263183517564,0.410590482842535,
-2.83337760768562));
#48601=CARTESIAN_POINT('Ctrl Pts',(-0.090669376315471,0.404886350107643,
-2.82675521537124));
#48602=CARTESIAN_POINT('Ctrl Pts',(-0.202271457956682,0.338016611261013,
-2.82013282305686));
#48603=CARTESIAN_POINT('Ctrl Pts',(-0.313873539597893,0.271146872414382,
-2.81351043074248));
#48604=CARTESIAN_POINT('Ctrl Pts',(-0.389482008213088,0.143111527456014,
-2.8068880384281));
#48605=CARTESIAN_POINT('Ctrl Pts',(-0.393813496269577,0.0128329553269884,
-2.80026564611372));
#48606=CARTESIAN_POINT('Ctrl Pts',(-0.393955056835797,0.00857522491277192,
-2.80004921481031));
#48607=CARTESIAN_POINT('Ctrl Pts',(-0.394020486735239,0.0043150985163057,
-2.79983278350691));
#48608=CARTESIAN_POINT('Ctrl Pts',(-0.394010867405998,5.4694194531556E-5,
-2.7996163522035));
#48609=CARTESIAN_POINT('Origin',(0.,0.,-2.22));
#48610=CARTESIAN_POINT('',(-0.39300565221066,0.000328329871180644,-2.6562836477965));
#48611=CARTESIAN_POINT('',(-0.392962952735427,0.00031460754753748,-2.6746163522035));
#48612=CARTESIAN_POINT('',(-0.3933,-4.81653586104654E-17,-2.22));
#48613=CARTESIAN_POINT('Ctrl Pts',(-0.39300565221066,0.000328329871180644,
-2.6562836477965));
#48614=CARTESIAN_POINT('Ctrl Pts',(-0.39332720747469,0.0411433485463145,
-2.65834488402921));
#48615=CARTESIAN_POINT('Ctrl Pts',(-0.387477274673374,0.081868491656979,
-2.66040612026193));
#48616=CARTESIAN_POINT('Ctrl Pts',(-0.375071232908909,0.120487600583847,
-2.66246735649464));
#48617=CARTESIAN_POINT('Ctrl Pts',(-0.335212785667873,0.244564058239049,
-2.66908974880902));
#48618=CARTESIAN_POINT('Ctrl Pts',(-0.227680558122831,0.346901509500663,
-2.6757121411234));
#48619=CARTESIAN_POINT('Ctrl Pts',(-0.101784662090584,0.380572608550405,
-2.68233453343778));
#48620=CARTESIAN_POINT('Ctrl Pts',(0.0241112339416628,0.414243707600147,
-2.68895692575216));
#48621=CARTESIAN_POINT('Ctrl Pts',(0.168370798461114,0.379248454438019,
-2.69557931806654));
#48622=CARTESIAN_POINT('Ctrl Pts',(0.264846786191469,0.291635199129418,
-2.70220171038092));
#48623=CARTESIAN_POINT('Ctrl Pts',(0.361322773921825,0.204021943820817,
-2.7088241026953));
#48624=CARTESIAN_POINT('Ctrl Pts',(0.410015184863085,0.0637906863657433,
-2.71544649500968));
#48625=CARTESIAN_POINT('Ctrl Pts',(0.388591027578597,-0.0647583673116287,
-2.72206888732406));
#48626=CARTESIAN_POINT('Ctrl Pts',(0.367166870294109,-0.193307420989001,
-2.72869127963844));
#48627=CARTESIAN_POINT('Ctrl Pts',(0.275626144783873,-0.310174270888672,
-2.73531367195282));
#48628=CARTESIAN_POINT('Ctrl Pts',(0.155954592874106,-0.361764920745412,
-2.7419360642672));
#48629=CARTESIAN_POINT('Ctrl Pts',(0.036283040964339,-0.413355570602153,
-2.74855845658158));
#48630=CARTESIAN_POINT('Ctrl Pts',(-0.111519337344959,-0.399670020415965,
-2.75518084889597));
#48631=CARTESIAN_POINT('Ctrl Pts',(-0.219697027799126,-0.326993181444773,
-2.76180324121035));
#48632=CARTESIAN_POINT('Ctrl Pts',(-0.325768735904897,-0.255731201113731,
-2.7682967100724));
#48633=CARTESIAN_POINT('Ctrl Pts',(-0.393743550091291,-0.127752436559022,
-2.77479017893445));
#48634=CARTESIAN_POINT('Ctrl Pts',(-0.393952734404645,4.1940781306567E-5,
-2.7812836477965));
#48635=CARTESIAN_POINT('Ctrl Pts',(-0.394010867405998,5.4694194531556E-5,
-2.7996163522035));
#48636=CARTESIAN_POINT('Ctrl Pts',(-0.393726153286074,-0.126045290173359,
-2.79321039119253));
#48637=CARTESIAN_POINT('Ctrl Pts',(-0.327694632260249,-0.252388750748456,
-2.78680443018155));
#48638=CARTESIAN_POINT('Ctrl Pts',(-0.223957356921664,-0.32405571896141,
-2.78039846917058));
#48639=CARTESIAN_POINT('Ctrl Pts',(-0.11671522201948,-0.3981440218211,-2.7737760768562));
#48640=CARTESIAN_POINT('Ctrl Pts',(0.0308235552826724,-0.413798828240797,
-2.76715368454182));
#48641=CARTESIAN_POINT('Ctrl Pts',(0.151148649024799,-0.363796630115481,
-2.76053129222743));
#48642=CARTESIAN_POINT('Ctrl Pts',(0.271473742766925,-0.313794431990164,
-2.75390889991305));
#48643=CARTESIAN_POINT('Ctrl Pts',(0.364585152949026,-0.198135229319833,
-2.74728650759867));
#48644=CARTESIAN_POINT('Ctrl Pts',(0.387712443649385,-0.0698775765452277,
-2.74066411528429));
#48645=CARTESIAN_POINT('Ctrl Pts',(0.410839734349744,0.0583800762293768,
-2.73404172296991));
#48646=CARTESIAN_POINT('Ctrl Pts',(0.363982905568364,0.199236179108254,
-2.72741933065553));
#48647=CARTESIAN_POINT('Ctrl Pts',(0.268666865662216,0.288113545745012,
-2.72079693834115));
#48648=CARTESIAN_POINT('Ctrl Pts',(0.173350825756067,0.376990912381769,
-2.71417454602677));
#48649=CARTESIAN_POINT('Ctrl Pts',(0.0295755747251501,0.413889542776405,
-2.70755215371239));
#48650=CARTESIAN_POINT('Ctrl Pts',(-0.0967512798405108,0.381883315850353,
-2.70092976139801));
#48651=CARTESIAN_POINT('Ctrl Pts',(-0.223078134406171,0.3498770889243,-2.69430736908363));
#48652=CARTESIAN_POINT('Ctrl Pts',(-0.331956592506576,0.24896600467756,
-2.68768497676925));
#48653=CARTESIAN_POINT('Ctrl Pts',(-0.373450060077915,0.125425952738769,
-2.68106258445487));
#48654=CARTESIAN_POINT('Ctrl Pts',(-0.386913297942314,0.0853413514175464,
-2.67891384037108));
#48655=CARTESIAN_POINT('Ctrl Pts',(-0.393282346889808,0.0428744069284828,
-2.67676509628729));
#48656=CARTESIAN_POINT('Ctrl Pts',(-0.392962952735427,0.00031460754753748,
-2.6746163522035));
#48657=CARTESIAN_POINT('Origin',(0.,0.,-2.22));
#48658=CARTESIAN_POINT('',(-0.39276380274066,-0.000209749112361407,-2.5312836477965));
#48659=CARTESIAN_POINT('',(-0.392793287557452,-0.000232553243135302,-2.5496163522035));
#48660=CARTESIAN_POINT('',(-0.3933,-4.81653586104654E-17,-2.22));
#48661=CARTESIAN_POINT('Ctrl Pts',(-0.39276380274066,-0.000209749112361407,
-2.5312836477965));
#48662=CARTESIAN_POINT('Ctrl Pts',(-0.392381433345052,0.0789898077510052,
-2.5352771968096));
#48663=CARTESIAN_POINT('Ctrl Pts',(-0.369164685986063,0.158395566123688,
-2.5392707458227));
#48664=CARTESIAN_POINT('Ctrl Pts',(-0.324646816974723,0.223159140648563,
-2.54326429483579));
#48665=CARTESIAN_POINT('Ctrl Pts',(-0.250824061168682,0.330554792180273,
-2.54988668715017));
#48666=CARTESIAN_POINT('Ctrl Pts',(-0.118426042679012,0.397686377849861,
-2.55650907946455));
#48667=CARTESIAN_POINT('Ctrl Pts',(0.011836349297656,0.393770822005192,
-2.56313147177893));
#48668=CARTESIAN_POINT('Ctrl Pts',(0.142098741274323,0.389855266160524,
-2.56975386409331));
#48669=CARTESIAN_POINT('Ctrl Pts',(0.270225506737988,0.3148925688016,-2.5763762564077));
#48670=CARTESIAN_POINT('Ctrl Pts',(0.337464415042443,0.203256760030363,
-2.58299864872208));
#48671=CARTESIAN_POINT('Ctrl Pts',(0.404703323346898,0.0916209512591259,
-2.58962104103646));
#48672=CARTESIAN_POINT('Ctrl Pts',(0.411054374492143,-0.0566879689244253,
-2.59624343335084));
#48673=CARTESIAN_POINT('Ctrl Pts',(0.353605200899493,-0.173663278362041,
-2.60286582566522));
#48674=CARTESIAN_POINT('Ctrl Pts',(0.296156027306843,-0.290638587799656,
-2.6094882179796));
#48675=CARTESIAN_POINT('Ctrl Pts',(0.174906628976298,-0.376280286491338,
-2.61611061029398));
#48676=CARTESIAN_POINT('Ctrl Pts',(0.0454558890327329,-0.391317435834831,
-2.62273300260836));
#48677=CARTESIAN_POINT('Ctrl Pts',(-0.0839948509108324,-0.406354585178324,
-2.62935539492274));
#48678=CARTESIAN_POINT('Ctrl Pts',(-0.221646932467417,-0.350787185173631,
-2.63597778723712));
#48679=CARTESIAN_POINT('Ctrl Pts',(-0.304380639777195,-0.250095753146889,
-2.6426001795515));
#48680=CARTESIAN_POINT('Ctrl Pts',(-0.361363272992008,-0.18074478211436,
-2.64716133563317));
#48681=CARTESIAN_POINT('Ctrl Pts',(-0.392294106525188,-0.0899881839271938,
-2.65172249171483));
#48682=CARTESIAN_POINT('Ctrl Pts',(-0.39300565221066,0.000328329871180644,
-2.6562836477965));
#48683=CARTESIAN_POINT('Ctrl Pts',(-0.392962952735427,0.00031460754753748,
-2.6746163522035));
#48684=CARTESIAN_POINT('Ctrl Pts',(-0.392297979598613,-0.0882941628644968,
-2.67014270397291));
#48685=CARTESIAN_POINT('Ctrl Pts',(-0.362640930570418,-0.177305426955751,
-2.66566905574232));
#48686=CARTESIAN_POINT('Ctrl Pts',(-0.307653528440411,-0.246057304588508,
-2.66119540751173));
#48687=CARTESIAN_POINT('Ctrl Pts',(-0.226255052189297,-0.347831490346152,
-2.65457301519735));
#48688=CARTESIAN_POINT('Ctrl Pts',(-0.0893496226447939,-0.405210842230597,
-2.64795062288297));
#48689=CARTESIAN_POINT('Ctrl Pts',(0.0402879227865041,-0.391883265826329,
-2.64132823056859));
#48690=CARTESIAN_POINT('Ctrl Pts',(0.169925468217803,-0.378555689422062,
-2.63470583825421));
#48691=CARTESIAN_POINT('Ctrl Pts',(0.292295129535897,-0.294521184729083,
-2.62808344593983));
#48692=CARTESIAN_POINT('Ctrl Pts',(0.35128302181726,-0.178314085485268,
-2.62146105362545));
#48693=CARTESIAN_POINT('Ctrl Pts',(0.410270914098623,-0.0621069862414521,
-2.61483866131107));
#48694=CARTESIAN_POINT('Ctrl Pts',(0.405877037343254,0.0862727075531994,
-2.60821626899669));
#48695=CARTESIAN_POINT('Ctrl Pts',(0.340116983457932,0.198786014393248,
-2.60159387668231));
#48696=CARTESIAN_POINT('Ctrl Pts',(0.274356929572611,0.311299321233295,
-2.59497148436793));
#48697=CARTESIAN_POINT('Ctrl Pts',(0.147230698557337,0.38794624111874,-2.58834909205354));
#48698=CARTESIAN_POINT('Ctrl Pts',(0.0170313711229766,0.393580345679592,
-2.58172669973916));
#48699=CARTESIAN_POINT('Ctrl Pts',(-0.113167956311385,0.399214450240444,
-2.57510430742478));
#48700=CARTESIAN_POINT('Ctrl Pts',(-0.246440380164833,0.333835739476704,
-2.5684819151104));
#48701=CARTESIAN_POINT('Ctrl Pts',(-0.321673867949857,0.227423564450892,
-2.56185952279602));
#48702=CARTESIAN_POINT('Ctrl Pts',(-0.368036591141922,0.161846939463297,
-2.55777846593185));
#48703=CARTESIAN_POINT('Ctrl Pts',(-0.392358130091861,0.080687221346171,
-2.55369740906767));
#48704=CARTESIAN_POINT('Ctrl Pts',(-0.392793287557452,-0.000232553243135302,
-2.5496163522035));
#48705=CARTESIAN_POINT('Origin',(0.,0.,-2.22));
#48706=CARTESIAN_POINT('',(-0.393773264356009,-0.00023371002059569,-2.4062836477965));
#48707=CARTESIAN_POINT('',(-0.393810998789827,-0.000208891560843762,-2.4246163522035));
#48708=CARTESIAN_POINT('',(-0.3933,-4.81653586104654E-17,-2.22));
#48709=CARTESIAN_POINT('Ctrl Pts',(-0.393773264356009,-0.00023371002059569,
-2.4062836477965));
#48710=CARTESIAN_POINT('Ctrl Pts',(-0.392952500563531,0.11651851875429,
-2.41220950958998));
#48711=CARTESIAN_POINT('Ctrl Pts',(-0.337733951007006,0.23394492666379,
-2.41813537138347));
#48712=CARTESIAN_POINT('Ctrl Pts',(-0.24685270843109,0.307016768785737,
-2.42406123317695));
#48713=CARTESIAN_POINT('Ctrl Pts',(-0.145289212127785,0.388677533503259,
-2.43068362549133));
#48714=CARTESIAN_POINT('Ctrl Pts',(0.000813329977278038,0.414943994822137,
-2.43730601780571));
#48715=CARTESIAN_POINT('Ctrl Pts',(0.124459873438975,0.373771716382449,
-2.44392841012009));
#48716=CARTESIAN_POINT('Ctrl Pts',(0.248106416900672,0.332599437942762,
-2.45055080243447));
#48717=CARTESIAN_POINT('Ctrl Pts',(0.349296961719004,0.22398841974451,-2.45717319474885));
#48718=CARTESIAN_POINT('Ctrl Pts',(0.381630776406502,0.0977420389515133,
-2.46379558706323));
#48719=CARTESIAN_POINT('Ctrl Pts',(0.413964591094,-0.0285043418414835,-2.47041797937761));
#48720=CARTESIAN_POINT('Ctrl Pts',(0.377441675650666,-0.172386085229224,
-2.47704037169199));
#48721=CARTESIAN_POINT('Ctrl Pts',(0.288809541620048,-0.267926491451958,
-2.48366276400637));
#48722=CARTESIAN_POINT('Ctrl Pts',(0.200177407589429,-0.363466897674693,
-2.49028515632075));
#48723=CARTESIAN_POINT('Ctrl Pts',(0.0594360549715268,-0.41066596673242,
-2.49690754863513));
#48724=CARTESIAN_POINT('Ctrl Pts',(-0.0688778315672936,-0.387880652908061,
-2.50352994094951));
#48725=CARTESIAN_POINT('Ctrl Pts',(-0.197191718106114,-0.365095339083702,
-2.51015233326389));
#48726=CARTESIAN_POINT('Ctrl Pts',(-0.313078138565853,-0.272325642377255,
-2.51677472557827));
#48727=CARTESIAN_POINT('Ctrl Pts',(-0.363397602234515,-0.152110935327116,
-2.52339711789265));
#48728=CARTESIAN_POINT('Ctrl Pts',(-0.383372556708641,-0.104390170331315,
-2.52602596119393));
#48729=CARTESIAN_POINT('Ctrl Pts',(-0.3930155059803,-0.0523446356110889,
-2.52865480449522));
#48730=CARTESIAN_POINT('Ctrl Pts',(-0.39276380274066,-0.000209749112361407,
-2.5312836477965));
#48731=CARTESIAN_POINT('Ctrl Pts',(-0.392793287557452,-0.000232553243135302,
-2.5496163522035));
#48732=CARTESIAN_POINT('Ctrl Pts',(-0.39306426665197,-0.0506225131556464,
-2.54707501675329));
#48733=CARTESIAN_POINT('Ctrl Pts',(-0.384072727828695,-0.10091942920435,
-2.54453368130309));
#48734=CARTESIAN_POINT('Ctrl Pts',(-0.365373106319892,-0.147302469940018,
-2.54199234585288));
#48735=CARTESIAN_POINT('Ctrl Pts',(-0.316644305188305,-0.268170690017237,
-2.5353699535385));
#48736=CARTESIAN_POINT('Ctrl Pts',(-0.201992151208531,-0.362461490883791,
-2.52874756122412));
#48737=CARTESIAN_POINT('Ctrl Pts',(-0.0739901136783288,-0.386937986140273,
-2.52212516890974));
#48738=CARTESIAN_POINT('Ctrl Pts',(0.0540119238518717,-0.411414481396754,
-2.51550277659536));
#48739=CARTESIAN_POINT('Ctrl Pts',(0.1953638449325,-0.366076671043165,-2.50888038428098));
#48740=CARTESIAN_POINT('Ctrl Pts',(0.285248963317479,-0.271714131682789,
-2.5022579919666));
#48741=CARTESIAN_POINT('Ctrl Pts',(0.375134081702459,-0.177351592322412,
-2.49563559965222));
#48742=CARTESIAN_POINT('Ctrl Pts',(0.413552397391789,-0.0339643239552482,
-2.48901320733784));
#48743=CARTESIAN_POINT('Ctrl Pts',(0.38288728052918,0.0926977181808754,
-2.48239081502346));
#48744=CARTESIAN_POINT('Ctrl Pts',(0.352222163666571,0.219359760317,-2.47576842270908));
#48745=CARTESIAN_POINT('Ctrl Pts',(0.252473614252022,0.329296576222083,
-2.4691460303947));
#48746=CARTESIAN_POINT('Ctrl Pts',(0.12938113226254,0.372096844648535,-2.46252363808032));
#48747=CARTESIAN_POINT('Ctrl Pts',(0.00628865027305796,0.414897113074987,
-2.45590124576594));
#48748=CARTESIAN_POINT('Ctrl Pts',(-0.140147764291357,0.390560834022808,
-2.44927885345156));
#48749=CARTESIAN_POINT('Ctrl Pts',(-0.242779966614497,0.310247363505348,
-2.44265646113718));
#48750=CARTESIAN_POINT('Ctrl Pts',(-0.335973685848564,0.237319852912212,
-2.43664309149262));
#48751=CARTESIAN_POINT('Ctrl Pts',(-0.393049557048956,0.118237518587536,
-2.43062972184806));
#48752=CARTESIAN_POINT('Ctrl Pts',(-0.393810998789827,-0.000208891560843762,
-2.4246163522035));
#48753=CARTESIAN_POINT('Origin',(0.,0.,-2.22));
#48754=CARTESIAN_POINT('',(-0.393484494376611,0.000340583921978138,-2.2812836477965));
#48755=CARTESIAN_POINT('',(-0.393432313413097,0.00034956597777247,-2.2996163522035));
#48756=CARTESIAN_POINT('',(-0.3933,-4.81653586104654E-17,-2.22));
#48757=CARTESIAN_POINT('Ctrl Pts',(-0.393484494376611,0.000340583921978138,
-2.2812836477965));
#48758=CARTESIAN_POINT('Ctrl Pts',(-0.39370719115912,0.0247346784797741,
-2.28251943005599));
#48759=CARTESIAN_POINT('Ctrl Pts',(-0.391633797841506,0.0490910240555078,
-2.28375521231547));
#48760=CARTESIAN_POINT('Ctrl Pts',(-0.387128134168714,0.0729887915576785,
-2.28499099457496));
#48761=CARTESIAN_POINT('Ctrl Pts',(-0.362982883458997,0.201053740396819,
-2.29161338688934));
#48762=CARTESIAN_POINT('Ctrl Pts',(-0.268989026604262,0.315949495614517,
-2.29823577920372));
#48763=CARTESIAN_POINT('Ctrl Pts',(-0.148247268569818,0.364990826350649,
-2.3048581715181));
#48764=CARTESIAN_POINT('Ctrl Pts',(-0.0275055105353745,0.41403215708678,
-2.31148056383248));
#48765=CARTESIAN_POINT('Ctrl Pts',(0.119984148678778,0.397219063341345,
-2.31810295614686));
#48766=CARTESIAN_POINT('Ctrl Pts',(0.226590605275426,0.322261157389841,
-2.32472534846124));
#48767=CARTESIAN_POINT('Ctrl Pts',(0.333197061872074,0.247303251438337,
-2.33134774077562));
#48768=CARTESIAN_POINT('Ctrl Pts',(0.398920315851218,0.114200533280764,
-2.33797013309));
#48769=CARTESIAN_POINT('Ctrl Pts',(0.393623093648558,-0.0160129978489424,
-2.34459252540438));
#48770=CARTESIAN_POINT('Ctrl Pts',(0.388325871445897,-0.14622652897865,
-2.35121491771876));
#48771=CARTESIAN_POINT('Ctrl Pts',(0.312008173061429,-0.27355087308049,
-2.35783731003314));
#48772=CARTESIAN_POINT('Ctrl Pts',(0.199665334447639,-0.339601693428282,
-2.36445970234752));
#48773=CARTESIAN_POINT('Ctrl Pts',(0.0873224958338501,-0.405652513776072,
-2.3710820946619));
#48774=CARTESIAN_POINT('Ctrl Pts',(-0.0610454830092596,-0.410429810369814,
-2.37770448697628));
#48775=CARTESIAN_POINT('Ctrl Pts',(-0.177404746411668,-0.351742962866779,
-2.38432687929066));
#48776=CARTESIAN_POINT('Ctrl Pts',(-0.293764009814075,-0.293056115363745,
-2.39094927160504));
#48777=CARTESIAN_POINT('Ctrl Pts',(-0.378114557775781,-0.170905123763935,
-2.39757166391942));
#48778=CARTESIAN_POINT('Ctrl Pts',(-0.391777606505862,-0.0413020939059466,
-2.4041940562338));
#48779=CARTESIAN_POINT('Ctrl Pts',(-0.393214659763545,-0.0276706958232436,
-2.4048905867547));
#48780=CARTESIAN_POINT('Ctrl Pts',(-0.393869737586711,-0.0139568600971337,
-2.4055871172756));
#48781=CARTESIAN_POINT('Ctrl Pts',(-0.393773264356009,-0.00023371002059569,
-2.4062836477965));
#48782=CARTESIAN_POINT('Ctrl Pts',(-0.393810998789827,-0.000208891560843762,
-2.4246163522035));
#48783=CARTESIAN_POINT('Ctrl Pts',(-0.393888116164835,-0.0122049192796106,
-2.42400732953368));
#48784=CARTESIAN_POINT('Ctrl Pts',(-0.393387602125509,-0.0241944241624916,
-2.42339830686386));
#48785=CARTESIAN_POINT('Ctrl Pts',(-0.392288475751339,-0.0361287983316595,
-2.42278928419403));
#48786=CARTESIAN_POINT('Ctrl Pts',(-0.380336792483176,-0.165900827668469,
-2.41616689187965));
#48787=CARTESIAN_POINT('Ctrl Pts',(-0.297605435864983,-0.289154224359348,
-2.40954449956527));
#48788=CARTESIAN_POINT('Ctrl Pts',(-0.182030711531421,-0.349371376506604,
-2.40292210725089));
#48789=CARTESIAN_POINT('Ctrl Pts',(-0.0664559871978615,-0.409588528653859,
-2.39629971493651));
#48790=CARTESIAN_POINT('Ctrl Pts',(0.0819621048510649,-0.406769436257494,
-2.38967732262213));
#48791=CARTESIAN_POINT('Ctrl Pts',(0.195166729089834,-0.342206788988941,
-2.38305493030775));
#48792=CARTESIAN_POINT('Ctrl Pts',(0.308371353328604,-0.277644141720387,
-2.37643253799337));
#48793=CARTESIAN_POINT('Ctrl Pts',(0.386362509757215,-0.151337939579646,
-2.36981014567899));
#48794=CARTESIAN_POINT('Ctrl Pts',(0.393377501689779,-0.0212056521456562,
-2.36318775336461));
#48795=CARTESIAN_POINT('Ctrl Pts',(0.400392493622343,0.108926635288333,
-2.35656536105023));
#48796=CARTESIAN_POINT('Ctrl Pts',(0.336431321058859,0.242885008015571,
-2.34994296873585));
#48797=CARTESIAN_POINT('Ctrl Pts',(0.230823258321736,0.319243107978586,
-2.34332057642147));
#48798=CARTESIAN_POINT('Ctrl Pts',(0.125215195584611,0.395601207941602,
-2.33669818410709));
#48799=CARTESIAN_POINT('Ctrl Pts',(-0.0220397573261533,0.414359035140395,
-2.33007579179271));
#48800=CARTESIAN_POINT('Ctrl Pts',(-0.143418120667098,0.366915223480943,
-2.32345339947833));
#48801=CARTESIAN_POINT('Ctrl Pts',(-0.264796484008043,0.319471411821491,
-2.31683100716395));
#48802=CARTESIAN_POINT('Ctrl Pts',(-0.360298257779167,0.205825961303794,
-2.31020861484957));
#48803=CARTESIAN_POINT('Ctrl Pts',(-0.386131284610396,0.0780907779253198,
-2.30358622253519));
#48804=CARTESIAN_POINT('Ctrl Pts',(-0.39129325438036,0.0525666626341382,
-2.30226293242462));
#48805=CARTESIAN_POINT('Ctrl Pts',(-0.393673472700586,0.0264799689052292,
-2.30093964231406));
#48806=CARTESIAN_POINT('Ctrl Pts',(-0.393432313413097,0.00034956597777247,
-2.2996163522035));
#48807=CARTESIAN_POINT('Origin',(0.,0.,-2.22));
#48808=CARTESIAN_POINT('',(-0.392657355902925,4.67015916158497E-5,-2.1562836477965));
#48809=CARTESIAN_POINT('',(-0.392653076767141,1.81848134072799E-5,-2.1746163522035));
#48810=CARTESIAN_POINT('',(-0.3933,-4.81653586104654E-17,-2.22));
#48811=CARTESIAN_POINT('Ctrl Pts',(-0.392657355902925,4.67015916158497E-5,
-2.1562836477965));
#48812=CARTESIAN_POINT('Ctrl Pts',(-0.392723854145937,0.0629185196199584,
-2.15945174283637));
#48813=CARTESIAN_POINT('Ctrl Pts',(-0.378505393622063,0.125761940444854,
-2.16261983787624));
#48814=CARTESIAN_POINT('Ctrl Pts',(-0.349841169009376,0.181126233397604,
-2.16578793291611));
#48815=CARTESIAN_POINT('Ctrl Pts',(-0.289923225139679,0.29685636886619,
-2.17241032523049));
#48816=CARTESIAN_POINT('Ctrl Pts',(-0.166884273336077,0.379906329935288,
-2.17903271754487));
#48817=CARTESIAN_POINT('Ctrl Pts',(-0.0371435918272561,0.392193714310694,
-2.18565510985925));
#48818=CARTESIAN_POINT('Ctrl Pts',(0.0925970896815651,0.404481098686101,
-2.19227750217363));
#48819=CARTESIAN_POINT('Ctrl Pts',(0.229039500895603,0.346005906367814,
-2.19889989448801));
#48820=CARTESIAN_POINT('Ctrl Pts',(0.309618232668553,0.243581826000877,
-2.20552228680239));
#48821=CARTESIAN_POINT('Ctrl Pts',(0.390196964441505,0.141157745633939,
-2.21214467911677));
#48822=CARTESIAN_POINT('Ctrl Pts',(0.414912016773367,-0.00521522278165044,
-2.21876707143115));
#48823=CARTESIAN_POINT('Ctrl Pts',(0.372430349245197,-0.128418031910157,
-2.22538946374554));
#48824=CARTESIAN_POINT('Ctrl Pts',(0.329948681717027,-0.251620841038662,
-2.23201185605992));
#48825=CARTESIAN_POINT('Ctrl Pts',(0.220270294328826,-0.351653490880085,
-2.23863424837429));
#48826=CARTESIAN_POINT('Ctrl Pts',(0.0936880038099836,-0.382646199380983,
-2.24525664068867));
#48827=CARTESIAN_POINT('Ctrl Pts',(-0.0328942867088593,-0.413638907881881,
-2.25187903300305));
#48828=CARTESIAN_POINT('Ctrl Pts',(-0.176380480358344,-0.375591675042255,
-2.25850142531744));
#48829=CARTESIAN_POINT('Ctrl Pts',(-0.270975254900737,-0.285950987392151,
-2.26512381763182));
#48830=CARTESIAN_POINT('Ctrl Pts',(-0.347918018104932,-0.213037845660076,
-2.27051042768671));
#48831=CARTESIAN_POINT('Ctrl Pts',(-0.392513788802351,-0.105990020856159,
-2.27589703774161));
#48832=CARTESIAN_POINT('Ctrl Pts',(-0.393484494376611,0.000340583921978138,
-2.2812836477965));
#48833=CARTESIAN_POINT('Ctrl Pts',(-0.393432313413097,0.00034956597777247,
-2.2996163522035));
#48834=CARTESIAN_POINT('Ctrl Pts',(-0.392466593423499,-0.104289374972686,
-2.29431724999968));
#48835=CARTESIAN_POINT('Ctrl Pts',(-0.349464615981463,-0.209629234065492,
-2.28901814779586));
#48836=CARTESIAN_POINT('Ctrl Pts',(-0.274724910660883,-0.282350424157676,
-2.28371904559205));
#48837=CARTESIAN_POINT('Ctrl Pts',(-0.181321229988805,-0.373231526622949,
-2.27709665327767));
#48838=CARTESIAN_POINT('Ctrl Pts',(-0.0383495887533156,-0.413168815314241,
-2.27047426096328));
#48839=CARTESIAN_POINT('Ctrl Pts',(0.0886306378313994,-0.383849122174911,
-2.2638518686489));
#48840=CARTESIAN_POINT('Ctrl Pts',(0.215610864416114,-0.35452942903558,
-2.25722947633452));
#48841=CARTESIAN_POINT('Ctrl Pts',(0.326599676350054,-0.255952754065626,
-2.25060708402015));
#48842=CARTESIAN_POINT('Ctrl Pts',(0.370703364216961,-0.133321244798174,
-2.24398469170577));
#48843=CARTESIAN_POINT('Ctrl Pts',(0.414807052083867,-0.0106897355307235,
-2.23736229939138));
#48844=CARTESIAN_POINT('Ctrl Pts',(0.392025615883743,0.135996608034224,
-2.230739907077));
#48845=CARTESIAN_POINT('Ctrl Pts',(0.312805440018932,0.239475040979098,
-2.22411751476262));
#48846=CARTESIAN_POINT('Ctrl Pts',(0.233585264154121,0.342953473923971,
-2.21749512244824));
#48847=CARTESIAN_POINT('Ctrl Pts',(0.0979263486246238,0.40322399624877,
-2.21087273013386));
#48848=CARTESIAN_POINT('Ctrl Pts',(-0.0319651678833566,0.392649674136003,
-2.20425033781948));
#48849=CARTESIAN_POINT('Ctrl Pts',(-0.161856684391337,0.382075352023237,
-2.1976279455051));
#48850=CARTESIAN_POINT('Ctrl Pts',(-0.285980801877801,0.300656185472903,
-2.19100555319072));
#48851=CARTESIAN_POINT('Ctrl Pts',(-0.347420641447049,0.185726779042249,
-2.18438316087634));
#48852=CARTESIAN_POINT('Ctrl Pts',(-0.377624789710302,0.129226878391847,
-2.18112755798539));
#48853=CARTESIAN_POINT('Ctrl Pts',(-0.392679669287032,0.0646283660230939,
-2.17787195509445));
#48854=CARTESIAN_POINT('Ctrl Pts',(-0.392653076767141,1.81848134072799E-5,
-2.1746163522035));
#48855=CARTESIAN_POINT('Origin',(0.,0.,-2.22));
#48856=CARTESIAN_POINT('',(-0.393312671622578,-0.000360778048017763,-2.0312836477965));
#48857=CARTESIAN_POINT('',(-0.393365397637326,-0.000357415208850981,-2.0496163522035));
#48858=CARTESIAN_POINT('',(-0.3933,-4.81653586104654E-17,-2.22));
#48859=CARTESIAN_POINT('Ctrl Pts',(-0.393312671622578,-0.000360778048017763,
-2.0312836477965));
#48860=CARTESIAN_POINT('Ctrl Pts',(-0.392382090476659,0.100433263636076,
-2.03638405561676));
#48861=CARTESIAN_POINT('Ctrl Pts',(-0.352868355048726,0.201875395553562,
-2.04148446343701));
#48862=CARTESIAN_POINT('Ctrl Pts',(-0.283060251797859,0.273993521475951,
-2.04658487125726));
#48863=CARTESIAN_POINT('Ctrl Pts',(-0.192421098470888,0.367632018566217,
-2.05320726357164));
#48864=CARTESIAN_POINT('Ctrl Pts',(-0.050710058864453,0.411834517909533,
-2.05982965588602));
#48865=CARTESIAN_POINT('Ctrl Pts',(0.0770915383084671,0.386332047182076,
-2.0664520482004));
#48866=CARTESIAN_POINT('Ctrl Pts',(0.204893135481385,0.360829576454619,
-2.07307444051478));
#48867=CARTESIAN_POINT('Ctrl Pts',(0.31878529022079,0.265622135656392,-2.07969683282916));
#48868=CARTESIAN_POINT('Ctrl Pts',(0.366542970761298,0.14436691637679,-2.08631922514355));
#48869=CARTESIAN_POINT('Ctrl Pts',(0.414300651301807,0.0231116970971894,
-2.09294161745793));
#48870=CARTESIAN_POINT('Ctrl Pts',(0.39592385764342,-0.124191300663785,
-2.09956400977231));
#48871=CARTESIAN_POINT('Ctrl Pts',(0.319839233699866,-0.229996566376417,
-2.10618640208669));
#48872=CARTESIAN_POINT('Ctrl Pts',(0.24375460975631,-0.335801832089051,
-2.11280879440107));
#48873=CARTESIAN_POINT('Ctrl Pts',(0.109962155527584,-0.40010936575334,
-2.11943118671545));
#48874=CARTESIAN_POINT('Ctrl Pts',(-0.020187852595031,-0.393431069650401,
-2.12605357902983));
#48875=CARTESIAN_POINT('Ctrl Pts',(-0.150337860717645,-0.386752773547463,
-2.13267597134421));
#48876=CARTESIAN_POINT('Ctrl Pts',(-0.276845422734146,-0.309088647677299,
-2.13929836365859));
#48877=CARTESIAN_POINT('Ctrl Pts',(-0.341700735774504,-0.196051429808179,
-2.14592075597297));
#48878=CARTESIAN_POINT('Ctrl Pts',(-0.375529829618191,-0.137090236470876,
-2.14937505324748));
#48879=CARTESIAN_POINT('Ctrl Pts',(-0.392584850281501,-0.0685048875892015,
-2.15282935052199));
#48880=CARTESIAN_POINT('Ctrl Pts',(-0.392657355902925,4.67015916158497E-5,
-2.1562836477965));
#48881=CARTESIAN_POINT('Ctrl Pts',(-0.392653076767141,1.81848134072799E-5,
-2.1746163522035));
#48882=CARTESIAN_POINT('Ctrl Pts',(-0.39262557604985,-0.0667985867737443,
-2.17124956278007));
#48883=CARTESIAN_POINT('Ctrl Pts',(-0.376468876623097,-0.133627837849165,
-2.16788277335663));
#48884=CARTESIAN_POINT('Ctrl Pts',(-0.344257961249291,-0.191525441321806,
-2.1645159839332));
#48885=CARTESIAN_POINT('Ctrl Pts',(-0.280899879830252,-0.305408608944229,
-2.15789359161882));
#48886=CARTESIAN_POINT('Ctrl Pts',(-0.155428155340142,-0.384735297878101,
-2.15127119930444));
#48887=CARTESIAN_POINT('Ctrl Pts',(-0.0253776093140804,-0.393130405212394,
-2.14464880699006));
#48888=CARTESIAN_POINT('Ctrl Pts',(0.104672936711982,-0.401525512546686,
-2.13802641467568));
#48889=CARTESIAN_POINT('Ctrl Pts',(0.239302304273997,-0.338989038281399,
-2.1314040223613));
#48890=CARTESIAN_POINT('Ctrl Pts',(0.31677645195751,-0.234196964203578,
-2.12478163004692));
#48891=CARTESIAN_POINT('Ctrl Pts',(0.394250599641022,-0.129404890125758,
-2.11815923773254));
#48892=CARTESIAN_POINT('Ctrl Pts',(0.414569527446035,0.0176427837645943,
-2.11153684541816));
#48893=CARTESIAN_POINT('Ctrl Pts',(0.368416029525569,0.13951762521486,-2.10491445310378));
#48894=CARTESIAN_POINT('Ctrl Pts',(0.322262531605102,0.261392466665128,
-2.0982920607894));
#48895=CARTESIAN_POINT('Ctrl Pts',(0.209636607959153,0.358094475675308,
-2.09166966847501));
#48896=CARTESIAN_POINT('Ctrl Pts',(0.0821826624843472,0.385281129234163,
-2.08504727616063));
#48897=CARTESIAN_POINT('Ctrl Pts',(-0.0452712829904564,0.412467782793019,
-2.07842488384625));
#48898=CARTESIAN_POINT('Ctrl Pts',(-0.187553250294117,0.370139080900551,
-2.07180249153187));
#48899=CARTESIAN_POINT('Ctrl Pts',(-0.27942011289984,0.27770476960976,-2.06518009921749));
#48900=CARTESIAN_POINT('Ctrl Pts',(-0.351387691014076,0.205292657891022,
-2.05999218354616));
#48901=CARTESIAN_POINT('Ctrl Pts',(-0.392415527723301,0.102130741981397,
-2.05480426787483));
#48902=CARTESIAN_POINT('Ctrl Pts',(-0.393365397637326,-0.000357415208850981,
-2.0496163522035));
#48903=CARTESIAN_POINT('Origin',(0.,0.,-2.22));
#48904=CARTESIAN_POINT('',(-0.393882499483816,0.000146440842145469,-1.9062836477965));
#48905=CARTESIAN_POINT('',(-0.393853641092568,0.000174899764659127,-1.9246163522035));
#48906=CARTESIAN_POINT('',(-0.3933,-4.81653586104654E-17,-2.22));
#48907=CARTESIAN_POINT('Ctrl Pts',(-0.393882499483816,0.000146440842145469,
-1.9062836477965));
#48908=CARTESIAN_POINT('Ctrl Pts',(-0.393921042941097,0.0082248682466142,
-1.90669397608276));
#48909=CARTESIAN_POINT('Ctrl Pts',(-0.393694085357014,0.0163010888479467,
-1.90710430436902));
#48910=CARTESIAN_POINT('Ctrl Pts',(-0.393194767449,0.0243604353283438,-1.90751463265527));
#48911=CARTESIAN_POINT('Ctrl Pts',(-0.385136149051954,0.154432272874696,
-1.91413702496965));
#48912=CARTESIAN_POINT('Ctrl Pts',(-0.306134336330414,0.280108815161806,
-1.92075941728403));
#48913=CARTESIAN_POINT('Ctrl Pts',(-0.192415460823864,0.343761321842059,
-1.92738180959842));
#48914=CARTESIAN_POINT('Ctrl Pts',(-0.0786965853173158,0.407413828522312,
-1.9340042019128));
#48915=CARTESIAN_POINT('Ctrl Pts',(0.069739352974242,0.409042299595711,
-1.94062659422718));
#48916=CARTESIAN_POINT('Ctrl Pts',(0.184827335787369,0.347900002736998,
-1.94724898654156));
#48917=CARTESIAN_POINT('Ctrl Pts',(0.299915318600494,0.286757705878285,
-1.95387137885594));
#48918=CARTESIAN_POINT('Ctrl Pts',(0.381655345935191,0.162844641087458,
-1.96049377117032));
#48919=CARTESIAN_POINT('Ctrl Pts',(0.392565683129179,0.0329809094474556,
-1.9671161634847));
#48920=CARTESIAN_POINT('Ctrl Pts',(0.403476020323167,-0.0968828221925501,
-1.97373855579908));
#48921=CARTESIAN_POINT('Ctrl Pts',(0.343556667376447,-0.232697220681733,
-1.98036094811346));
#48922=CARTESIAN_POINT('Ctrl Pts',(0.240283530054112,-0.312184850919123,
-1.98698334042784));
#48923=CARTESIAN_POINT('Ctrl Pts',(0.137010392731777,-0.391672481156512,
-1.99360573274222));
#48924=CARTESIAN_POINT('Ctrl Pts',(-0.00961652896617249,-0.414833343142106,
-2.0002281250566));
#48925=CARTESIAN_POINT('Ctrl Pts',(-0.132361737907768,-0.371047067495075,
-2.00685051737098));
#48926=CARTESIAN_POINT('Ctrl Pts',(-0.255106946849363,-0.327260791848045,
-2.01347290968536));
#48927=CARTESIAN_POINT('Ctrl Pts',(-0.353970443034605,-0.216527378568391,
-2.02009530199974));
#48928=CARTESIAN_POINT('Ctrl Pts',(-0.383618557603471,-0.0896234245099577,
-2.02671769431412));
#48929=CARTESIAN_POINT('Ctrl Pts',(-0.390432405003592,-0.0604578539500652,
-2.02823967880825));
#48930=CARTESIAN_POINT('Ctrl Pts',(-0.393590361196535,-0.030438170670314,
-2.02976166330238));
#48931=CARTESIAN_POINT('Ctrl Pts',(-0.393312671622578,-0.000360778048017763,
-2.0312836477965));
#48932=CARTESIAN_POINT('Ctrl Pts',(-0.393365397637326,-0.000357415208850981,
-2.0496163522035));
#48933=CARTESIAN_POINT('Ctrl Pts',(-0.393628039956887,-0.0286957454733452,
-2.04818187556045));
#48934=CARTESIAN_POINT('Ctrl Pts',(-0.390826554813069,-0.0569825640779221,
-2.0467473989174));
#48935=CARTESIAN_POINT('Ctrl Pts',(-0.384767761572825,-0.0845535818946124,
-2.04531292227435));
#48936=CARTESIAN_POINT('Ctrl Pts',(-0.356796789732301,-0.21183770141908,
-2.03869052995997));
#48937=CARTESIAN_POINT('Ctrl Pts',(-0.259403088143465,-0.323866019778899,
-2.03206813764559));
#48938=CARTESIAN_POINT('Ctrl Pts',(-0.137246354138968,-0.369268163849161,
-2.02544574533121));
#48939=CARTESIAN_POINT('Ctrl Pts',(-0.0150896201344695,-0.414670307919424,
-2.01882335301683));
#48940=CARTESIAN_POINT('Ctrl Pts',(0.13183014628569,-0.393446277700128,
-2.01220096070245));
#48941=CARTESIAN_POINT('Ctrl Pts',(0.236143164597026,-0.315328312035364,
-2.00557856838807));
#48942=CARTESIAN_POINT('Ctrl Pts',(0.340456182908363,-0.2372103463706,-1.99895617607369));
#48943=CARTESIAN_POINT('Ctrl Pts',(0.402162453110875,-0.102198445260367,
-1.99233378375931));
#48944=CARTESIAN_POINT('Ctrl Pts',(0.392966681917479,0.0277979398469947,
-1.98571139144493));
#48945=CARTESIAN_POINT('Ctrl Pts',(0.383770910724084,0.157794324954353,
-1.97908899913055));
#48946=CARTESIAN_POINT('Ctrl Pts',(0.303673098134783,0.282775194058841,
-1.97246660681617));
#48947=CARTESIAN_POINT('Ctrl Pts',(0.189401944351842,0.345430806432652,
-1.96584421450179));
#48948=CARTESIAN_POINT('Ctrl Pts',(0.0751307905688987,0.408086418806465,
-1.95922182218741));
#48949=CARTESIAN_POINT('Ctrl Pts',(-0.0733137044076861,0.4084167744496,
-1.95259942987303));
#48950=CARTESIAN_POINT('Ctrl Pts',(-0.187862598662765,0.34627038940782,
-1.94597703755865));
#48951=CARTESIAN_POINT('Ctrl Pts',(-0.302411492917843,0.28412400436604,
-1.93935464524427));
#48952=CARTESIAN_POINT('Ctrl Pts',(-0.383064786451416,0.159500878639347,
-1.93273225292988));
#48953=CARTESIAN_POINT('Ctrl Pts',(-0.392839064326688,0.0295467104074692,
-1.9261098606155));
#48954=CARTESIAN_POINT('Ctrl Pts',(-0.393573842411656,0.0197774490783411,
-1.92561202447817));
#48955=CARTESIAN_POINT('Ctrl Pts',(-0.393908066836798,0.00997806079885537,
-1.92511418834083));
#48956=CARTESIAN_POINT('Ctrl Pts',(-0.393853641092568,0.000174899764659127,
-1.9246163522035));
#48957=CARTESIAN_POINT('Origin',(0.,0.,-2.22));
#48958=CARTESIAN_POINT('',(-0.392871469582262,0.000278750737986277,-1.7812836477965));
#48959=CARTESIAN_POINT('',(-0.392835179244401,0.000259422774165058,-1.7996163522035));
#48960=CARTESIAN_POINT('',(-0.3933,-4.81653586104654E-17,-2.22));
#48961=CARTESIAN_POINT('Ctrl Pts',(-0.392871469582262,0.000278750737986277,
-1.7812836477965));
#48962=CARTESIAN_POINT('Ctrl Pts',(-0.39317461768958,0.0467057909606455,
-1.78362628886315));
#48963=CARTESIAN_POINT('Ctrl Pts',(-0.385570977921022,0.0930367504725677,
-1.78596892992979));
#48964=CARTESIAN_POINT('Ctrl Pts',(-0.369622026727067,0.136290547422904,
-1.78831157099643));
#48965=CARTESIAN_POINT('Ctrl Pts',(-0.324536070831699,0.258564341974944,
-1.79493396331081));
#48966=CARTESIAN_POINT('Ctrl Pts',(-0.212760094011492,0.356247558037995,
-1.80155635562519));
#48967=CARTESIAN_POINT('Ctrl Pts',(-0.085548758656478,0.3845477419658,-1.80817874793957));
#48968=CARTESIAN_POINT('Ctrl Pts',(0.0416625766985363,0.412847925893605,
-1.81480114025395));
#48969=CARTESIAN_POINT('Ctrl Pts',(0.184309270588358,0.371765077686166,
-1.82142353256833));
#48970=CARTESIAN_POINT('Ctrl Pts',(0.276980951801137,0.280137659549723,
-1.82804592488271));
#48971=CARTESIAN_POINT('Ctrl Pts',(0.369652633013916,0.188510241413279,
-1.83466831719709));
#48972=CARTESIAN_POINT('Ctrl Pts',(0.412349301549651,0.0463382533478326,
-1.84129070951147));
#48973=CARTESIAN_POINT('Ctrl Pts',(0.385492480948253,-0.0811856088911138,
-1.84791310182585));
#48974=CARTESIAN_POINT('Ctrl Pts',(0.358635660346854,-0.208709471130062,
-1.85453549414023));
#48975=CARTESIAN_POINT('Ctrl Pts',(0.262225350608317,-0.32158520754251,
-1.86115788645461));
#48976=CARTESIAN_POINT('Ctrl Pts',(0.140470316595559,-0.368053863061106,
-1.86778027876899));
#48977=CARTESIAN_POINT('Ctrl Pts',(0.0187152825828021,-0.414522518579702,
-1.87440267108337));
#48978=CARTESIAN_POINT('Ctrl Pts',(-0.128384475704176,-0.394584093204449,
-1.88102506339775));
#48979=CARTESIAN_POINT('Ctrl Pts',(-0.233376642811389,-0.317381314114025,
-1.88764745571213));
#48980=CARTESIAN_POINT('Ctrl Pts',(-0.331863418218086,-0.244962075855163,
-1.89385951974026));
#48981=CARTESIAN_POINT('Ctrl Pts',(-0.393298980305362,-0.122154921174261,
-1.90007158376838));
#48982=CARTESIAN_POINT('Ctrl Pts',(-0.393882499483816,0.000146440842145469,
-1.9062836477965));
#48983=CARTESIAN_POINT('Ctrl Pts',(-0.393853641092568,0.000174899764659127,
-1.9246163522035));
#48984=CARTESIAN_POINT('Ctrl Pts',(-0.393184076344219,-0.120427053295461,
-1.91849179602645));
#48985=CARTESIAN_POINT('Ctrl Pts',(-0.333693123404451,-0.241600004870103,
-1.91236723984941));
#48986=CARTESIAN_POINT('Ctrl Pts',(-0.237544312713443,-0.314274144743834,
-1.90624268367236));
#48987=CARTESIAN_POINT('Ctrl Pts',(-0.133580021007958,-0.392855620926195,
-1.89962029135798));
#48988=CARTESIAN_POINT('Ctrl Pts',(0.0132438246199847,-0.414733362553856,
-1.8929978990436));
#48989=CARTESIAN_POINT('Ctrl Pts',(0.135601427943425,-0.369875372654999,
-1.88637550672922));
#48990=CARTESIAN_POINT('Ctrl Pts',(0.257959031266865,-0.325017382756143,
-1.87975311441484));
#48991=CARTESIAN_POINT('Ctrl Pts',(0.355850392285805,-0.21342366133077,
-1.87313072210046));
#48992=CARTESIAN_POINT('Ctrl Pts',(0.384387612878835,-0.0862652979029292,
-1.86650832978608));
#48993=CARTESIAN_POINT('Ctrl Pts',(0.412924833471865,0.0408930655249115,
-1.8598859374717));
#48994=CARTESIAN_POINT('Ctrl Pts',(0.372107913638987,0.183616070955221,
-1.85326354515732));
#48995=CARTESIAN_POINT('Ctrl Pts',(0.280653374634137,0.276458354663846,
-1.84664115284294));
#48996=CARTESIAN_POINT('Ctrl Pts',(0.189198835629287,0.369300638372471,
-1.84001876052856));
#48997=CARTESIAN_POINT('Ctrl Pts',(0.0471066774524689,0.41226220035941,
-1.83339636821418));
#48998=CARTESIAN_POINT('Ctrl Pts',(-0.0804670099849952,0.385643097774413,
-1.8267739758998));
#48999=CARTESIAN_POINT('Ctrl Pts',(-0.20804069742246,0.359023995189416,
-1.82015158358542));
#49000=CARTESIAN_POINT('Ctrl Pts',(-0.321095914120569,0.26282422803248,
-1.81352919127104));
#49001=CARTESIAN_POINT('Ctrl Pts',(-0.36779140466704,0.141156017264642,
-1.80690679895666));
#49002=CARTESIAN_POINT('Ctrl Pts',(-0.38492675250312,0.0965087271794117,
-1.80447665003894));
#49003=CARTESIAN_POINT('Ctrl Pts',(-0.393126154036473,0.0484318773639158,
-1.80204650112122));
#49004=CARTESIAN_POINT('Ctrl Pts',(-0.392835179244401,0.000259422774165058,
-1.7996163522035));
#49005=CARTESIAN_POINT('Origin',(0.,0.,-2.22));
#49006=CARTESIAN_POINT('',(-0.392869409576936,-0.000277735283692127,-1.6562836477965));
#49007=CARTESIAN_POINT('',(-0.392908213753388,-0.000295413535636864,-1.6746163522035));
#49008=CARTESIAN_POINT('',(-0.3933,-4.81653586104654E-17,-2.22));
#49009=CARTESIAN_POINT('Ctrl Pts',(-0.392869409576936,-0.000277735283692127,
-1.6562836477965));
#49010=CARTESIAN_POINT('Ctrl Pts',(-0.39231841054015,0.0844454737480786,
-1.66055860164353));
#49011=CARTESIAN_POINT('Ctrl Pts',(-0.365440590195796,0.169487353070121,
-1.66483355549056));
#49012=CARTESIAN_POINT('Ctrl Pts',(-0.314887675254022,0.236730454170513,
-1.66910850933758));
#49013=CARTESIAN_POINT('Ctrl Pts',(-0.236575429704786,0.340897706463111,
-1.67573090165196));
#49014=CARTESIAN_POINT('Ctrl Pts',(-0.10144875175385,0.402352247389522,
-1.68235329396634));
#49015=CARTESIAN_POINT('Ctrl Pts',(0.0285302764476099,0.392914213645273,
-1.68897568628072));
#49016=CARTESIAN_POINT('Ctrl Pts',(0.158509304649072,0.383476179901023,
-1.6955980785951));
#49017=CARTESIAN_POINT('Ctrl Pts',(0.283340683101057,0.30314557148611,-1.70222047090948));
#49018=CARTESIAN_POINT('Ctrl Pts',(0.345783219731226,0.188757836687558,
-1.70884286322386));
#49019=CARTESIAN_POINT('Ctrl Pts',(0.408225756361394,0.0743701018890073,
-1.71546525553824));
#49020=CARTESIAN_POINT('Ctrl Pts',(0.408279451169747,-0.0740747592931836,
-1.72208764785262));
#49021=CARTESIAN_POINT('Ctrl Pts',(0.345919682503651,-0.188507637020978,
-1.728710040167));
#49022=CARTESIAN_POINT('Ctrl Pts',(0.283559913837555,-0.302940514748773,
-1.73533243248138));
#49023=CARTESIAN_POINT('Ctrl Pts',(0.15878668169701,-0.383361409022173,
-1.74195482479577));
#49024=CARTESIAN_POINT('Ctrl Pts',(0.0288145152734106,-0.392893471144811,
-1.74857721711015));
#49025=CARTESIAN_POINT('Ctrl Pts',(-0.101157651150189,-0.402425533267448,
-1.75519960942453));
#49026=CARTESIAN_POINT('Ctrl Pts',(-0.23632875185684,-0.341068763239323,
-1.7618220017389));
#49027=CARTESIAN_POINT('Ctrl Pts',(-0.314716334724902,-0.236958191704746,
-1.76844439405329));
#49028=CARTESIAN_POINT('Ctrl Pts',(-0.36537466779562,-0.169676259847524,
-1.77272414530102));
#49029=CARTESIAN_POINT('Ctrl Pts',(-0.392317650856458,-0.0845384182902281,
-1.77700389654876));
#49030=CARTESIAN_POINT('Ctrl Pts',(-0.392871469582262,0.000278750737986277,
-1.7812836477965));
#49031=CARTESIAN_POINT('Ctrl Pts',(-0.392835179244401,0.000259422774165058,
-1.7996163522035));
#49032=CARTESIAN_POINT('Ctrl Pts',(-0.392333219409033,-0.0828427497644315,
-1.79542410880684));
#49033=CARTESIAN_POINT('Ctrl Pts',(-0.366564232623453,-0.166229438361573,
-1.79123186541018));
#49034=CARTESIAN_POINT('Ctrl Pts',(-0.317815695830655,-0.232784711784617,
-1.78703962201352));
#49035=CARTESIAN_POINT('Ctrl Pts',(-0.240808732052964,-0.3379205756873,
-1.78041722969914));
#49036=CARTESIAN_POINT('Ctrl Pts',(-0.106459040102747,-0.401055649113928,
-1.77379483738475));
#49037=CARTESIAN_POINT('Ctrl Pts',(0.0236275833273017,-0.393239463766141,
-1.76717244507037));
#49038=CARTESIAN_POINT('Ctrl Pts',(0.153714206757352,-0.385423278418353,
-1.76055005275599));
#49039=CARTESIAN_POINT('Ctrl Pts',(0.279537761667233,-0.306655834296148,
-1.75392766044161));
#49040=CARTESIAN_POINT('Ctrl Pts',(0.343402095349705,-0.193055793661839,
-1.74730526812723));
#49041=CARTESIAN_POINT('Ctrl Pts',(0.407266429032176,-0.0794557530275321,
-1.74068287581285));
#49042=CARTESIAN_POINT('Ctrl Pts',(0.409171541487239,0.0689768841188778,
-1.73406048349847));
#49043=CARTESIAN_POINT('Ctrl Pts',(0.348243847008224,0.184178613247801,
-1.72743809118409));
#49044=CARTESIAN_POINT('Ctrl Pts',(0.287316152529208,0.299380342376726,
-1.72081569886971));
#49045=CARTESIAN_POINT('Ctrl Pts',(0.163555651116115,0.381351163488164,
-1.71419330655533));
#49046=CARTESIAN_POINT('Ctrl Pts',(0.033712486204077,0.392503511870799,
-1.70757091424095));
#49047=CARTESIAN_POINT('Ctrl Pts',(-0.0961306787079625,0.403655860253434,
-1.70094852192657));
#49048=CARTESIAN_POINT('Ctrl Pts',(-0.232056507118945,0.343989735907263,
-1.69432612961219));
#49049=CARTESIAN_POINT('Ctrl Pts',(-0.311736467948381,0.240864927102387,
-1.68770373729781));
#49050=CARTESIAN_POINT('Ctrl Pts',(-0.364225170025122,0.172932070337224,
-1.68334127559971));
#49051=CARTESIAN_POINT('Ctrl Pts',(-0.392306329059268,0.0861405888035373,
-1.6789788139016));
#49052=CARTESIAN_POINT('Ctrl Pts',(-0.392908213753388,-0.000295413535636864,
-1.6746163522035));
#49053=CARTESIAN_POINT('Origin',(0.,0.,-2.22));
#49054=CARTESIAN_POINT('',(-0.393881034687168,-0.000148036108369887,-1.5312836477965));
#49055=CARTESIAN_POINT('',(-0.393905480442768,-0.000118364692204371,-1.5496163522035));
#49056=CARTESIAN_POINT('',(-0.3933,-4.81653586104654E-17,-2.22));
#49057=CARTESIAN_POINT('Ctrl Pts',(-0.393881034687168,-0.000148036108369887,
-1.5312836477965));
#49058=CARTESIAN_POINT('Ctrl Pts',(-0.393292473280845,0.122060084085854,
-1.53749091442391));
#49059=CARTESIAN_POINT('Ctrl Pts',(-0.33196452645596,0.244777913826582,
-1.54369818105132));
#49060=CARTESIAN_POINT('Ctrl Pts',(-0.233606185198687,0.317212399183223,
-1.54990544767873));
#49061=CARTESIAN_POINT('Ctrl Pts',(-0.128669896443015,0.394491112651675,
-1.55652783999311));
#49062=CARTESIAN_POINT('Ctrl Pts',(0.0184153992780236,0.414535949323148,
-1.56315023230749));
#49063=CARTESIAN_POINT('Ctrl Pts',(0.140204018292651,0.368155387320699,
-1.56977262462187));
#49064=CARTESIAN_POINT('Ctrl Pts',(0.261992637307281,0.321774825318249,
-1.57639501693625));
#49065=CARTESIAN_POINT('Ctrl Pts',(0.358484579615499,0.208968864641871,
-1.58301740925064));
#49066=CARTESIAN_POINT('Ctrl Pts',(0.385433647894231,0.0814644648273466,
-1.58963980156502));
#49067=CARTESIAN_POINT('Ctrl Pts',(0.412382716172962,-0.0460399349871773,
-1.5962621938794));
#49068=CARTESIAN_POINT('Ctrl Pts',(0.36978891042221,-0.188242773939847,
-1.60288458619378));
#49069=CARTESIAN_POINT('Ctrl Pts',(0.277183539566904,-0.279937209659278,
-1.60950697850816));
#49070=CARTESIAN_POINT('Ctrl Pts',(0.184578168711598,-0.371631645378708,
-1.61612937082254));
#49071=CARTESIAN_POINT('Ctrl Pts',(0.0419612327517392,-0.412817677864899,
-1.62275176313692));
#49072=CARTESIAN_POINT('Ctrl Pts',(-0.0852705425432246,-0.384609529956089,
-1.6293741554513));
#49073=CARTESIAN_POINT('Ctrl Pts',(-0.21250231783819,-0.356401382047279,
-1.63599654776568));
#49074=CARTESIAN_POINT('Ctrl Pts',(-0.324348932468261,-0.258799053743466,
-1.64261894008006));
#49075=CARTESIAN_POINT('Ctrl Pts',(-0.369523333209527,-0.136557907762166,
-1.64924133239444));
#49076=CARTESIAN_POINT('Ctrl Pts',(-0.385536296653187,-0.0932271060295508,
-1.65158877086179));
#49077=CARTESIAN_POINT('Ctrl Pts',(-0.393171971050278,-0.0468004644348565,
-1.65393620932915));
#49078=CARTESIAN_POINT('Ctrl Pts',(-0.392869409576936,-0.000277735283692127,
-1.6562836477965));
#49079=CARTESIAN_POINT('Ctrl Pts',(-0.392908213753388,-0.000295413535636864,
-1.6746163522035));
#49080=CARTESIAN_POINT('Ctrl Pts',(-0.393220014232531,-0.0450727391726227,
-1.67235642158722));
#49081=CARTESIAN_POINT('Ctrl Pts',(-0.386157320865123,-0.089754666397697,
-1.67009649097095));
#49082=CARTESIAN_POINT('Ctrl Pts',(-0.371293088633588,-0.131669969582669,
-1.66783656035467));
#49083=CARTESIAN_POINT('Ctrl Pts',(-0.327735655241467,-0.254496564199282,
-1.66121416804029));
#49084=CARTESIAN_POINT('Ctrl Pts',(-0.217186695209332,-0.353566260168928,
-1.65459177572591));
#49085=CARTESIAN_POINT('Ctrl Pts',(-0.090338224703861,-0.383450836111131,
-1.64796938341153));
#49086=CARTESIAN_POINT('Ctrl Pts',(0.0365102458016081,-0.413335412053333,
-1.64134699109715));
#49087=CARTESIAN_POINT('Ctrl Pts',(0.179658226780413,-0.374034867968095,
-1.63472459878277));
#49088=CARTESIAN_POINT('Ctrl Pts',(0.273465482775833,-0.283570393883337,
-1.62810220646839));
#49089=CARTESIAN_POINT('Ctrl Pts',(0.367272738771253,-0.193105919798579,
-1.62147981415401));
#49090=CARTESIAN_POINT('Ctrl Pts',(0.411739269783289,-0.0514775157143005,
-1.61485742183963));
#49091=CARTESIAN_POINT('Ctrl Pts',(0.386475032266683,0.0763713820186354,
-1.60823502952524));
#49092=CARTESIAN_POINT('Ctrl Pts',(0.361210794750077,0.204220279751574,
-1.60161263721086));
#49093=CARTESIAN_POINT('Ctrl Pts',(0.266215788704827,0.318289671133168,
-1.59499024489648));
#49094=CARTESIAN_POINT('Ctrl Pts',(0.145049794166852,0.366273252871574,
-1.5883678525821));
#49095=CARTESIAN_POINT('Ctrl Pts',(0.0238837996288819,0.414256834609979,
-1.58174546026772));
#49096=CARTESIAN_POINT('Ctrl Pts',(-0.123453183401811,0.396154606705199,
-1.57512306795334));
#49097=CARTESIAN_POINT('Ctrl Pts',(-0.229400060514477,0.320267311464852,
-1.56850067563896));
#49098=CARTESIAN_POINT('Ctrl Pts',(-0.330105616220708,0.248134253403169,
-1.56220590116047));
#49099=CARTESIAN_POINT('Ctrl Pts',(-0.393415005972842,0.12379210044259,
-1.55591112668199));
#49100=CARTESIAN_POINT('Ctrl Pts',(-0.393905480442768,-0.000118364692204371,
-1.5496163522035));
#49101=CARTESIAN_POINT('Origin',(0.,0.,-2.22));
#49102=CARTESIAN_POINT('',(-0.393315558933435,0.000360657844753393,-1.4062836477965));
#49103=CARTESIAN_POINT('',(-0.393263050796212,0.000361685240310451,-1.4246163522035));
#49104=CARTESIAN_POINT('',(-0.3933,-4.81653586104654E-17,-2.22));
#49105=CARTESIAN_POINT('Ctrl Pts',(-0.393315558933435,0.000360657844753393,
-1.4062836477965));
#49106=CARTESIAN_POINT('Ctrl Pts',(-0.393592470507005,0.0303426814093579,
-1.40780083488992));
#49107=CARTESIAN_POINT('Ctrl Pts',(-0.390454628709984,0.0602673346706706,
-1.40931802198333));
#49108=CARTESIAN_POINT('Ctrl Pts',(-0.383683293576175,0.0893458795311712,
-1.41083520907674));
#49109=CARTESIAN_POINT('Ctrl Pts',(-0.354126993009887,0.216271248744692,
-1.41745760139113));
#49110=CARTESIAN_POINT('Ctrl Pts',(-0.255343630670031,0.327076153958157,
-1.42407999370551));
#49111=CARTESIAN_POINT('Ctrl Pts',(-0.132630130193656,0.370951215826925,
-1.43070238601989));
#49112=CARTESIAN_POINT('Ctrl Pts',(-0.00991662971728322,0.414826277695692,
-1.43732477833427));
#49113=CARTESIAN_POINT('Ctrl Pts',(0.13672700889561,0.391771496219764,-1.44394717064865));
#49114=CARTESIAN_POINT('Ctrl Pts',(0.24005762300338,0.312358597763255,-1.45056956296303));
#49115=CARTESIAN_POINT('Ctrl Pts',(0.343388237111154,0.232945699306743,
-1.45719195527741));
#49116=CARTESIAN_POINT('Ctrl Pts',(0.403405826713803,0.0971746838696504,
-1.46381434759179));
#49117=CARTESIAN_POINT('Ctrl Pts',(0.39258943981379,-0.0326969066633951,
-1.47043673990617));
#49118=CARTESIAN_POINT('Ctrl Pts',(0.381773052913776,-0.162568497196441,
-1.47705913222055));
#49119=CARTESIAN_POINT('Ctrl Pts',(0.300122689511095,-0.286540662825437,
-1.48368152453493));
#49120=CARTESIAN_POINT('Ctrl Pts',(0.185078969041886,-0.347766201890081,
-1.49030391684931));
#49121=CARTESIAN_POINT('Ctrl Pts',(0.0700352485726779,-0.408991740954724,
-1.49692630916369));
#49122=CARTESIAN_POINT('Ctrl Pts',(-0.0784018289630594,-0.407470653455019,
-1.50354870147807));
#49123=CARTESIAN_POINT('Ctrl Pts',(-0.192166722903624,-0.343900431181965,
-1.51017109379245));
#49124=CARTESIAN_POINT('Ctrl Pts',(-0.305931616844188,-0.280330208908911,
-1.51679348610683));
#49125=CARTESIAN_POINT('Ctrl Pts',(-0.385024327189582,-0.154710851862508,
-1.52341587842121));
#49126=CARTESIAN_POINT('Ctrl Pts',(-0.393177041467126,-0.0246448782065889,
-1.53003827073559));
#49127=CARTESIAN_POINT('Ctrl Pts',(-0.393688095623158,-0.0164916725216676,
-1.53045339642256));
#49128=CARTESIAN_POINT('Ctrl Pts',(-0.393920396128007,-0.00832099417415774,
-1.53086852210953));
#49129=CARTESIAN_POINT('Ctrl Pts',(-0.393881034687168,-0.000148036108369887,
-1.5312836477965));
#49130=CARTESIAN_POINT('Ctrl Pts',(-0.393905480442768,-0.000118364692204371,
-1.5496163522035));
#49131=CARTESIAN_POINT('Ctrl Pts',(-0.393931007677293,-0.00656740882723717,
-1.54928873436761));
#49132=CARTESIAN_POINT('Ctrl Pts',(-0.393786371902764,-0.0130152836122568,
-1.54896111653171));
#49133=CARTESIAN_POINT('Ctrl Pts',(-0.393467988982188,-0.0194545676714611,
-1.54863349869582));
#49134=CARTESIAN_POINT('Ctrl Pts',(-0.387032269142592,-0.149616788991508,
-1.54201110638144));
#49135=CARTESIAN_POINT('Ctrl Pts',(-0.309604058268761,-0.276268869055684,
-1.53538871406706));
#49136=CARTESIAN_POINT('Ctrl Pts',(-0.196687915754401,-0.341334736517045,
-1.52876632175268));
#49137=CARTESIAN_POINT('Ctrl Pts',(-0.0837717732400437,-0.406400603978403,
-1.5221439294383));
#49138=CARTESIAN_POINT('Ctrl Pts',(0.0646323009148415,-0.40988025883695,
-1.51552153712392));
#49139=CARTESIAN_POINT('Ctrl Pts',(0.180473899686314,-0.350178111950168,
-1.50889914480954));
#49140=CARTESIAN_POINT('Ctrl Pts',(0.29631549845779,-0.290475965063384,
-1.50227675249516));
#49141=CARTESIAN_POINT('Ctrl Pts',(0.379594621845851,-0.167592016431268,
-1.49565436018078));
#49142=CARTESIAN_POINT('Ctrl Pts',(0.392123785609061,-0.0378744678720334,
-1.4890319678664));
#49143=CARTESIAN_POINT('Ctrl Pts',(0.40465294937227,0.0918430806872008,
-1.48240957555202));
#49144=CARTESIAN_POINT('Ctrl Pts',(0.346432153510629,0.228394229173553,
-1.47578718323764));
#49145=CARTESIAN_POINT('Ctrl Pts',(0.244158433656106,0.30916370717076,-1.46916479092326));
#49146=CARTESIAN_POINT('Ctrl Pts',(0.141884713801586,0.389933185167965,
-1.46254239860888));
#49147=CARTESIAN_POINT('Ctrl Pts',(-0.00444193004581186,0.414920992676028,
-1.4559200062945));
#49148=CARTESIAN_POINT('Ctrl Pts',(-0.127723692593558,0.372669017906287,
-1.44929761398012));
#49149=CARTESIAN_POINT('Ctrl Pts',(-0.251005455141308,0.330417043136545,
-1.44267522166574));
#49150=CARTESIAN_POINT('Ctrl Pts',(-0.351242336389405,0.220925286088996,
-1.43605282935135));
#49151=CARTESIAN_POINT('Ctrl Pts',(-0.382470904359394,0.0944009845048089,
-1.42943043703697));
#49152=CARTESIAN_POINT('Ctrl Pts',(-0.390038007419168,0.0637424403610792,
-1.42782574209248));
#49153=CARTESIAN_POINT('Ctrl Pts',(-0.393553230514098,0.0320838163330584,
-1.42622104714799));
#49154=CARTESIAN_POINT('Ctrl Pts',(-0.393263050796212,0.000361685240310451,
-1.4246163522035));
#49155=CARTESIAN_POINT('Origin',(0.,0.,-2.22));
#49156=CARTESIAN_POINT('',(-0.392657025633087,-4.51440007200321E-5,-1.2812836477965));
#49157=CARTESIAN_POINT('',(-0.392664786614424,-7.33973318879278E-5,-1.2996163522035));
#49158=CARTESIAN_POINT('',(-0.3933,-4.81653586104654E-17,-2.22));
#49159=CARTESIAN_POINT('Ctrl Pts',(-0.392657025633087,-4.51440007200321E-5,
-1.2812836477965));
#49160=CARTESIAN_POINT('Ctrl Pts',(-0.392587038824807,0.0684113828747579,
-1.2847331476703));
#49161=CARTESIAN_POINT('Ctrl Pts',(-0.375581983361472,0.136900451219797,
-1.2881826475441));
#49162=CARTESIAN_POINT('Ctrl Pts',(-0.341842476026,0.195804181628159,-1.2916321474179));
#49163=CARTESIAN_POINT('Ctrl Pts',(-0.277068954575367,0.30888828825698,
-1.29825453973228));
#49164=CARTESIAN_POINT('Ctrl Pts',(-0.150617610293015,0.386643913286418,
-1.30487693204666));
#49165=CARTESIAN_POINT('Ctrl Pts',(-0.0204724675134631,0.393416362182065,
-1.31149932436104));
#49166=CARTESIAN_POINT('Ctrl Pts',(0.109672675266089,0.400188811077712,
-1.31812171667542));
#49167=CARTESIAN_POINT('Ctrl Pts',(0.243511616542838,0.335978083839568,
-1.3247441089898));
#49168=CARTESIAN_POINT('Ctrl Pts',(0.319672763377695,0.230227887783232,
-1.33136650130418));
#49169=CARTESIAN_POINT('Ctrl Pts',(0.39583391021255,0.124477691726897,-1.33798889361856));
#49170=CARTESIAN_POINT('Ctrl Pts',(0.414317262605513,-0.0228119731476319,
-1.34461128593294));
#49171=CARTESIAN_POINT('Ctrl Pts',(0.366647314337019,-0.144101710080452,
-1.35123367824732));
#49172=CARTESIAN_POINT('Ctrl Pts',(0.318977366068527,-0.265391447013271,
-1.3578560705617));
#49173=CARTESIAN_POINT('Ctrl Pts',(0.205154117138584,-0.360681256004386,
-1.36447846287608));
#49174=CARTESIAN_POINT('Ctrl Pts',(0.07737100268419,-0.386276175685614,
-1.37110085519046));
#49175=CARTESIAN_POINT('Ctrl Pts',(-0.0504121117702055,-0.411871095366841,
-1.37772324750484));
#49176=CARTESIAN_POINT('Ctrl Pts',(-0.192155091749049,-0.36777112573818,
-1.38434563981922));
#49177=CARTESIAN_POINT('Ctrl Pts',(-0.282861962342114,-0.27419822431706,
-1.3909680321336));
#49178=CARTESIAN_POINT('Ctrl Pts',(-0.352787929778942,-0.202062832422688,
-1.39607323735457));
#49179=CARTESIAN_POINT('Ctrl Pts',(-0.392383775096574,-0.100526295321156,
-1.40117844257554));
#49180=CARTESIAN_POINT('Ctrl Pts',(-0.393315558933435,0.000360657844753393,
-1.4062836477965));
#49181=CARTESIAN_POINT('Ctrl Pts',(-0.393263050796212,0.000361685240310451,
-1.4246163522035));
#49182=CARTESIAN_POINT('Ctrl Pts',(-0.392355692041059,-0.0988297868196482,
-1.41959865483361));
#49183=CARTESIAN_POINT('Ctrl Pts',(-0.354241338381814,-0.198642193679393,
-1.41458095746372));
#49184=CARTESIAN_POINT('Ctrl Pts',(-0.286455499065155,-0.270441834064746,
-1.40956326009383));
#49185=CARTESIAN_POINT('Ctrl Pts',(-0.196991271109047,-0.365203504929285,
-1.40294086777945));
#49186=CARTESIAN_POINT('Ctrl Pts',(-0.0558425605049488,-0.411170000537543,
-1.39631847546507));
#49187=CARTESIAN_POINT('Ctrl Pts',(0.0722671589327426,-0.387263471420634,
-1.38969608315069));
#49188=CARTESIAN_POINT('Ctrl Pts',(0.200376878370438,-0.363356942303724,
-1.38307369083631));
#49189=CARTESIAN_POINT('Ctrl Pts',(0.315447606641727,-0.269577388461642,
-1.37645129852193));
#49190=CARTESIAN_POINT('Ctrl Pts',(0.364713879321218,-0.148927246625453,
-1.36982890620755));
#49191=CARTESIAN_POINT('Ctrl Pts',(0.413980152000709,-0.0282771047892618,
-1.36320651389317));
#49192=CARTESIAN_POINT('Ctrl Pts',(0.397441969088403,0.119243625041034,
-1.35658412157879));
#49193=CARTESIAN_POINT('Ctrl Pts',(0.322682883023998,0.225989591707873,
-1.34996172926441));
#49194=CARTESIAN_POINT('Ctrl Pts',(0.247923796959597,0.332735558374708,
-1.34333933695003));
#49195=CARTESIAN_POINT('Ctrl Pts',(0.114943807743101,0.398706761878086,
-1.33671694463565));
#49196=CARTESIAN_POINT('Ctrl Pts',(-0.015279362526179,0.393652231846543,
-1.33009455232127));
#49197=CARTESIAN_POINT('Ctrl Pts',(-0.145502532795462,0.388597701814998,
-1.32347216000689));
#49198=CARTESIAN_POINT('Ctrl Pts',(-0.272968884117532,0.312517438248528,
-1.31684976769251));
#49199=CARTESIAN_POINT('Ctrl Pts',(-0.339228962602927,0.200297901856989,
-1.31022737537813));
#49200=CARTESIAN_POINT('Ctrl Pts',(-0.374618350354063,0.140361650989309,
-1.30669036765325));
#49201=CARTESIAN_POINT('Ctrl Pts',(-0.392547983298784,0.0701162796154407,
-1.30315335992837));
#49202=CARTESIAN_POINT('Ctrl Pts',(-0.392664786614424,-7.33973318879278E-5,
-1.2996163522035));
#49203=CARTESIAN_POINT('Origin',(0.,0.,-2.22));
#49204=CARTESIAN_POINT('',(-0.393481653172021,-0.000341139932622969,-1.1562836477965));
#49205=CARTESIAN_POINT('',(-0.393533012869392,-0.000329848589259697,-1.1746163522035));
#49206=CARTESIAN_POINT('',(-0.3933,-4.81653586104654E-17,-2.22));
#49207=CARTESIAN_POINT('Ctrl Pts',(-0.393481653172021,-0.000341139932622969,
-1.1562836477965));
#49208=CARTESIAN_POINT('Ctrl Pts',(-0.392511039428293,0.105896743864737,
-1.16166546045068));
#49209=CARTESIAN_POINT('Ctrl Pts',(-0.348003565773197,0.212851082423324,
-1.16704727310487));
#49210=CARTESIAN_POINT('Ctrl Pts',(-0.271182049778677,0.285754880687094,
-1.17242908575905));
#49211=CARTESIAN_POINT('Ctrl Pts',(-0.17665214883428,0.375463977665029,
-1.17905147807343));
#49212=CARTESIAN_POINT('Ctrl Pts',(-0.0331935172773672,0.413615002898312,
-1.18567387038781));
#49213=CARTESIAN_POINT('Ctrl Pts',(0.0934111612013362,0.382713876050605,
-1.19229626270219));
#49214=CARTESIAN_POINT('Ctrl Pts',(0.220015839680038,0.351812749202898,
-1.19891865501657));
#49215=CARTESIAN_POINT('Ctrl Pts',(0.329766565080531,0.251859470274202,
-1.20554104733095));
#49216=CARTESIAN_POINT('Ctrl Pts',(0.372337350214068,0.128687425936748,
-1.21216343964533));
#49217=CARTESIAN_POINT('Ctrl Pts',(0.414908135347607,0.00551538159929298,
-1.21878583195971));
#49218=CARTESIAN_POINT('Ctrl Pts',(0.390298980214189,-0.140875428146921,
-1.22540822427409));
#49219=CARTESIAN_POINT('Ctrl Pts',(0.309794366273512,-0.243357774858033,
-1.23203061658847));
#49220=CARTESIAN_POINT('Ctrl Pts',(0.229289752332836,-0.345840121569143,
-1.23865300890285));
#49221=CARTESIAN_POINT('Ctrl Pts',(0.0928896795849039,-0.404414005245154,
-1.24527540121723));
#49222=CARTESIAN_POINT('Ctrl Pts',(-0.0368598570476348,-0.392220482505807,
-1.25189779353161));
#49223=CARTESIAN_POINT('Ctrl Pts',(-0.166609393680174,-0.38002695976646,
-1.258520185846));
#49224=CARTESIAN_POINT('Ctrl Pts',(-0.289708394197319,-0.297066030611755,
-1.26514257816038));
#49225=CARTESIAN_POINT('Ctrl Pts',(-0.349710045146433,-0.181379271920303,
-1.27176497047476));
#49226=CARTESIAN_POINT('Ctrl Pts',(-0.378457780961706,-0.125951924112699,
-1.27493786291534));
#49227=CARTESIAN_POINT('Ctrl Pts',(-0.392721400360745,-0.0630122999880512,
-1.27811075535592));
#49228=CARTESIAN_POINT('Ctrl Pts',(-0.392657025633087,-4.51440007200321E-5,
-1.2812836477965));
#49229=CARTESIAN_POINT('Ctrl Pts',(-0.392664786614424,-7.33973318879278E-5,
-1.2996163522035));
#49230=CARTESIAN_POINT('Ctrl Pts',(-0.392766675888667,-0.0613008993450839,
-1.29653096761399));
#49231=CARTESIAN_POINT('Ctrl Pts',(-0.379314189765856,-0.122486021613986,
-1.29344558302449));
#49232=CARTESIAN_POINT('Ctrl Pts',(-0.352072966544274,-0.176748874920563,
-1.29036019843499));
#49233=CARTESIAN_POINT('Ctrl Pts',(-0.293603086351501,-0.293217306089983,
-1.28373780612061));
#49234=CARTESIAN_POINT('Ctrl Pts',(-0.171609520317232,-0.37779535921221,
-1.27711541380623));
#49235=CARTESIAN_POINT('Ctrl Pts',(-0.042032187006433,-0.39169992827728,
-1.27049302149184));
#49236=CARTESIAN_POINT('Ctrl Pts',(0.0875451463043619,-0.40560449734235,
-1.26387062917746));
#49237=CARTESIAN_POINT('Ctrl Pts',(0.224706246891688,-0.348835582350259,
-1.25724823686308));
#49238=CARTESIAN_POINT('Ctrl Pts',(0.306556151959042,-0.247424461711115,
-1.2506258445487));
#49239=CARTESIAN_POINT('Ctrl Pts',(0.388406057026397,-0.14601334107197,
-1.24400345223432));
#49240=CARTESIAN_POINT('Ctrl Pts',(0.414944766573788,3.99852142250606E-5,
-1.23738105991994));
#49241=CARTESIAN_POINT('Ctrl Pts',(0.374003005620899,0.123763041104785,
-1.23075866760556));
#49242=CARTESIAN_POINT('Ctrl Pts',(0.333061244668009,0.247486096995346,
-1.22413627529118));
#49243=CARTESIAN_POINT('Ctrl Pts',(0.224639013214835,0.348878882490268,
-1.2175138829768));
#49244=CARTESIAN_POINT('Ctrl Pts',(0.0984531200676662,0.381447927908793,
-1.21089149066242));
#49245=CARTESIAN_POINT('Ctrl Pts',(-0.0277327730795022,0.414016973327319,
-1.20426909834804));
#49246=CARTESIAN_POINT('Ctrl Pts',(-0.171682327920667,0.377762278669448,
-1.19764670603366));
#49247=CARTESIAN_POINT('Ctrl Pts',(-0.267387748823254,0.289308365479125,
-1.19102431371928));
#49248=CARTESIAN_POINT('Ctrl Pts',(-0.346429218455074,0.216255791995698,
-1.18555499321402));
#49249=CARTESIAN_POINT('Ctrl Pts',(-0.392564206260852,0.107599042506983,
-1.18008567270876));
#49250=CARTESIAN_POINT('Ctrl Pts',(-0.393533012869392,-0.000329848589259697,
-1.1746163522035));
#49251=CARTESIAN_POINT('Origin',(0.,0.,-2.22));
#49252=CARTESIAN_POINT('',(-0.393775421980258,0.000232396782078516,-1.0312836477965));
#49253=CARTESIAN_POINT('',(-0.393734572290504,0.000255441356017315,-1.0496163522035));
#49254=CARTESIAN_POINT('',(-0.3933,-4.81653586104654E-17,-2.22));
#49255=CARTESIAN_POINT('Ctrl Pts',(-0.393775421980258,0.000232396782078516,
-1.0312836477965));
#49256=CARTESIAN_POINT('Ctrl Pts',(-0.393870807162874,0.0138608314386894,
-1.03197538091669));
#49257=CARTESIAN_POINT('Ctrl Pts',(-0.393224744870318,0.0274801192648313,
-1.03266711403687));
#49258=CARTESIAN_POINT('Ctrl Pts',(-0.391807383245153,0.0410186590863903,
-1.03335884715706));
#49259=CARTESIAN_POINT('Ctrl Pts',(-0.3782380969709,0.170631539322734,-1.03998123947144));
#49260=CARTESIAN_POINT('Ctrl Pts',(-0.29397593879586,0.292843520708426,
-1.04660363178582));
#49261=CARTESIAN_POINT('Ctrl Pts',(-0.177659161700493,0.351614530732929,
-1.0532260241002));
#49262=CARTESIAN_POINT('Ctrl Pts',(-0.0613423846051261,0.410385540757432,
-1.05984841641458));
#49263=CARTESIAN_POINT('Ctrl Pts',(0.0870290114105677,0.405715579420747,
-1.06647080872896));
#49264=CARTESIAN_POINT('Ctrl Pts',(0.199419603821458,0.33974604864568,-1.07309320104334));
#49265=CARTESIAN_POINT('Ctrl Pts',(0.311810196232349,0.273776517870612,
-1.07971559335772));
#49266=CARTESIAN_POINT('Ctrl Pts',(0.388219985038436,0.146507417657162,
-1.0863379856721));
#49267=CARTESIAN_POINT('Ctrl Pts',(0.393611406355585,0.0162977527726593,
-1.09296037798648));
#49268=CARTESIAN_POINT('Ctrl Pts',(0.399002827672734,-0.113911912111845,
-1.09958277030087));
#49269=CARTESIAN_POINT('Ctrl Pts',(0.333375881500942,-0.247062141667403,
-1.10620516261525));
#49270=CARTESIAN_POINT('Ctrl Pts',(0.226823679664539,-0.322097150409778,
-1.11282755492963));
#49271=CARTESIAN_POINT('Ctrl Pts',(0.120271477828136,-0.397132159152151,
-1.11944994724401));
#49272=CARTESIAN_POINT('Ctrl Pts',(-0.0272059796728769,-0.414051947081344,
-1.12607233955839));
#49273=CARTESIAN_POINT('Ctrl Pts',(-0.147983184125541,-0.365097977500186,
-1.13269473187277));
#49274=CARTESIAN_POINT('Ctrl Pts',(-0.268760388578204,-0.316144007919027,
-1.13931712418715));
#49275=CARTESIAN_POINT('Ctrl Pts',(-0.362837339982519,-0.201316280827518,
-1.14593951650153));
#49276=CARTESIAN_POINT('Ctrl Pts',(-0.387075230518735,-0.0732688329204707,
-1.15256190881591));
#49277=CARTESIAN_POINT('Ctrl Pts',(-0.391615739835896,-0.0492815709352832,
-1.15380248847611));
#49278=CARTESIAN_POINT('Ctrl Pts',(-0.39370539259696,-0.0248303903488462,
-1.1550430681363));
#49279=CARTESIAN_POINT('Ctrl Pts',(-0.393481653172021,-0.000341139932622969,
-1.1562836477965));
#49280=CARTESIAN_POINT('Ctrl Pts',(-0.393533012869392,-0.000329848589259697,
-1.1746163522035));
#49281=CARTESIAN_POINT('Ctrl Pts',(-0.393737261932456,-0.0230840027100406,
-1.17346328039438));
#49282=CARTESIAN_POINT('Ctrl Pts',(-0.391933993525686,-0.045805805447558,
-1.17231020858526));
#49283=CARTESIAN_POINT('Ctrl Pts',(-0.388008326502387,-0.0681548026318557,
-1.17115713677614));
#49284=CARTESIAN_POINT('Ctrl Pts',(-0.365462196314924,-0.196510925829749,
-1.16453474446176));
#49285=CARTESIAN_POINT('Ctrl Pts',(-0.272908648975983,-0.312570040502759,
-1.15791235214738));
#49286=CARTESIAN_POINT('Ctrl Pts',(-0.152787938257515,-0.363113459513673,
-1.151289959833));
#49287=CARTESIAN_POINT('Ctrl Pts',(-0.0326672275390472,-0.413656878524587,
-1.14466756751862));
#49288=CARTESIAN_POINT('Ctrl Pts',(0.115020646558947,-0.398684601873405,
-1.13804517520424));
#49289=CARTESIAN_POINT('Ctrl Pts',(0.222553689191635,-0.325062138650695,
-1.13142278288986));
#49290=CARTESIAN_POINT('Ctrl Pts',(0.330086731824319,-0.251439675427988,
-1.12480039057547));
#49291=CARTESIAN_POINT('Ctrl Pts',(0.3974649429917,-0.119167025633755,-1.11817799826109));
#49292=CARTESIAN_POINT('Ctrl Pts',(0.393792171623827,0.0111024377845789,
-1.11155560594671));
#49293=CARTESIAN_POINT('Ctrl Pts',(0.390119400255954,0.141371901202919,
-1.10493321363233));
#49294=CARTESIAN_POINT('Ctrl Pts',(0.315395646352824,0.269638178245362,
-1.09831082131795));
#49295=CARTESIAN_POINT('Ctrl Pts',(0.203885345688334,0.337085010598986,
-1.09168842900357));
#49296=CARTESIAN_POINT('Ctrl Pts',(0.092375045023848,0.404531842952609,
-1.08506603668919));
#49297=CARTESIAN_POINT('Ctrl Pts',(-0.0559218024019938,0.411159230617415,
-1.07844364437481));
#49298=CARTESIAN_POINT('Ctrl Pts',(-0.173003958178694,0.353928197536556,
-1.07182125206043));
#49299=CARTESIAN_POINT('Ctrl Pts',(-0.290086113955397,0.296697164455695,
-1.06519885974605));
#49300=CARTESIAN_POINT('Ctrl Pts',(-0.375953578082954,0.175607710629166,
-1.05857646743167));
#49301=CARTESIAN_POINT('Ctrl Pts',(-0.391231987577939,0.0461851756820929,
-1.05195407511729));
#49302=CARTESIAN_POINT('Ctrl Pts',(-0.393029761265915,0.0309563373638524,
-1.05117483414603));
#49303=CARTESIAN_POINT('Ctrl Pts',(-0.39385018271193,0.0156121220150227,
-1.05039559317476));
#49304=CARTESIAN_POINT('Ctrl Pts',(-0.393734572290504,0.000255441356017315,
-1.0496163522035));
#49305=CARTESIAN_POINT('Origin',(0.,0.,-2.22));
#49306=CARTESIAN_POINT('',(-0.392765335323044,0.000211032987566279,-0.906283647796502));
#49307=CARTESIAN_POINT('',(-0.392738865073111,0.000187005706935053,-0.924616352203497));
#49308=CARTESIAN_POINT('',(-0.3933,-4.81653586104654E-17,-2.22));
#49309=CARTESIAN_POINT('Ctrl Pts',(-0.392765335323044,0.000211032987566279,
-0.906283647796502));
#49310=CARTESIAN_POINT('Ctrl Pts',(-0.393018178513626,0.0522502699719019,
-0.908907693697072));
#49311=CARTESIAN_POINT('Ctrl Pts',(-0.383411587472077,0.104199912603151,
-0.911531739597643));
#49312=CARTESIAN_POINT('Ctrl Pts',(-0.363507551178323,0.151848003592403,
-0.914155785498213));
#49313=CARTESIAN_POINT('Ctrl Pts',(-0.313275069746406,0.272099082848873,
-0.920778177812594));
#49314=CARTESIAN_POINT('Ctrl Pts',(-0.197455787633044,0.364952588896186,
-0.927400570126975));
#49315=CARTESIAN_POINT('Ctrl Pts',(-0.0691584172096336,0.387830722464993,
-0.934022962441355));
#49316=CARTESIAN_POINT('Ctrl Pts',(0.0591389532137729,0.410708856033799,
-0.940645354755735));
#49317=CARTESIAN_POINT('Ctrl Pts',(0.199914411947228,0.363611617124105,
-0.947267747070115));
#49318=CARTESIAN_POINT('Ctrl Pts',(0.288615639114422,0.268135355403262,
-0.953890139384496));
#49319=CARTESIAN_POINT('Ctrl Pts',(0.377316866281618,0.172659093682417,
-0.960512531698877));
#49320=CARTESIAN_POINT('Ctrl Pts',(0.41394386188255,0.028803809150419,-0.967134924013258));
#49321=CARTESIAN_POINT('Ctrl Pts',(0.38170138648123,-0.0974659300318142,
-0.973757316327638));
#49322=CARTESIAN_POINT('Ctrl Pts',(0.349458911079909,-0.223735669214047,
-0.980379708642019));
#49323=CARTESIAN_POINT('Ctrl Pts',(0.24834696467634,-0.332419863046513,
-0.987002100956397));
#49324=CARTESIAN_POINT('Ctrl Pts',(0.124730238718036,-0.373681580370242,
-0.993624493270778));
#49325=CARTESIAN_POINT('Ctrl Pts',(0.00111351275973311,-0.414943297693971,
-1.00024688558516));
#49326=CARTESIAN_POINT('Ctrl Pts',(-0.145007992753303,-0.388782538508961,
-1.00686927789954));
#49327=CARTESIAN_POINT('Ctrl Pts',(-0.246630538323087,-0.307195269372958,
-1.01349167021392));
#49328=CARTESIAN_POINT('Ctrl Pts',(-0.337638236992966,-0.234130089169133,
-1.01942232940811));
#49329=CARTESIAN_POINT('Ctrl Pts',(-0.392957625356443,-0.116612668084744,
-1.02535298860231));
#49330=CARTESIAN_POINT('Ctrl Pts',(-0.393775421980258,0.000232396782078516,
-1.0312836477965));
#49331=CARTESIAN_POINT('Ctrl Pts',(-0.393734572290504,0.000255441356017315,
-1.0496163522035));
#49332=CARTESIAN_POINT('Ctrl Pts',(-0.392867665628586,-0.114896883184711,
-1.04377320086038));
#49333=CARTESIAN_POINT('Ctrl Pts',(-0.33936979228434,-0.230750104080959,
-1.03793004951726));
#49334=CARTESIAN_POINT('Ctrl Pts',(-0.250662643696462,-0.303914095777196,
-1.03208689817415));
#49335=CARTESIAN_POINT('Ctrl Pts',(-0.150125535457593,-0.386835216221796,
-1.02546450585977));
#49336=CARTESIAN_POINT('Ctrl Pts',(-0.00436196411744454,-0.414921841043383,
-1.01884211354539));
#49337=CARTESIAN_POINT('Ctrl Pts',(0.119788460862806,-0.37529490164548,
-1.01221972123101));
#49338=CARTESIAN_POINT('Ctrl Pts',(0.243938885843059,-0.335667962247576,
-1.00559732891663));
#49339=CARTESIAN_POINT('Ctrl Pts',(0.346476164463412,-0.228327458630178,
-0.998974936602248));
#49340=CARTESIAN_POINT('Ctrl Pts',(0.380382021888903,-0.102494175350018,
-0.992352544287867));
#49341=CARTESIAN_POINT('Ctrl Pts',(0.414287879314394,0.0233391079301406,
-0.985730151973486));
#49342=CARTESIAN_POINT('Ctrl Pts',(0.379562315545022,0.167665170873064,
-0.979107759659106));
#49343=CARTESIAN_POINT('Ctrl Pts',(0.292128672053041,0.264303570769479,
-0.972485367344726));
#49344=CARTESIAN_POINT('Ctrl Pts',(0.204695028561061,0.360941970665893,
-0.965862975030346));
#49345=CARTESIAN_POINT('Ctrl Pts',(0.0645533053464747,0.409892707515805,
-0.959240582715966));
#49346=CARTESIAN_POINT('Ctrl Pts',(-0.064034775935856,0.388709513683181,
-0.952618190401585));
#49347=CARTESIAN_POINT('Ctrl Pts',(-0.19262285721819,0.367526319850557,
-0.945995798087205));
#49348=CARTESIAN_POINT('Ctrl Pts',(-0.309657296568267,0.276209195335393,
-0.939373405772824));
#49349=CARTESIAN_POINT('Ctrl Pts',(-0.361472173566141,0.156631434566436,
-0.932751013458443));
#49350=CARTESIAN_POINT('Ctrl Pts',(-0.382687894025607,0.107670045625049,
-0.930039459706794));
#49351=CARTESIAN_POINT('Ctrl Pts',(-0.39296947761259,0.0539707275446464,
-0.927327905955146));
#49352=CARTESIAN_POINT('Ctrl Pts',(-0.392738865073111,0.000187005706935053,
-0.924616352203497));
#49353=CARTESIAN_POINT('Origin',(0.,0.,-2.22));
#49354=CARTESIAN_POINT('',(-0.393002927928462,-0.000327777057962136,-0.781283647796501));
#49355=CARTESIAN_POINT('',(-0.39304905505562,-0.000339067021170478,-0.799616352203498));
#49356=CARTESIAN_POINT('',(-0.3933,-4.81653586104654E-17,-2.22));
#49357=CARTESIAN_POINT('Ctrl Pts',(-0.393002927928462,-0.000327777057962136,
-0.781283647796501));
#49358=CARTESIAN_POINT('Ctrl Pts',(-0.392293971122862,0.0898952132304527,
-0.785840006477456));
#49359=CARTESIAN_POINT('Ctrl Pts',(-0.36143409706416,0.180556321363059,
-0.790396365158411));
#49360=CARTESIAN_POINT('Ctrl Pts',(-0.304561599573614,0.249875545069579,
-0.794952723839366));
#49361=CARTESIAN_POINT('Ctrl Pts',(-0.221900857377157,0.350626852518592,
-0.801575116153747));
#49362=CARTESIAN_POINT('Ctrl Pts',(-0.084288791991676,0.406293711194743,
-0.808197508468127));
#49363=CARTESIAN_POINT('Ctrl Pts',(0.0451728447326011,0.391350188523557,
-0.814819900782507));
#49364=CARTESIAN_POINT('Ctrl Pts',(0.17463448145688,0.37640666585237,-0.821442293096888));
#49365=CARTESIAN_POINT('Ctrl Pts',(0.295945689519953,0.290852761833842,
-0.828064685411268));
#49366=CARTESIAN_POINT('Ctrl Pts',(0.353479444311675,0.173919057057502,
-0.834687077725648));
#49367=CARTESIAN_POINT('Ctrl Pts',(0.411013199103396,0.056985352281164,
-0.841309470040029));
#49368=CARTESIAN_POINT('Ctrl Pts',(0.404769500623766,-0.0913281532529836,
-0.847931862354409));
#49369=CARTESIAN_POINT('Ctrl Pts',(0.33761138498075,-0.203012582590438,
-0.85455425466879));
#49370=CARTESIAN_POINT('Ctrl Pts',(0.270453269337734,-0.314697011927891,
-0.86117664698317));
#49371=CARTESIAN_POINT('Ctrl Pts',(0.142380736531329,-0.389752365068654,
-0.867799039297551));
#49372=CARTESIAN_POINT('Ctrl Pts',(0.0121212038221099,-0.393762152036687,
-0.874421431611931));
#49373=CARTESIAN_POINT('Ctrl Pts',(-0.118138328887113,-0.397771939004719,
-0.881043823926311));
#49374=CARTESIAN_POINT('Ctrl Pts',(-0.250584861499151,-0.330736159800021,
-0.887666216240692));
#49375=CARTESIAN_POINT('Ctrl Pts',(-0.324485287429933,-0.223393943964857,
-0.894288608555073));
#49376=CARTESIAN_POINT('Ctrl Pts',(-0.369103529444641,-0.15858483218769,
-0.898286954968882));
#49377=CARTESIAN_POINT('Ctrl Pts',(-0.39238006970551,-0.0790828911501493,
-0.902285301382692));
#49378=CARTESIAN_POINT('Ctrl Pts',(-0.392765335323044,0.000211032987566279,
-0.906283647796502));
#49379=CARTESIAN_POINT('Ctrl Pts',(-0.392738865073111,0.000187005706935053,
-0.924616352203497));
#49380=CARTESIAN_POINT('Ctrl Pts',(-0.392406255619253,-0.0773845538766605,
-0.920705513640765));
#49381=CARTESIAN_POINT('Ctrl Pts',(-0.370206263908016,-0.155131689448642,
-0.916794675078034));
#49382=CARTESIAN_POINT('Ctrl Pts',(-0.327404810574654,-0.219092739655027,
-0.912883836515302));
#49383=CARTESIAN_POINT('Ctrl Pts',(-0.254927255939623,-0.32740075608478,
-0.906261444200922));
#49384=CARTESIAN_POINT('Ctrl Pts',(-0.123376832023891,-0.396178391921544,
-0.899639051886542));
#49385=CARTESIAN_POINT('Ctrl Pts',(0.0069242635333148,-0.393887792564699,
-0.893016659572162));
#49386=CARTESIAN_POINT('Ctrl Pts',(0.137225359090526,-0.391597193207854,
-0.886394267257781));
#49387=CARTESIAN_POINT('Ctrl Pts',(0.266277126289207,-0.318238358657399,
-0.8797718749434));
#49388=CARTESIAN_POINT('Ctrl Pts',(0.334903121793558,-0.207449843504157,
-0.87314948262902));
#49389=CARTESIAN_POINT('Ctrl Pts',(0.403529117297906,-0.0966613283509224,
-0.86652709031464));
#49390=CARTESIAN_POINT('Ctrl Pts',(0.411729341107924,0.0515568674050974,
-0.85990469800026));
#49391=CARTESIAN_POINT('Ctrl Pts',(0.355743596132414,0.169239570927571,
-0.85328230568588));
#49392=CARTESIAN_POINT('Ctrl Pts',(0.299757851156902,0.28692227445005,-0.846659913371499));
#49393=CARTESIAN_POINT('Ctrl Pts',(0.179586137395857,0.374069485738985,
-0.840037521057118));
#49394=CARTESIAN_POINT('Ctrl Pts',(0.0503329665062123,0.390720016174824,
-0.833415128742737));
#49395=CARTESIAN_POINT('Ctrl Pts',(-0.0789202043834344,0.407370546610663,
-0.826792736428357));
#49396=CARTESIAN_POINT('Ctrl Pts',(-0.217254832401677,0.353524396193406,
-0.820170344113977));
#49397=CARTESIAN_POINT('Ctrl Pts',(-0.301237835972056,0.253872615175097,
-0.813547951799596));
#49398=CARTESIAN_POINT('Ctrl Pts',(-0.36012982560746,0.183993099018452,
-0.808904085267564));
#49399=CARTESIAN_POINT('Ctrl Pts',(-0.39229530980714,0.0915894274629187,
-0.804260218735531));
#49400=CARTESIAN_POINT('Ctrl Pts',(-0.39304905505562,-0.000339067021170478,
-0.799616352203498));
#49401=CARTESIAN_POINT('Origin',(0.,0.,-2.22));
#49402=CARTESIAN_POINT('',(-0.393941093179356,-4.92117729247177E-5,-0.656283647796501));
#49403=CARTESIAN_POINT('',(-0.393947723570607,-1.70646636204014E-5,-0.674616352203497));
#49404=CARTESIAN_POINT('',(-0.3933,-4.81653586104654E-17,-2.22));
#49405=CARTESIAN_POINT('Ctrl Pts',(-0.393941093179356,-4.92117729247177E-5,
-0.656283647796501));
#49406=CARTESIAN_POINT('Ctrl Pts',(-0.393716310075701,0.12764716684489,
-0.662772319257841));
#49407=CARTESIAN_POINT('Ctrl Pts',(-0.325876029158443,0.255548516106423,
-0.66926099071918));
#49408=CARTESIAN_POINT('Ctrl Pts',(-0.219939066679139,0.326836905668438,
-0.675749662180519));
#49409=CARTESIAN_POINT('Ctrl Pts',(-0.1118189175374,0.399594431758779,-0.6823720544949));
#49410=CARTESIAN_POINT('Ctrl Pts',(0.035984312963528,0.41338155429621,-0.68899444680928));
#49411=CARTESIAN_POINT('Ctrl Pts',(0.155695733519729,0.361876214363877,
-0.69561683912366));
#49412=CARTESIAN_POINT('Ctrl Pts',(0.275407154075931,0.310370874431544,
-0.702239231438041));
#49413=CARTESIAN_POINT('Ctrl Pts',(0.367026764687403,0.193573072029449,
-0.708861623752421));
#49414=CARTESIAN_POINT('Ctrl Pts',(0.388542566498581,0.0650402181532038,
-0.715484016066801));
#49415=CARTESIAN_POINT('Ctrl Pts',(0.410058368309758,-0.0634926357230411,
-0.722106408381182));
#49416=CARTESIAN_POINT('Ctrl Pts',(0.361470361320636,-0.203760541073438,
-0.728728800695563));
#49417=CARTESIAN_POINT('Ctrl Pts',(0.265058484077097,-0.291443915663717,
-0.735351193009943));
#49418=CARTESIAN_POINT('Ctrl Pts',(0.168646606833558,-0.379127290253996,
-0.741973585324323));
#49419=CARTESIAN_POINT('Ctrl Pts',(0.0244108593356022,-0.414226134084162,
-0.748595977638704));
#49420=CARTESIAN_POINT('Ctrl Pts',(-0.101509729683807,-0.380645938817388,
-0.755218369953084));
#49421=CARTESIAN_POINT('Ctrl Pts',(-0.227430318703216,-0.347065743550613,
-0.761840762267464));
#49422=CARTESIAN_POINT('Ctrl Pts',(-0.335035749244076,-0.244806509186898,
-0.768463154581844));
#49423=CARTESIAN_POINT('Ctrl Pts',(-0.37498375501079,-0.120759013894103,
-0.775085546896225));
#49424=CARTESIAN_POINT('Ctrl Pts',(-0.387446611269409,-0.0820590569524739,
-0.77715158052965));
#49425=CARTESIAN_POINT('Ctrl Pts',(-0.393324397046145,-0.0412384571638166,
-0.779217614163076));
#49426=CARTESIAN_POINT('Ctrl Pts',(-0.393002927928462,-0.000327777057962136,
-0.781283647796501));
#49427=CARTESIAN_POINT('Ctrl Pts',(-0.39304905505562,-0.000339067021170478,
-0.799616352203498));
#49428=CARTESIAN_POINT('Ctrl Pts',(-0.393370189265045,-0.0395053297064864,
-0.797637826421151));
#49429=CARTESIAN_POINT('Ctrl Pts',(-0.387989471362798,-0.0785853383517939,
-0.795659300638803));
#49430=CARTESIAN_POINT('Ctrl Pts',(-0.376544560585247,-0.115800399181673,
-0.793680774856456));
#49431=CARTESIAN_POINT('Ctrl Pts',(-0.338236902505551,-0.240364220900791,
-0.787058382542075));
#49432=CARTESIAN_POINT('Ctrl Pts',(-0.231990207223642,-0.344034452719668,
-0.780435990227694));
#49433=CARTESIAN_POINT('Ctrl Pts',(-0.106523695556455,-0.379273306260755,
-0.773813597913313));
#49434=CARTESIAN_POINT('Ctrl Pts',(0.0189428161107277,-0.414512159801841,
-0.767191205598933));
#49435=CARTESIAN_POINT('Ctrl Pts',(0.163629144163188,-0.381319635065142,
-0.760568813284553));
#49436=CARTESIAN_POINT('Ctrl Pts',(0.261189647008292,-0.294916101379107,
-0.753946420970173));
#49437=CARTESIAN_POINT('Ctrl Pts',(0.358750149853395,-0.208512567693073,
-0.747324028655793));
#49438=CARTESIAN_POINT('Ctrl Pts',(0.409184827491143,-0.068898025057705,
-0.740701636341412));
#49439=CARTESIAN_POINT('Ctrl Pts',(0.389366954048811,0.0599075425278824,
-0.734079244027032));
#49440=CARTESIAN_POINT('Ctrl Pts',(0.369549080606479,0.188713110113473,
-0.727456851712651));
#49441=CARTESIAN_POINT('Ctrl Pts',(0.279478656084064,0.306709702649283,
-0.720834459398271));
#49442=CARTESIAN_POINT('Ctrl Pts',(0.160457302990818,0.359790206195045,
-0.71421206708389));
#49443=CARTESIAN_POINT('Ctrl Pts',(0.0414359498975732,0.412870709740808,
-0.70758967476951));
#49444=CARTESIAN_POINT('Ctrl Pts',(-0.106536331766501,0.401035124296523,
-0.700967282455129));
#49445=CARTESIAN_POINT('Ctrl Pts',(-0.215607132606148,0.329710635142869,
-0.694344890140749));
#49446=CARTESIAN_POINT('Ctrl Pts',(-0.323916805307495,0.258883869259115,
-0.687768710828331));
#49447=CARTESIAN_POINT('Ctrl Pts',(-0.39386603477197,0.129395564904208,
-0.681192531515914));
#49448=CARTESIAN_POINT('Ctrl Pts',(-0.393947723570607,-1.70646636204014E-5,
-0.674616352203497));
#49449=CARTESIAN_POINT('Origin',(0.,0.,-2.22));
#49450=CARTESIAN_POINT('',(-0.393149297351444,0.000355296501015012,-0.531283647796502));
#49451=CARTESIAN_POINT('',(-0.393099733010831,0.000348606307955762,-0.549616352203497));
#49452=CARTESIAN_POINT('',(-0.3933,-4.81653586104654E-17,-2.22));
#49453=CARTESIAN_POINT('Ctrl Pts',(-0.393149297351444,0.000355296501015012,
-0.531283647796502));
#49454=CARTESIAN_POINT('Ctrl Pts',(-0.393461166186674,0.0359366493735391,
-0.533082239723845));
#49455=CARTESIAN_POINT('Ctrl Pts',(-0.389030068485141,0.0714416959129314,
-0.534880831651188));
#49456=CARTESIAN_POINT('Ctrl Pts',(-0.37954765186827,0.105542105043303,
-0.53667942357853));
#49457=CARTESIAN_POINT('Ctrl Pts',(-0.344633515998606,0.231099372319518,
-0.543301815892911));
#49458=CARTESIAN_POINT('Ctrl Pts',(-0.241238502260482,0.337613929272207,
-0.549924208207292));
#49459=CARTESIAN_POINT('Ctrl Pts',(-0.116774198388218,0.376243727589222,
-0.556546600521672));
#49460=CARTESIAN_POINT('Ctrl Pts',(0.00769010548404041,0.414873525906236,
-0.563168992836052));
#49461=CARTESIAN_POINT('Ctrl Pts',(0.153223699490438,0.385618565587579,
-0.569791385150432));
#49462=CARTESIAN_POINT('Ctrl Pts',(0.253092429885495,0.30189365327583,-0.576413777464812));
#49463=CARTESIAN_POINT('Ctrl Pts',(0.352961160280556,0.218168740964078,
-0.583036169779193));
#49464=CARTESIAN_POINT('Ctrl Pts',(0.407165027064274,0.0799738766592314,
-0.589658562093574));
#49465=CARTESIAN_POINT('Ctrl Pts',(0.390848949798998,-0.0493219464573787,
-0.596280954407955));
#49466=CARTESIAN_POINT('Ctrl Pts',(0.374532872533722,-0.178617769573987,
-0.602903346722335));
#49467=CARTESIAN_POINT('Ctrl Pts',(0.28769685121945,-0.29901455150236,-0.609525739036715));
#49468=CARTESIAN_POINT('Ctrl Pts',(0.170159378914752,-0.355304575999081,
-0.616148131351095));
#49469=CARTESIAN_POINT('Ctrl Pts',(0.05262190661006,-0.4115946004958,-0.622770523665475));
#49470=CARTESIAN_POINT('Ctrl Pts',(-0.0956170166850531,-0.403777867560876,
-0.629392915979855));
#49471=CARTESIAN_POINT('Ctrl Pts',(-0.206582713566911,-0.33543872527383,
-0.636015308294236));
#49472=CARTESIAN_POINT('Ctrl Pts',(-0.317548410448779,-0.267099582986778,
-0.642637700608617));
#49473=CARTESIAN_POINT('Ctrl Pts',(-0.391240880917382,-0.138238031347586,
-0.649260092922997));
#49474=CARTESIAN_POINT('Ctrl Pts',(-0.393868582260403,-0.00794329070636282,
-0.655882485237378));
#49475=CARTESIAN_POINT('Ctrl Pts',(-0.393921641404054,-0.00531234964485795,
-0.656016206090419));
#49476=CARTESIAN_POINT('Ctrl Pts',(-0.393945725589634,-0.00268082423485301,
-0.65614992694346));
#49477=CARTESIAN_POINT('Ctrl Pts',(-0.393941093179356,-4.92117729247177E-5,
-0.656283647796501));
#49478=CARTESIAN_POINT('Ctrl Pts',(-0.393947723570607,-1.70646636204014E-5,
-0.674616352203497));
#49479=CARTESIAN_POINT('Ctrl Pts',(-0.393948297624998,-0.000926490307316668,
-0.674570139201534));
#49480=CARTESIAN_POINT('Ctrl Pts',(-0.393945421382037,-0.00183591221393385,
-0.674523926199571));
#49481=CARTESIAN_POINT('Ctrl Pts',(-0.393939083907698,-0.00274530999968196,
-0.674477713197608));
#49482=CARTESIAN_POINT('Ctrl Pts',(-0.393030914354389,-0.133063373125564,
-0.667855320883227));
#49483=CARTESIAN_POINT('Ctrl Pts',(-0.321045255232549,-0.262886106514305,
-0.661232928568847));
#49484=CARTESIAN_POINT('Ctrl Pts',(-0.210990994142462,-0.332683541744497,
-0.654610536254467));
#49485=CARTESIAN_POINT('Ctrl Pts',(-0.100936733052379,-0.402480976974688,
-0.647988143940086));
#49486=CARTESIAN_POINT('Ctrl Pts',(0.0471861300059487,-0.412253114046332,
-0.641365751625706));
#49487=CARTESIAN_POINT('Ctrl Pts',(0.165456136825064,-0.357518958020196,
-0.634743359311326));
#49488=CARTESIAN_POINT('Ctrl Pts',(0.283726143644182,-0.302784801994057,
-0.628120966996945));
#49489=CARTESIAN_POINT('Ctrl Pts',(0.372143294224086,-0.183544352870135,
-0.621498574682565));
#49490=CARTESIAN_POINT('Ctrl Pts',(0.390164071687642,-0.0544750926708616,
-0.614876182368184));
#49491=CARTESIAN_POINT('Ctrl Pts',(0.408184849151198,0.0745941675284096,
-0.608253790053804));
#49492=CARTESIAN_POINT('Ctrl Pts',(0.355809253498406,0.213492238803036,
-0.601631397739424));
#49493=CARTESIAN_POINT('Ctrl Pts',(0.257054014883852,0.298527673739638,
-0.595009005425043));
#49494=CARTESIAN_POINT('Ctrl Pts',(0.1582987762693,0.383563108676239,-0.588386613110663));
#49495=CARTESIAN_POINT('Ctrl Pts',(0.0131638946929933,0.414735907274821,
-0.581764220796283));
#49496=CARTESIAN_POINT('Ctrl Pts',(-0.111799304890707,0.377751841799355,
-0.575141828481902));
#49497=CARTESIAN_POINT('Ctrl Pts',(-0.236762504474413,0.340767776323887,
-0.568519436167522));
#49498=CARTESIAN_POINT('Ctrl Pts',(-0.341554022065504,0.235626846774361,
-0.561897043853141));
#49499=CARTESIAN_POINT('Ctrl Pts',(-0.378121905807111,0.110541227188991,
-0.555274651538761));
#49500=CARTESIAN_POINT('Ctrl Pts',(-0.388536673484437,0.0749160409747374,
-0.553388551760339));
#49501=CARTESIAN_POINT('Ctrl Pts',(-0.39341750218428,0.0376730473914621,
-0.551502451981918));
#49502=CARTESIAN_POINT('Ctrl Pts',(-0.393099733010831,0.000348606307955763,
-0.549616352203497));
#49503=CARTESIAN_POINT('Origin',(0.,0.,-2.22));
#49504=CARTESIAN_POINT('',(-0.392695136859145,-0.000134165267275832,-0.406283647796501));
#49505=CARTESIAN_POINT('',(-0.392714565881386,-0.000160383691160823,-0.424616352203497));
#49506=CARTESIAN_POINT('',(-0.3933,-4.81653586104654E-17,-2.22));
#49507=CARTESIAN_POINT('Ctrl Pts',(-0.392695136859145,-0.000134165267275832,
-0.406283647796501));
#49508=CARTESIAN_POINT('Ctrl Pts',(-0.39246894279338,0.0738890083694187,
-0.410014552504228));
#49509=CARTESIAN_POINT('Ctrl Pts',(-0.37239005838269,0.148026006512791,
-0.413745457211955));
#49510=CARTESIAN_POINT('Ctrl Pts',(-0.333228315284828,0.210129594475008,
-0.417476361919683));
#49511=CARTESIAN_POINT('Ctrl Pts',(-0.263715838600052,0.320364069980268,
-0.424098754234063));
#49512=CARTESIAN_POINT('Ctrl Pts',(-0.134079768270662,0.392685365088865,
-0.430721146548443));
#49513=CARTESIAN_POINT('Ctrl Pts',(-0.00376448297534652,0.393930685299415,
-0.437343538862824));
#49514=CARTESIAN_POINT('Ctrl Pts',(0.126550802319978,0.395176005509965,
-0.443965931177205));
#49515=CARTESIAN_POINT('Ctrl Pts',(0.257545302581228,0.325345350822453,
-0.450588323491586));
#49516=CARTESIAN_POINT('Ctrl Pts',(0.329151740126991,0.216459436501167,
-0.457210715805967));
#49517=CARTESIAN_POINT('Ctrl Pts',(0.400758177672747,0.107573522179891,
-0.463833108120347));
#49518=CARTESIAN_POINT('Ctrl Pts',(0.412976552503033,-0.0403676517751508,
-0.470455500434727));
#49519=CARTESIAN_POINT('Ctrl Pts',(0.360204150830326,-0.159525940801276,
-0.477077892749107));
#49520=CARTESIAN_POINT('Ctrl Pts',(0.307431749157616,-0.278684229827407,
-0.483700285063487));
#49521=CARTESIAN_POINT('Ctrl Pts',(0.189668570981906,-0.369059633924617,
-0.490322677377868));
#49522=CARTESIAN_POINT('Ctrl Pts',(0.0609146991362926,-0.389210682541646,
-0.496945069692248));
#49523=CARTESIAN_POINT('Ctrl Pts',(-0.0678391727093149,-0.409361731158675,
-0.503567462006628));
#49524=CARTESIAN_POINT('Ctrl Pts',(-0.207583738224827,-0.359288424295527,
-0.510189854321009));
#49525=CARTESIAN_POINT('Ctrl Pts',(-0.29423939198198,-0.261951782064089,
-0.516812246635389));
#49526=CARTESIAN_POINT('Ctrl Pts',(-0.357360022154415,-0.191051039525867,
-0.521636047022427));
#49527=CARTESIAN_POINT('Ctrl Pts',(-0.392312869151574,-0.0950734336898258,
-0.526459847409464));
#49528=CARTESIAN_POINT('Ctrl Pts',(-0.393149297351444,0.000355296501015012,
-0.531283647796502));
#49529=CARTESIAN_POINT('Ctrl Pts',(-0.393099733010831,0.000348606307955763,
-0.549616352203497));
#49530=CARTESIAN_POINT('Ctrl Pts',(-0.392301764747654,-0.0933789227099603,
-0.544880059667538));
#49531=CARTESIAN_POINT('Ctrl Pts',(-0.358721910614404,-0.187620052264415,
-0.540143767131579));
#49532=CARTESIAN_POINT('Ctrl Pts',(-0.297670339742412,-0.258046327990718,
-0.535407474595619));
#49533=CARTESIAN_POINT('Ctrl Pts',(-0.212306640043985,-0.356517953963846,
-0.528785082281239));
#49534=CARTESIAN_POINT('Ctrl Pts',(-0.0732349907550094,-0.408430896288897,
-0.522162689966859));
#49535=CARTESIAN_POINT('Ctrl Pts',(0.0557735668882773,-0.389980573611445,
-0.515540297652478));
#49536=CARTESIAN_POINT('Ctrl Pts',(0.184782124531568,-0.371530250933992,
-0.508917905338098));
#49537=CARTESIAN_POINT('Ctrl Pts',(0.303727590529166,-0.282716663254033,
-0.502295513023718));
#49538=CARTESIAN_POINT('Ctrl Pts',(0.358067746721792,-0.16426511294754,
-0.495673120709337));
#49539=CARTESIAN_POINT('Ctrl Pts',(0.412407902914418,-0.0458135626410491,
-0.489050728394957));
#49540=CARTESIAN_POINT('Ctrl Pts',(0.402142749302071,0.102275950291979,
-0.482428336080576));
#49541=CARTESIAN_POINT('Ctrl Pts',(0.331979352798454,0.212097260317369,
-0.475805943766196));
#49542=CARTESIAN_POINT('Ctrl Pts',(0.261815956294839,0.321918570342758,
-0.469183551451815));
#49543=CARTESIAN_POINT('Ctrl Pts',(0.131754316899958,0.393471677460513,
-0.462561159137435));
#49544=CARTESIAN_POINT('Ctrl Pts',(0.00143395259859793,0.393946039901013,
-0.455938766823055));
#49545=CARTESIAN_POINT('Ctrl Pts',(-0.128886411702766,0.394420402341514,
-0.449316374508674));
#49546=CARTESIAN_POINT('Ctrl Pts',(-0.259465500910607,0.323816020104756,
-0.442693982194294));
#49547=CARTESIAN_POINT('Ctrl Pts',(-0.33042652043779,0.214508399029338,
-0.436071589879914));
#49548=CARTESIAN_POINT('Ctrl Pts',(-0.371342013704453,0.151482596075745,
-0.432253177321108));
#49549=CARTESIAN_POINT('Ctrl Pts',(-0.392437043766175,0.0755896183641849,
-0.428434764762302));
#49550=CARTESIAN_POINT('Ctrl Pts',(-0.392714565881386,-0.000160383691160823,
-0.424616352203497));
#49551=CARTESIAN_POINT('Origin',(0.,0.,-2.22));
#49552=CARTESIAN_POINT('',(-0.393642003299011,-0.000296307799958484,-0.281283647796501));
#49553=CARTESIAN_POINT('',(-0.393688345169262,-0.000277587037033014,-0.299616352203497));
#49554=CARTESIAN_POINT('',(-0.3933,-4.81653586104654E-17,-2.22));
#49555=CARTESIAN_POINT('Ctrl Pts',(-0.393642003299011,-0.000296307799958484,
-0.281283647796501));
#49556=CARTESIAN_POINT('Ctrl Pts',(-0.392705570089931,0.111378501625261,
-0.286946865284613));
#49557=CARTESIAN_POINT('Ctrl Pts',(-0.342835655720549,0.223784343425498,
-0.292610082772724));
#49558=CARTESIAN_POINT('Ctrl Pts',(-0.258815660133244,0.297001729802868,
-0.298273300260836));
#49559=CARTESIAN_POINT('Ctrl Pts',(-0.160565261980655,0.382619889063466,
-0.304895692575216));
#49560=CARTESIAN_POINT('Ctrl Pts',(-0.0156172090648659,0.414650797671215,
-0.311518084889597));
#49561=CARTESIAN_POINT('Ctrl Pts',(0.109562634218419,0.378406661592715,
-0.318140477203977));
#49562=CARTESIAN_POINT('Ctrl Pts',(0.234742477501703,0.342162525514216,
-0.324762869518358));
#49563=CARTESIAN_POINT('Ctrl Pts',(0.340154111152485,0.237643344749466,
-0.331385261832738));
#49564=CARTESIAN_POINT('Ctrl Pts',(0.37746133962886,0.112776234214326,-0.338007654147118));
#49565=CARTESIAN_POINT('Ctrl Pts',(0.414768568105235,-0.0120908763208124,
-0.344630046461499));
#49566=CARTESIAN_POINT('Ctrl Pts',(0.383971391407208,-0.157305916626339,
-0.351252438775879));
#49567=CARTESIAN_POINT('Ctrl Pts',(0.299191739449069,-0.256280827360889,
-0.357874831090259));
#49568=CARTESIAN_POINT('Ctrl Pts',(0.214412087490928,-0.35525573809544,
-0.36449722340464));
#49569=CARTESIAN_POINT('Ctrl Pts',(0.0756499602726728,-0.407990519259011,
-0.37111961571902));
#49570=CARTESIAN_POINT('Ctrl Pts',(-0.0534655018538449,-0.390303725242715,
-0.377742008033401));
#49571=CARTESIAN_POINT('Ctrl Pts',(-0.182580963980366,-0.37261693122642,
-0.384364400347781));
#49572=CARTESIAN_POINT('Ctrl Pts',(-0.302049761015151,-0.284508562030254,
-0.390986792662162));
#49573=CARTESIAN_POINT('Ctrl Pts',(-0.357089718012459,-0.166380549481205,
-0.397609184976543));
#49574=CARTESIAN_POINT('Ctrl Pts',(-0.381121419242666,-0.114803163535286,
-0.400500672583195));
#49575=CARTESIAN_POINT('Ctrl Pts',(-0.392870439470467,-0.0575028481854697,
-0.403392160189848));
#49576=CARTESIAN_POINT('Ctrl Pts',(-0.392695136859145,-0.000134165267275832,
-0.406283647796501));
#49577=CARTESIAN_POINT('Ctrl Pts',(-0.392714565881386,-0.000160383691160823,
-0.424616352203497));
#49578=CARTESIAN_POINT('Ctrl Pts',(-0.392918359049566,-0.0557859791387052,
-0.421812372447922));
#49579=CARTESIAN_POINT('Ctrl Pts',(-0.381896468881979,-0.111334476047582,
-0.419008392692347));
#49580=CARTESIAN_POINT('Ctrl Pts',(-0.359254083037642,-0.161654081597039,
-0.416204412936772));
#49581=CARTESIAN_POINT('Ctrl Pts',(-0.305777676263785,-0.28049808123393,
-0.409582020622392));
#49582=CARTESIAN_POINT('Ctrl Pts',(-0.187481912869543,-0.370175220593635,
-0.402959628308012));
#49583=CARTESIAN_POINT('Ctrl Pts',(-0.0586110886880626,-0.389564216829724,
-0.396337235993631));
#49584=CARTESIAN_POINT('Ctrl Pts',(0.0702597354934178,-0.408953213065813,
-0.389714843679251));
#49585=CARTESIAN_POINT('Ctrl Pts',(0.209705620462139,-0.358054066178287,
-0.38309245136487));
#49586=CARTESIAN_POINT('Ctrl Pts',(0.29578391539786,-0.260206484498071,
-0.376470059050489));
#49587=CARTESIAN_POINT('Ctrl Pts',(0.381862210333579,-0.162358902817856,
-0.369847666736109));
#49588=CARTESIAN_POINT('Ctrl Pts',(0.414572915236302,-0.0175628863449562,
-0.363225274421729));
#49589=CARTESIAN_POINT('Ctrl Pts',(0.378916606915431,0.1077856277556,-0.356602882107349));
#49590=CARTESIAN_POINT('Ctrl Pts',(0.34326029859456,0.233134141856158,-0.349980489792969));
#49591=CARTESIAN_POINT('Ctrl Pts',(0.23923697705009,0.33903515358437,-0.343358097478588));
#49592=CARTESIAN_POINT('Ctrl Pts',(0.114546322886326,0.376927951129987,
-0.336735705164207));
#49593=CARTESIAN_POINT('Ctrl Pts',(-0.0101443312774386,0.414820748675605,
-0.330113312849827));
#49594=CARTESIAN_POINT('Ctrl Pts',(-0.155502318060499,0.384705332038629,
-0.323490920535446));
#49595=CARTESIAN_POINT('Ctrl Pts',(-0.254873976640853,0.300391075219788,
-0.316868528221066));
#49596=CARTESIAN_POINT('Ctrl Pts',(-0.341165921887652,0.227174613535666,
-0.311117802881876));
#49597=CARTESIAN_POINT('Ctrl Pts',(-0.392780654944496,0.11308807687727,
-0.305367077542686));
#49598=CARTESIAN_POINT('Ctrl Pts',(-0.393688345169262,-0.000277587037033014,
-0.299616352203497));
#49599=CARTESIAN_POINT('Origin',(0.,0.,-2.22));
#49600=CARTESIAN_POINT('',(-0.393631981127146,0.00030016282702406,-0.156283647796501));
#49601=CARTESIAN_POINT('',(-0.393585661406795,0.000315388445219644,-0.174616352203498));
#49602=CARTESIAN_POINT('',(-0.3933,-4.81653586104654E-17,-2.22));
#49603=CARTESIAN_POINT('Ctrl Pts',(-0.393631981127146,0.00030016282702406,
-0.156283647796501));
#49604=CARTESIAN_POINT('Ctrl Pts',(-0.393792621966079,0.0194912539892937,
-0.157256785750617));
#49605=CARTESIAN_POINT('Ctrl Pts',(-0.392509708971423,0.0386605451791385,
-0.158229923704732));
#49606=CARTESIAN_POINT('Ctrl Pts',(-0.389708810446672,0.0576052757599894,
-0.159203061658848));
#49607=CARTESIAN_POINT('Ctrl Pts',(-0.370648153337135,0.186527837731874,
-0.165825453973228));
#49608=CARTESIAN_POINT('Ctrl Pts',(-0.281288581648335,0.305050849275526,
-0.172447846287608));
#49609=CARTESIAN_POINT('Ctrl Pts',(-0.16258600572988,0.358833504095236,
-0.179070238601988));
#49610=CARTESIAN_POINT('Ctrl Pts',(-0.0438834298114263,0.412616158914947,
-0.185692630916368));
#49611=CARTESIAN_POINT('Ctrl Pts',(0.104162150336679,0.401658457010715,
-0.192315023230749));
#49612=CARTESIAN_POINT('Ctrl Pts',(0.213654399121235,0.330981012427604,
-0.198937415545129));
#49613=CARTESIAN_POINT('Ctrl Pts',(0.323146647905798,0.26030356784449,-0.20555980785951));
#49614=CARTESIAN_POINT('Ctrl Pts',(0.394085565326806,0.129906380582479,
-0.212182200173891));
#49615=CARTESIAN_POINT('Ctrl Pts',(0.393947632619649,-0.000415066957393126,
-0.218804592488271));
#49616=CARTESIAN_POINT('Ctrl Pts',(0.393809699912491,-0.130736514497255,
-0.225426984802652));
#49617=CARTESIAN_POINT('Ctrl Pts',(0.322594917077188,-0.260982222314982,
-0.232049377117032));
#49618=CARTESIAN_POINT('Ctrl Pts',(0.212955874119221,-0.331429364260128,
-0.238671769431412));
#49619=CARTESIAN_POINT('Ctrl Pts',(0.103316831161247,-0.401876506205278,
-0.245294161745793));
#49620=CARTESIAN_POINT('Ctrl Pts',(-0.0447464719193912,-0.412525082277837,
-0.251916554060173));
#49621=CARTESIAN_POINT('Ctrl Pts',(-0.163338418470475,-0.358491635469819,
-0.258538946374553));
#49622=CARTESIAN_POINT('Ctrl Pts',(-0.281930365021556,-0.304458188661802,
-0.265161338688934));
#49623=CARTESIAN_POINT('Ctrl Pts',(-0.371050955043081,-0.185742718973213,
-0.271783731003314));
#49624=CARTESIAN_POINT('Ctrl Pts',(-0.389834878359152,-0.0567822791721963,
-0.278406123317694));
#49625=CARTESIAN_POINT('Ctrl Pts',(-0.392555506423457,-0.0381038920320804,
-0.279365298143963));
#49626=CARTESIAN_POINT('Ctrl Pts',(-0.393800606277357,-0.0192105850909033,
-0.280324472970232));
#49627=CARTESIAN_POINT('Ctrl Pts',(-0.393642003299011,-0.000296307799958484,
-0.281283647796501));
#49628=CARTESIAN_POINT('Ctrl Pts',(-0.393688345169262,-0.000277587037033014,
-0.299616352203497));
#49629=CARTESIAN_POINT('Ctrl Pts',(-0.393825928438496,-0.017461002958714,
-0.298744685228306));
#49630=CARTESIAN_POINT('Ctrl Pts',(-0.392798516291064,-0.0346278568133537,
-0.297873018253116));
#49631=CARTESIAN_POINT('Ctrl Pts',(-0.390550285770528,-0.0516333105353148,
-0.297001351277925));
#49632=CARTESIAN_POINT('Ctrl Pts',(-0.373469605942206,-0.18083034247088,
-0.290378958963545));
#49633=CARTESIAN_POINT('Ctrl Pts',(-0.285922915907914,-0.300711309341301,
-0.283756566649164));
#49634=CARTESIAN_POINT('Ctrl Pts',(-0.168054469471746,-0.35630499614788,
-0.277134174334784));
#49635=CARTESIAN_POINT('Ctrl Pts',(-0.0501860230355798,-0.411898682954459,
-0.270511782020403));
#49636=CARTESIAN_POINT('Ctrl Pts',(0.0980041798024627,-0.403205089697194,
-0.263889389706022));
#49637=CARTESIAN_POINT('Ctrl Pts',(0.208563582086416,-0.334210694524994,
-0.257266997391642));
#49638=CARTESIAN_POINT('Ctrl Pts',(0.319122984370366,-0.265216299352795,
-0.250644605077262));
#49639=CARTESIAN_POINT('Ctrl Pts',(0.392051586100232,-0.135921102265661,
-0.244022212762882));
#49640=CARTESIAN_POINT('Ctrl Pts',(0.39390853670177,-0.00561308011220472,
-0.237399820448502));
#49641=CARTESIAN_POINT('Ctrl Pts',(0.395765487303308,0.124694942041256,
-0.230777428134121));
#49642=CARTESIAN_POINT('Ctrl Pts',(0.326550786776514,0.256015789261044,
-0.22415503581974));
#49643=CARTESIAN_POINT('Ctrl Pts',(0.218001897880293,0.328132362043281,
-0.21753264350536));
#49644=CARTESIAN_POINT('Ctrl Pts',(0.109453008984069,0.400248934825521,
-0.210910251190979));
#49645=CARTESIAN_POINT('Ctrl Pts',(-0.0384300682815738,0.413161233170207,
-0.204287858876599));
#49646=CARTESIAN_POINT('Ctrl Pts',(-0.157834284113371,0.360948679891727,
-0.197665466562219));
#49647=CARTESIAN_POINT('Ctrl Pts',(-0.277238499945161,0.308736126613249,
-0.191043074247839));
#49648=CARTESIAN_POINT('Ctrl Pts',(-0.368163854343102,0.191398721711606,
-0.184420681933458));
#49649=CARTESIAN_POINT('Ctrl Pts',(-0.38891965580233,0.0627406728828643,
-0.177798289619078));
#49650=CARTESIAN_POINT('Ctrl Pts',(-0.392243915783628,0.0421347327155593,
-0.176737643813884));
#49651=CARTESIAN_POINT('Ctrl Pts',(-0.39376822901556,0.0212384022666582,
-0.175676998008691));
#49652=CARTESIAN_POINT('Ctrl Pts',(-0.393585661406795,0.000315388445219644,
-0.174616352203498));
#49653=CARTESIAN_POINT('Origin',(0.,0.,-2.22));
#49654=CARTESIAN_POINT('',(-0.3933,-4.81653586104654E-17,-0.04));
#49655=CARTESIAN_POINT('',(-0.39272888104496,9.19390291685468E-5,-0.0496163522034977));
#49656=CARTESIAN_POINT('',(-0.3933,-4.81653586104654E-17,-2.22));
#49657=CARTESIAN_POINT('',(-0.356151197810523,0.166856867698425,-0.04));
#49658=CARTESIAN_POINT('Origin',(0.,0.,-0.04));
#49659=CARTESIAN_POINT('Ctrl Pts',(-0.356151197810523,0.166856867698425,
-0.04));
#49660=CARTESIAN_POINT('Ctrl Pts',(-0.300608260002572,0.285411675199488,
-0.0466223923143805));
#49661=CARTESIAN_POINT('Ctrl Pts',(-0.181688079154573,0.373019047260479,
-0.0532447846287612));
#49662=CARTESIAN_POINT('Ctrl Pts',(-0.0527476824217043,0.390367240993339,
-0.0598671769431416));
#49663=CARTESIAN_POINT('Ctrl Pts',(0.0761927143111604,0.407715434726198,
-0.0664895692575218));
#49664=CARTESIAN_POINT('Ctrl Pts',(0.215153326928898,0.35480445013093,-0.0731119615719019));
#49665=CARTESIAN_POINT('Ctrl Pts',(0.2998027398245,0.25567960187594,-0.0797343538862821));
#49666=CARTESIAN_POINT('Ctrl Pts',(0.384452152720104,0.156554753620946,
-0.0863567462006626));
#49667=CARTESIAN_POINT('Ctrl Pts',(0.414790365893573,0.0112160417062353,
-0.0929791385150429));
#49668=CARTESIAN_POINT('Ctrl Pts',(0.377183219450442,-0.113586432810944,
-0.0996015308294233));
#49669=CARTESIAN_POINT('Ctrl Pts',(0.33957607300731,-0.238388907328124,
-0.106223923143804));
#49670=CARTESIAN_POINT('Ctrl Pts',(0.234023566947572,-0.342655144447766,
-0.112846315458184));
#49671=CARTESIAN_POINT('Ctrl Pts',(0.108786645000273,-0.378628284581708,
-0.119468707772564));
#49672=CARTESIAN_POINT('Ctrl Pts',(-0.0164502769470251,-0.41460142471565,
-0.126091100086945));
#49673=CARTESIAN_POINT('Ctrl Pts',(-0.161371614781888,-0.382281467863894,
-0.132713492401325));
#49674=CARTESIAN_POINT('Ctrl Pts',(-0.259451412434183,-0.296460433237957,
-0.139335884715706));
#49675=CARTESIAN_POINT('Ctrl Pts',(-0.34311871848278,-0.223250506817523,
-0.144985139075971));
#49676=CARTESIAN_POINT('Ctrl Pts',(-0.39269942993444,-0.11110783946927,
-0.150634393436236));
#49677=CARTESIAN_POINT('Ctrl Pts',(-0.393631981127146,0.00030016282702406,
-0.156283647796501));
#49678=CARTESIAN_POINT('Ctrl Pts',(-0.393585661406795,0.000315388445219644,
-0.174616352203498));
#49679=CARTESIAN_POINT('Ctrl Pts',(-0.39262832507852,-0.109399370726316,
-0.169054605694311));
#49680=CARTESIAN_POINT('Ctrl Pts',(-0.34473728496773,-0.219847836359808,
-0.163492859185123));
#49681=CARTESIAN_POINT('Ctrl Pts',(-0.263331321875656,-0.293007221603574,
-0.157931112675936));
#49682=CARTESIAN_POINT('Ctrl Pts',(-0.166400937969243,-0.380118374505416,
-0.151308720361556));
#49683=CARTESIAN_POINT('Ctrl Pts',(-0.0219539216358963,-0.414361987553257,
-0.144686328047175));
#49684=CARTESIAN_POINT('Ctrl Pts',(0.103762983130385,-0.380038051262661,
-0.138063935732795));
#49685=CARTESIAN_POINT('Ctrl Pts',(0.22947988789667,-0.345714114972064,
-0.131441543418414));
#49686=CARTESIAN_POINT('Ctrl Pts',(0.336466681095895,-0.242822629343032,
-0.124819151104034));
#49687=CARTESIAN_POINT('Ctrl Pts',(0.375685521011522,-0.118539821363215,
-0.118196758789653));
#49688=CARTESIAN_POINT('Ctrl Pts',(0.414904360927149,0.0057429866165986,
-0.111574366475273));
#49689=CARTESIAN_POINT('Ctrl Pts',(0.386355247559182,0.151417116947191,
-0.104951974160893));
#49690=CARTESIAN_POINT('Ctrl Pts',(0.303089588085626,0.251675418462943,
-0.0983295818465127));
#49691=CARTESIAN_POINT('Ctrl Pts',(0.219823928612068,0.351933719978697,
-0.0917071895321323));
#49692=CARTESIAN_POINT('Ctrl Pts',(0.081841723032909,0.406776192679608,
-0.0850847972177514));
#49693=CARTESIAN_POINT('Ctrl Pts',(-0.0475093665302487,0.391071300758949,
-0.0784624049033708));
#49694=CARTESIAN_POINT('Ctrl Pts',(-0.176860456093399,0.37536640883829,
-0.0718400125889905));
#49695=CARTESIAN_POINT('Ctrl Pts',(-0.297580429640553,0.289114152296078,
-0.0652176202746104));
#49696=CARTESIAN_POINT('Ctrl Pts',(-0.354460273107469,0.171833994016063,
-0.0585952279602302));
#49697=CARTESIAN_POINT('Ctrl Pts',(-0.380166846769823,0.118829786476159,
-0.0556022693746527));
#49698=CARTESIAN_POINT('Ctrl Pts',(-0.392833787442048,0.0594879907984162,
-0.0526093107890752));
#49699=CARTESIAN_POINT('Ctrl Pts',(-0.39272888104496,9.19390291685468E-5,
-0.0496163522034977));
#49700=CARTESIAN_POINT('Origin',(0.,0.,-3.17777734492731));
#49701=CARTESIAN_POINT('',(-0.322547029539158,0.000245957221170181,-0.115277344927309));
#49702=CARTESIAN_POINT('',(-0.321807017896681,7.53360046316098E-5,-0.0906226550726903));
#49703=CARTESIAN_POINT('',(-0.322275,-1.53308031181269E-15,-3.17777734492731));
#49704=CARTESIAN_POINT('',(0.258431022718474,0.193451597832761,-0.0400000000000002));
#49705=CARTESIAN_POINT('Ctrl Pts',(-0.322547029539158,0.000245957221170202,
-0.115277344927309));
#49706=CARTESIAN_POINT('Ctrl Pts',(-0.321782885283814,-0.0910431705185724,
-0.109628090567044));
#49707=CARTESIAN_POINT('Ctrl Pts',(-0.233530360647496,-0.290654535970315,
-0.0973564438923979));
#49708=CARTESIAN_POINT('Ctrl Pts',(0.105270814003626,-0.366213039015092,
-0.0784624049033714));
#49709=CARTESIAN_POINT('Ctrl Pts',(0.359206608534133,-0.115371720754992,
-0.0590192109545344));
#49710=CARTESIAN_POINT('Ctrl Pts',(0.317979897957302,0.113102706613816,
-0.046198409320077));
#49711=CARTESIAN_POINT('Ctrl Pts',(0.258434353604258,0.193455249693963,
-0.0400000000000002));
#49712=CARTESIAN_POINT('',(0.266526038810872,-0.181176836987473,-0.04));
#49713=CARTESIAN_POINT('Origin',(0.,0.,-0.04));
#49714=CARTESIAN_POINT('Ctrl Pts',(-0.321807017896681,7.53360046315855E-5,
-0.0906226550726902));
#49715=CARTESIAN_POINT('Ctrl Pts',(-0.3217027758797,-0.0589445560984634,
-0.0869932213438877));
#49716=CARTESIAN_POINT('Ctrl Pts',(-0.277937787262726,-0.225838884443167,
-0.0767413953007049));
#49717=CARTESIAN_POINT('Ctrl Pts',(-0.00893422490495668,-0.380826657875824,
-0.0598671769431404));
#49718=CARTESIAN_POINT('Ctrl Pts',(0.206216301921741,-0.269897423691928,
-0.0466223923143805));
#49719=CARTESIAN_POINT('Ctrl Pts',(0.266526038810872,-0.181176836987473,
-0.04));
#49720=CARTESIAN_POINT('Origin',(0.,0.,-3.17777734492731));
#49721=CARTESIAN_POINT('',(-0.322555241833687,-0.000242798363153271,-0.240277344927309));
#49722=CARTESIAN_POINT('',(-0.322509074573798,0.000258433285462066,-0.21562265507269));
#49723=CARTESIAN_POINT('',(-0.322275,-1.53308031181269E-15,-3.17777734492731));
#49724=CARTESIAN_POINT('Ctrl Pts',(-0.322555241833687,-0.000242798363153243,
-0.240277344927309));
#49725=CARTESIAN_POINT('Ctrl Pts',(-0.322685203122389,-0.0157413966696349,
-0.23931817010104));
#49726=CARTESIAN_POINT('Ctrl Pts',(-0.314620877302866,-0.138110524338227,
-0.23173660296039));
#49727=CARTESIAN_POINT('Ctrl Pts',(-0.157990771009751,-0.346753853915265,
-0.21753264350536));
#49728=CARTESIAN_POINT('Ctrl Pts',(0.205984064995685,-0.320577119714015,
-0.197665466562219));
#49729=CARTESIAN_POINT('Ctrl Pts',(0.381046949345406,-0.000402173207826333,
-0.177798289619077));
#49730=CARTESIAN_POINT('Ctrl Pts',(0.206662207836228,0.320145145822377,
-0.157931112675937));
#49731=CARTESIAN_POINT('Ctrl Pts',(-0.157269060983239,0.347081784885588,
-0.138063935732795));
#49732=CARTESIAN_POINT('Ctrl Pts',(-0.314473566646606,0.138571928724442,
-0.12384601314992));
#49733=CARTESIAN_POINT('Ctrl Pts',(-0.322678660676628,0.0159713803188515,
-0.116250482881424));
#49734=CARTESIAN_POINT('Ctrl Pts',(-0.322547029539158,0.000245957221170202,
-0.115277344927309));
#49735=CARTESIAN_POINT('Ctrl Pts',(-0.322509074573798,0.000258433285462089,
-0.21562265507269));
#49736=CARTESIAN_POINT('Ctrl Pts',(-0.321724621064523,-0.08964322959784,
-0.210060908563503));
#49737=CARTESIAN_POINT('Ctrl Pts',(-0.235755875896869,-0.287908207227001,
-0.197876769739936));
#49738=CARTESIAN_POINT('Ctrl Pts',(0.100372392813672,-0.367593109417031,
-0.179070238601988));
#49739=CARTESIAN_POINT('Ctrl Pts',(0.363371391885224,-0.114661350979993,
-0.159203061658847));
#49740=CARTESIAN_POINT('Ctrl Pts',(0.29319087692976,0.243440329815534,-0.139335884715706));
#49741=CARTESIAN_POINT('Ctrl Pts',(-0.0460022222542214,0.378256179469882,
-0.119468707772565));
#49742=CARTESIAN_POINT('Ctrl Pts',(-0.28854735638966,0.204962030061018,
-0.103230964558226));
#49743=CARTESIAN_POINT('Ctrl Pts',(-0.32189297952679,0.0487452129025094,
-0.093615613658268));
#49744=CARTESIAN_POINT('Ctrl Pts',(-0.321807017896681,7.53360046315855E-5,
-0.0906226550726902));
#49745=CARTESIAN_POINT('Origin',(0.,0.,-3.17777734492731));
#49746=CARTESIAN_POINT('',(-0.321779367483552,-0.000109936718809572,-0.365277344927308));
#49747=CARTESIAN_POINT('',(-0.322593214948955,-0.000227458332986402,-0.340622655072689));
#49748=CARTESIAN_POINT('',(-0.322275,-1.53308031181269E-15,-3.17777734492731));
#49749=CARTESIAN_POINT('Ctrl Pts',(-0.321779367483552,-0.000109936718809583,
-0.365277344927308));
#49750=CARTESIAN_POINT('Ctrl Pts',(-0.321923012662968,-0.0471185619094107,
-0.362385857320655));
#49751=CARTESIAN_POINT('Ctrl Pts',(-0.290246260065477,-0.201607010980205,
-0.352871977399622));
#49752=CARTESIAN_POINT('Ctrl Pts',(-0.0517149087271477,-0.377524144911485,
-0.336735705164208));
#49753=CARTESIAN_POINT('Ctrl Pts',(0.289395423456396,-0.247889502657562,
-0.316868528221066));
#49754=CARTESIAN_POINT('Ctrl Pts',(0.365102213085359,0.109083625599228,
-0.297001351277925));
#49755=CARTESIAN_POINT('Ctrl Pts',(0.105975331050231,0.366016646048953,
-0.277134174334784));
#49756=CARTESIAN_POINT('Ctrl Pts',(-0.233138726856483,0.291078548034463,
-0.258226172217912));
#49757=CARTESIAN_POINT('Ctrl Pts',(-0.321787916604962,0.0912649545163569,
-0.24594056241542));
#49758=CARTESIAN_POINT('Ctrl Pts',(-0.322555241833687,-0.000242798363153243,
-0.240277344927309));
#49759=CARTESIAN_POINT('Ctrl Pts',(-0.322593214948955,-0.000227458332986343,
-0.340622655072689));
#49760=CARTESIAN_POINT('Ctrl Pts',(-0.322705952421856,-0.0143077669171678,
-0.339750988097499));
#49761=CARTESIAN_POINT('Ctrl Pts',(-0.315468030408353,-0.135244967949515,
-0.332256928807928));
#49762=CARTESIAN_POINT('Ctrl Pts',(-0.162551991338471,-0.344638636705144,
-0.318140477203977));
#49763=CARTESIAN_POINT('Ctrl Pts',(0.201734794471057,-0.323267715522956,
-0.298273300260835));
#49764=CARTESIAN_POINT('Ctrl Pts',(0.381010653528974,-0.00542935060109167,
-0.278406123317695));
#49765=CARTESIAN_POINT('Ctrl Pts',(0.210864447485707,0.317388544423747,
-0.258538946374552));
#49766=CARTESIAN_POINT('Ctrl Pts',(-0.152667350575211,0.34913004670471,
-0.238671769431413));
#49767=CARTESIAN_POINT('Ctrl Pts',(-0.313610945544451,0.141435461467442,
-0.224366338997457));
#49768=CARTESIAN_POINT('Ctrl Pts',(-0.322658672784109,0.0174030157398424,
-0.216683300877883));
#49769=CARTESIAN_POINT('Ctrl Pts',(-0.322509074573798,0.000258433285462089,
-0.21562265507269));
#49770=CARTESIAN_POINT('Origin',(0.,0.,-3.17777734492731));
#49771=CARTESIAN_POINT('',(-0.322151512341563,0.00029113445171856,-0.490277344927309));
#49772=CARTESIAN_POINT('',(-0.321795287870388,-0.000131420427339407,-0.465622655072689));
#49773=CARTESIAN_POINT('',(-0.322275,-1.53308031181269E-15,-3.17777734492731));
#49774=CARTESIAN_POINT('Ctrl Pts',(-0.322151512341563,0.000291134451718522,
-0.490277344927308));
#49775=CARTESIAN_POINT('Ctrl Pts',(-0.321466132483658,-0.0779043753938241,
-0.485453544540271));
#49776=CARTESIAN_POINT('Ctrl Pts',(-0.253505572034916,-0.264518412404189,
-0.474007351838853));
#49777=CARTESIAN_POINT('Ctrl Pts',(0.0589201893379548,-0.376466887562887,
-0.455938766823054));
#49778=CARTESIAN_POINT('Ctrl Pts',(0.348410107313365,-0.154302636186626,
-0.436071589879914));
#49779=CARTESIAN_POINT('Ctrl Pts',(0.318374434175064,0.20937197736306,-0.416204412936773));
#49780=CARTESIAN_POINT('Ctrl Pts',(-0.0036412223595689,0.38103234532199,
-0.396337235993631));
#49781=CARTESIAN_POINT('Ctrl Pts',(-0.27593708477359,0.229124088827818,
-0.379361546657143));
#49782=CARTESIAN_POINT('Ctrl Pts',(-0.321594021201972,0.0605455890471819,
-0.369008249635035));
#49783=CARTESIAN_POINT('Ctrl Pts',(-0.321779367483552,-0.000109936718809583,
-0.365277344927308));
#49784=CARTESIAN_POINT('Ctrl Pts',(-0.321795287870388,-0.000131420427339393,
-0.465622655072689));
#49785=CARTESIAN_POINT('Ctrl Pts',(-0.321962278572841,-0.0457117376733506,
-0.462818675317115));
#49786=CARTESIAN_POINT('Ctrl Pts',(-0.291600412951676,-0.198730500604296,
-0.453392303247159));
#49787=CARTESIAN_POINT('Ctrl Pts',(-0.0566920069213143,-0.376808846437738,
-0.437343538862825));
#49788=CARTESIAN_POINT('Ctrl Pts',(0.286099164537831,-0.251686630090085,
-0.417476361919683));
#49789=CARTESIAN_POINT('Ctrl Pts',(0.366509861887374,0.104256437864189,
-0.397609184976542));
#49790=CARTESIAN_POINT('Ctrl Pts',(0.110795781408782,0.364586327678901,
-0.3777420080334));
#49791=CARTESIAN_POINT('Ctrl Pts',(-0.230851227146932,0.293803550391354,
-0.35874649806545));
#49792=CARTESIAN_POINT('Ctrl Pts',(-0.321849442085529,0.0926658021246373,
-0.346373380411879));
#49793=CARTESIAN_POINT('Ctrl Pts',(-0.322593214948955,-0.000227458332986343,
-0.340622655072689));
#49794=CARTESIAN_POINT('Origin',(0.,0.,-3.17777734492731));
#49795=CARTESIAN_POINT('',(-0.322800319868744,-4.03247498678985E-5,-0.615277344927307));
#49796=CARTESIAN_POINT('',(-0.322110898693276,0.000285652422795588,-0.590622655072689));
#49797=CARTESIAN_POINT('',(-0.322275,-1.53308031181269E-15,-3.17777734492731));
#49798=CARTESIAN_POINT('Ctrl Pts',(-0.322800319868744,-4.03247498679347E-5,
-0.615277344927308));
#49799=CARTESIAN_POINT('Ctrl Pts',(-0.322804115724382,-0.00219670132288585,
-0.615143624074267));
#49800=CARTESIAN_POINT('Ctrl Pts',(-0.32180703019643,-0.111141880060886,
-0.608387510906845));
#49801=CARTESIAN_POINT('Ctrl Pts',(-0.199818644945625,-0.324455567408028,
-0.595009005425044));
#49802=CARTESIAN_POINT('Ctrl Pts',(0.164587907342214,-0.343670957237192,
-0.575141828481902));
#49803=CARTESIAN_POINT('Ctrl Pts',(0.378051513513506,-0.0477070144762039,
-0.555274651538762));
#49804=CARTESIAN_POINT('Ctrl Pts',(0.24480550918305,0.2920088504654,-0.535407474595619));
#49805=CARTESIAN_POINT('Ctrl Pts',(-0.112950699881881,0.363924505207545,
-0.515540297652479));
#49806=CARTESIAN_POINT('Ctrl Pts',(-0.30540724597967,0.165661329846195,
-0.500496921096375));
#49807=CARTESIAN_POINT('Ctrl Pts',(-0.322407061614062,0.0294469455297607,
-0.492075936854651));
#49808=CARTESIAN_POINT('Ctrl Pts',(-0.322151512341563,0.000291134451718522,
-0.490277344927308));
#49809=CARTESIAN_POINT('Ctrl Pts',(-0.322110898693276,0.000285652422795598,
-0.590622655072689));
#49810=CARTESIAN_POINT('Ctrl Pts',(-0.321457033394476,-0.0765158716408842,
-0.58588636253673));
#49811=CARTESIAN_POINT('Ctrl Pts',(-0.25546811539684,-0.261712333349606,
-0.574527677686391));
#49812=CARTESIAN_POINT('Ctrl Pts',(0.0539473916324327,-0.377211570275388,
-0.556546600521672));
#49813=CARTESIAN_POINT('Ctrl Pts',(0.346343654442317,-0.158886635343591,
-0.53667942357853));
#49814=CARTESIAN_POINT('Ctrl Pts',(0.321109463897549,0.205152630716595,
-0.516812246635389));
#49815=CARTESIAN_POINT('Ctrl Pts',(0.00138700138049073,0.381047196669113,
-0.496945069692247));
#49816=CARTESIAN_POINT('Ctrl Pts',(-0.274303504523829,0.231980772818264,
-0.479881872504682));
#49817=CARTESIAN_POINT('Ctrl Pts',(-0.321567882735176,0.0619390904101579,
-0.469441067631495));
#49818=CARTESIAN_POINT('Ctrl Pts',(-0.321795287870388,-0.000131420427339393,
-0.465622655072689));
#49819=CARTESIAN_POINT('Origin',(0.,0.,-3.17777734492731));
#49820=CARTESIAN_POINT('',(-0.322031575383028,-0.00026858467163699,-0.740277344927308));
#49821=CARTESIAN_POINT('',(-0.32280575289529,-1.39830014679876E-5,-0.715622655072688));
#49822=CARTESIAN_POINT('',(-0.322275,-1.53308031181269E-15,-3.17777734492731));
#49823=CARTESIAN_POINT('Ctrl Pts',(-0.322031575383028,-0.000268584671637075,
-0.740277344927308));
#49824=CARTESIAN_POINT('Ctrl Pts',(-0.322294991248528,-0.0337913139650879,
-0.738211311293882));
#49825=CARTESIAN_POINT('Ctrl Pts',(-0.302040555874669,-0.174456222783985,
-0.729522885346076));
#49826=CARTESIAN_POINT('Ctrl Pts',(-0.098186030593751,-0.368182576296315,
-0.714212067083892));
#49827=CARTESIAN_POINT('Ctrl Pts',(0.256379762883779,-0.281901265118838,
-0.694344890140749));
#49828=CARTESIAN_POINT('Ctrl Pts',(0.375820647341585,0.0629106280680267,
-0.674477713197609));
#49829=CARTESIAN_POINT('Ctrl Pts',(0.150597840249194,0.35002742264572,-0.654610536254467));
#49830=CARTESIAN_POINT('Ctrl Pts',(-0.210292157648995,0.316363512819851,
-0.634877080164367));
#49831=CARTESIAN_POINT('Ctrl Pts',(-0.322616129747388,0.104595704792612,
-0.621766016388647));
#49832=CARTESIAN_POINT('Ctrl Pts',(-0.322800319868744,-4.03247498679347E-5,
-0.615277344927308));
#49833=CARTESIAN_POINT('Ctrl Pts',(-0.32280575289529,-1.39830014679308E-5,
-0.715622655072688));
#49834=CARTESIAN_POINT('Ctrl Pts',(-0.322806223282726,-0.000759177889134405,
-0.715576442070726));
#49835=CARTESIAN_POINT('Ctrl Pts',(-0.322466129202107,-0.10829147308526,
-0.708907836754383));
#49836=CARTESIAN_POINT('Ctrl Pts',(-0.204082586668139,-0.321790595931231,
-0.695616839123661));
#49837=CARTESIAN_POINT('Ctrl Pts',(0.160038661936921,-0.345812834487786,
-0.675749662180518));
#49838=CARTESIAN_POINT('Ctrl Pts',(0.377389060130195,-0.0526914329514625,
-0.655882485237377));
#49839=CARTESIAN_POINT('Ctrl Pts',(0.248637381342986,0.288753082075454,
-0.636015308294237));
#49840=CARTESIAN_POINT('Ctrl Pts',(-0.108138697680715,0.365383239728838,
-0.616148131351095));
#49841=CARTESIAN_POINT('Ctrl Pts',(-0.304329303822686,0.168538464761997,
-0.601017246943913));
#49842=CARTESIAN_POINT('Ctrl Pts',(-0.322371282777625,0.0308697720520624,
-0.59250875485111));
#49843=CARTESIAN_POINT('Ctrl Pts',(-0.322110898693276,0.000285652422795598,
-0.590622655072689));
#49844=CARTESIAN_POINT('Origin',(0.,0.,-3.17777734492731));
#49845=CARTESIAN_POINT('',(-0.32183688899373,0.000172923102116511,-0.865277344927308));
#49846=CARTESIAN_POINT('',(-0.322069372535088,-0.000277835810467392,-0.840622655072689));
#49847=CARTESIAN_POINT('',(-0.322275,-1.53308031181269E-15,-3.17777734492731));
#49848=CARTESIAN_POINT('Ctrl Pts',(-0.32183688899373,0.000172923102116473,
-0.865277344927309));
#49849=CARTESIAN_POINT('Ctrl Pts',(-0.321521197468452,-0.0648015223631276,
-0.861278998513499));
#49850=CARTESIAN_POINT('Ctrl Pts',(-0.270857672103809,-0.237844790870895,
-0.850658259785309));
#49851=CARTESIAN_POINT('Ctrl Pts',(0.0117243233039672,-0.38086932973796,
-0.833415128742737));
#49852=CARTESIAN_POINT('Ctrl Pts',(0.326557088446483,-0.196365409574429,
-0.813547951799597));
#49853=CARTESIAN_POINT('Ctrl Pts',(0.341905585223924,0.168224483606484,
-0.793680774856455));
#49854=CARTESIAN_POINT('Ctrl Pts',(0.0436937654029756,0.378536340338528,
-0.773813597913315));
#49855=CARTESIAN_POINT('Ctrl Pts',(-0.259410588849515,0.255924509718627,
-0.756012454603599));
#49856=CARTESIAN_POINT('Ctrl Pts',(-0.321450647199645,0.0736612759823137,
-0.744833703608263));
#49857=CARTESIAN_POINT('Ctrl Pts',(-0.322031575383028,-0.000268584671637075,
-0.740277344927308));
#49858=CARTESIAN_POINT('Ctrl Pts',(-0.322069372535088,-0.000277835810467364,
-0.840622655072689));
#49859=CARTESIAN_POINT('Ctrl Pts',(-0.322332513972518,-0.032371167381551,
-0.838644129290342));
#49860=CARTESIAN_POINT('Ctrl Pts',(-0.303165873677557,-0.171577957634514,
-0.830043211193615));
#49861=CARTESIAN_POINT('Ctrl Pts',(-0.103035825860727,-0.366854887387893,
-0.814819900782507));
#49862=CARTESIAN_POINT('Ctrl Pts',(0.25263760185176,-0.285259762219933,
-0.794952723839366));
#49863=CARTESIAN_POINT('Ctrl Pts',(0.376618042246158,0.0579460099220519,
-0.775085546896225));
#49864=CARTESIAN_POINT('Ctrl Pts',(0.15520350324569,0.348009715944001,-0.755218369953084));
#49865=CARTESIAN_POINT('Ctrl Pts',(-0.207701459761879,0.318982707307465,
-0.735397406011905));
#49866=CARTESIAN_POINT('Ctrl Pts',(-0.322738816059344,0.106028364300782,
-0.722198834385106));
#49867=CARTESIAN_POINT('Ctrl Pts',(-0.32280575289529,-1.39830014679308E-5,
-0.715622655072688));
#49868=CARTESIAN_POINT('Origin',(0.,0.,-3.17777734492731));
#49869=CARTESIAN_POINT('',(-0.322664566790459,0.000190428865854771,-0.990277344927309));
#49870=CARTESIAN_POINT('',(-0.321815198935766,0.000153234844127104,-0.965622655072689));
#49871=CARTESIAN_POINT('',(-0.322275,-1.53308031181269E-15,-3.17777734492731));
#49872=CARTESIAN_POINT('Ctrl Pts',(-0.322664566790459,0.00019042886585479,
-0.990277344927309));
#49873=CARTESIAN_POINT('Ctrl Pts',(-0.321994453881888,-0.0955538967887449,
-0.984346685733115));
#49874=CARTESIAN_POINT('Ctrl Pts',(-0.226048562226605,-0.299375993968961,
-0.97179363422454));
#49875=CARTESIAN_POINT('Ctrl Pts',(0.12064623827576,-0.361446249505908,
-0.952618190401585));
#49876=CARTESIAN_POINT('Ctrl Pts',(0.369203465790718,-0.0942746357198006,
-0.932751013458444));
#49877=CARTESIAN_POINT('Ctrl Pts',(0.279165593881561,0.259355889242436,
-0.912883836515302));
#49878=CARTESIAN_POINT('Ctrl Pts',(-0.0668939863116134,0.375132110978679,
-0.893016659572163));
#49879=CARTESIAN_POINT('Ctrl Pts',(-0.294306079939019,0.192813503700519,
-0.87714782904283));
#49880=CARTESIAN_POINT('Ctrl Pts',(-0.322044071905618,0.0428145328125884,
-0.867901390827879));
#49881=CARTESIAN_POINT('Ctrl Pts',(-0.32183688899373,0.000172923102116473,
-0.865277344927309));
#49882=CARTESIAN_POINT('Ctrl Pts',(-0.321815198935766,0.000153234844127097,
-0.965622655072689));
#49883=CARTESIAN_POINT('Ctrl Pts',(-0.321542654537741,-0.0634098832967347,
-0.961711816509958));
#49884=CARTESIAN_POINT('Ctrl Pts',(-0.272548169464614,-0.23499467138165,
-0.951178585632847));
#49885=CARTESIAN_POINT('Ctrl Pts',(0.00669754469093416,-0.380990856460232,
-0.934022962441355));
#49886=CARTESIAN_POINT('Ctrl Pts',(0.323937501014007,-0.200657382739803,
-0.914155785498214));
#49887=CARTESIAN_POINT('Ctrl Pts',(0.34409560267971,0.163698216324051,-0.894288608555072));
#49888=CARTESIAN_POINT('Ctrl Pts',(0.0486849310371447,0.377926801512009,
-0.874421431611931));
#49889=CARTESIAN_POINT('Ctrl Pts',(-0.257508780691039,0.258742235111471,
-0.856532780451136));
#49890=CARTESIAN_POINT('Ctrl Pts',(-0.321451744134498,0.0750495365766745,
-0.845266521604723));
#49891=CARTESIAN_POINT('Ctrl Pts',(-0.322069372535088,-0.000277835810467364,
-0.840622655072689));
#49892=CARTESIAN_POINT('Origin',(0.,0.,-3.17777734492731));
#49893=CARTESIAN_POINT('',(-0.322423848909263,-0.000279534380340588,-1.11527734492731));
#49894=CARTESIAN_POINT('',(-0.322631094037432,0.000209311881509786,-1.09062265507269));
#49895=CARTESIAN_POINT('',(-0.322275,-1.53308031181269E-15,-3.17777734492731));
#49896=CARTESIAN_POINT('Ctrl Pts',(-0.322423848909263,-0.000279534380340587,
-1.11527734492731));
#49897=CARTESIAN_POINT('Ctrl Pts',(-0.322607183827066,-0.0203463362564853,
-1.11403676526711));
#49898=CARTESIAN_POINT('Ctrl Pts',(-0.311754457112276,-0.14733488942806,
-1.10617379329253));
#49899=CARTESIAN_POINT('Ctrl Pts',(-0.14313782027769,-0.353143696670534,
-1.09168842900357));
#49900=CARTESIAN_POINT('Ctrl Pts',(0.219396867869826,-0.311550831263358,
-1.07182125206043));
#49901=CARTESIAN_POINT('Ctrl Pts',(0.380723519872219,0.0157641209106834,
-1.05195407511729));
#49902=CARTESIAN_POINT('Ctrl Pts',(0.192890074506225,0.328621857533794,
-1.03208689817415));
#49903=CARTESIAN_POINT('Ctrl Pts',(-0.171842127255466,0.340101733886045,
-1.01221972123101));
#49904=CARTESIAN_POINT('Ctrl Pts',(-0.317145139018747,0.129357440676627,
-0.998283203482062));
#49905=CARTESIAN_POINT('Ctrl Pts',(-0.322742726616871,0.0113577407879511,
-0.990969078047496));
#49906=CARTESIAN_POINT('Ctrl Pts',(-0.322664566790459,0.00019042886585479,
-0.990277344927309));
#49907=CARTESIAN_POINT('Ctrl Pts',(-0.322631094037432,0.000209311881509799,
-1.09062265507269));
#49908=CARTESIAN_POINT('Ctrl Pts',(-0.321920739741796,-0.0941479609162504,
-1.08477950372957));
#49909=CARTESIAN_POINT('Ctrl Pts',(-0.228401002517511,-0.296671203383949,
-1.07231396007208));
#49910=CARTESIAN_POINT('Ctrl Pts',(0.115866267398166,-0.363006746342826,
-1.0532260241002));
#49911=CARTESIAN_POINT('Ctrl Pts',(0.367927300711469,-0.0991382428851851,
-1.03335884715706));
#49912=CARTESIAN_POINT('Ctrl Pts',(0.282563600758959,0.255649567449899,
-1.01349167021392));
#49913=CARTESIAN_POINT('Ctrl Pts',(-0.0619381067084859,0.375982128230261,
-0.99362449327078));
#49914=CARTESIAN_POINT('Ctrl Pts',(-0.293003380988379,0.19569146729556,
-0.977668154890368));
#49915=CARTESIAN_POINT('Ctrl Pts',(-0.322004165770655,0.0442242975322807,
-0.968334208824338));
#49916=CARTESIAN_POINT('Ctrl Pts',(-0.321815198935766,0.000153234844127097,
-0.965622655072689));
#49917=CARTESIAN_POINT('Origin',(0.,0.,-3.17777734492731));
#49918=CARTESIAN_POINT('',(-0.321748138662352,-3.69915658214744E-5,-1.24027734492731));
#49919=CARTESIAN_POINT('',(-0.32246593369561,-0.000270282110639619,-1.21562265507269));
#49920=CARTESIAN_POINT('',(-0.322275,-1.53308031181269E-15,-3.17777734492731));
#49921=CARTESIAN_POINT('Ctrl Pts',(-0.321748138662352,-3.69915658215321E-5,
-1.24027734492731));
#49922=CARTESIAN_POINT('Ctrl Pts',(-0.321800888129312,-0.0516330764776327,
-1.23710445248673));
#49923=CARTESIAN_POINT('Ctrl Pts',(-0.285718595171699,-0.210849744615903,
-1.22730916773176));
#49924=CARTESIAN_POINT('Ctrl Pts',(-0.0356529670902981,-0.379378138576325,
-1.21089149066242));
#49925=CARTESIAN_POINT('Ctrl Pts',(0.299650873068665,-0.235389592720591,
-1.19102431371928));
#49926=CARTESIAN_POINT('Ctrl Pts',(0.360146033027642,0.124473856638375,
-1.17115713677614));
#49927=CARTESIAN_POINT('Ctrl Pts',(0.0903526308274595,0.37018280375314,
-1.151289959833));
#49928=CARTESIAN_POINT('Ctrl Pts',(-0.240281721815781,0.28225474119053,
-1.13266336255005));
#49929=CARTESIAN_POINT('Ctrl Pts',(-0.321628515717655,0.0867731327968641,
-1.12065915758149));
#49930=CARTESIAN_POINT('Ctrl Pts',(-0.322423848909263,-0.000279534380340587,
-1.11527734492731));
#49931=CARTESIAN_POINT('Ctrl Pts',(-0.32246593369561,-0.000270282110639604,
-1.21562265507269));
#49932=CARTESIAN_POINT('Ctrl Pts',(-0.322633297964103,-0.0189153241123458,
-1.21446958326357));
#49933=CARTESIAN_POINT('Ctrl Pts',(-0.312669314181208,-0.144464950082961,
-1.20669411914007));
#49934=CARTESIAN_POINT('Ctrl Pts',(-0.147785253953922,-0.351224157091969,
-1.19229626270219));
#49935=CARTESIAN_POINT('Ctrl Pts',(0.21526668826523,-0.314418737887087,
-1.17242908575905));
#49936=CARTESIAN_POINT('Ctrl Pts',(0.38089836640381,0.0107389143816884,
-1.15256190881591));
#49937=CARTESIAN_POINT('Ctrl Pts',(0.197209596082445,0.326047948964853,
-1.13269473187277));
#49938=CARTESIAN_POINT('Ctrl Pts',(-0.167339347503859,0.342339645072217,
-1.11282755492962));
#49939=CARTESIAN_POINT('Ctrl Pts',(-0.316340318579248,0.132219940356831,
-1.0988035293296));
#49940=CARTESIAN_POINT('Ctrl Pts',(-0.322725826680619,0.0127927704611822,
-1.09140189604395));
#49941=CARTESIAN_POINT('Ctrl Pts',(-0.322631094037432,0.000209311881509799,
-1.09062265507269));
#49942=CARTESIAN_POINT('Origin',(0.,0.,-3.17777734492731));
#49943=CARTESIAN_POINT('',(-0.322287749187065,0.000295527604654457,-1.36527734492731));
#49944=CARTESIAN_POINT('',(-0.32175449810873,-6.01427031357848E-5,-1.34062265507269));
#49945=CARTESIAN_POINT('',(-0.322275,-1.53308031181269E-15,-3.17777734492731));
#49946=CARTESIAN_POINT('Ctrl Pts',(-0.322287749187065,0.000295527604654462,
-1.36527734492731));
#49947=CARTESIAN_POINT('Ctrl Pts',(-0.321524233712806,-0.0823725192591668,
-1.36017213970634));
#49948=CARTESIAN_POINT('Ctrl Pts',(-0.246991313292718,-0.273499001818416,
-1.348444542171));
#49949=CARTESIAN_POINT('Ctrl Pts',(0.0748376698498334,-0.373628464203982,
-1.33009455232127));
#49950=CARTESIAN_POINT('Ctrl Pts',(0.354642304090093,-0.139383436037601,
-1.31022737537813));
#49951=CARTESIAN_POINT('Ctrl Pts',(0.309205825124097,0.222689613141937,
-1.29036019843499));
#49952=CARTESIAN_POINT('Ctrl Pts',(-0.0198021443645707,0.380534861964767,
-1.27049302149184));
#49953=CARTESIAN_POINT('Ctrl Pts',(-0.281005665237226,0.219919384599868,
-1.25379873698929));
#49954=CARTESIAN_POINT('Ctrl Pts',(-0.32169079058547,0.056057153358656,
-1.24372684480111));
#49955=CARTESIAN_POINT('Ctrl Pts',(-0.321748138662352,-3.69915658215321E-5,
-1.24027734492731));
#49956=CARTESIAN_POINT('Ctrl Pts',(-0.32175449810873,-6.01427031357918E-5,
-1.34062265507269));
#49957=CARTESIAN_POINT('Ctrl Pts',(-0.321837987470172,-0.0502307331208825,
-1.33753727048319));
#49958=CARTESIAN_POINT('Ctrl Pts',(-0.287155063447946,-0.207976961406838,
-1.3278294935793));
#49959=CARTESIAN_POINT('Ctrl Pts',(-0.040655941181135,-0.378874628680604,
-1.31149932436104));
#49960=CARTESIAN_POINT('Ctrl Pts',(0.296518686521221,-0.239323125407717,
-1.29163214741789));
#49961=CARTESIAN_POINT('Ctrl Pts',(0.361757150437206,0.119710709290111,
-1.27176497047476));
#49962=CARTESIAN_POINT('Ctrl Pts',(0.0952295025228559,0.368958306127452,
-1.25189779353161));
#49963=CARTESIAN_POINT('Ctrl Pts',(-0.238094936424389,0.285008232302127,
-1.23318368839759));
#49964=CARTESIAN_POINT('Ctrl Pts',(-0.321672081293464,0.0881680178589641,
-1.22109197557795));
#49965=CARTESIAN_POINT('Ctrl Pts',(-0.32246593369561,-0.000270282110639604,
-1.21562265507269));
#49966=CARTESIAN_POINT('Origin',(0.,0.,-3.17777734492731));
#49967=CARTESIAN_POINT('',(-0.322751107179779,-0.000121302661654257,-1.49027734492731));
#49968=CARTESIAN_POINT('',(-0.322244723354561,0.000296369465573723,-1.46562265507269));
#49969=CARTESIAN_POINT('',(-0.322275,-1.53308031181269E-15,-3.17777734492731));
#49970=CARTESIAN_POINT('Ctrl Pts',(-0.322751107179779,-0.000121302661654219,
-1.49027734492731));
#49971=CARTESIAN_POINT('Ctrl Pts',(-0.3227833604428,-0.00681832798748842,
-1.48986221924034));
#49972=CARTESIAN_POINT('Ctrl Pts',(-0.319556406731551,-0.120319591508497,
-1.48282470123899));
#49973=CARTESIAN_POINT('Ctrl Pts',(-0.185874672239764,-0.332640214513727,
-1.46916479092326));
#49974=CARTESIAN_POINT('Ctrl Pts',(0.179018990329492,-0.336379409585943,
-1.44929761398012));
#49975=CARTESIAN_POINT('Ctrl Pts',(0.379735015238712,-0.0316263227965929,
-1.42943043703697));
#49976=CARTESIAN_POINT('Ctrl Pts',(0.232197496633113,0.302131144785331,
-1.40956326009383));
#49977=CARTESIAN_POINT('Ctrl Pts',(-0.128287466249961,0.358805284374608,
-1.38969608315069));
#49978=CARTESIAN_POINT('Ctrl Pts',(-0.308720453379187,0.156414319310542,
-1.37493411142852));
#49979=CARTESIAN_POINT('Ctrl Pts',(-0.322514654036729,0.024863177348577,
-1.36679453202072));
#49980=CARTESIAN_POINT('Ctrl Pts',(-0.322287749187065,0.000295527604654462,
-1.36527734492731));
#49981=CARTESIAN_POINT('Ctrl Pts',(-0.322244723354561,0.000296369465573685,
-1.46562265507269));
#49982=CARTESIAN_POINT('Ctrl Pts',(-0.321501222101524,-0.0809823787116948,
-1.4606049577028));
#49983=CARTESIAN_POINT('Ctrl Pts',(-0.249050437632911,-0.270713713036289,
-1.44896486801853));
#49984=CARTESIAN_POINT('Ctrl Pts',(0.0699009395453964,-0.374583433245331,
-1.43070238601989));
#49985=CARTESIAN_POINT('Ctrl Pts',(0.352772174889632,-0.144050971655273,
-1.41083520907674));
#49986=CARTESIAN_POINT('Ctrl Pts',(0.312117385430717,0.218590090175839,
-1.3909680321336));
#49987=CARTESIAN_POINT('Ctrl Pts',(-0.0147790754750554,0.380763008627795,
-1.37110085519046));
#49988=CARTESIAN_POINT('Ctrl Pts',(-0.279459402901632,0.222784460857227,
-1.35431906283682));
#49989=CARTESIAN_POINT('Ctrl Pts',(-0.321658787992924,0.0574541673355203,
-1.34415966279757));
#49990=CARTESIAN_POINT('Ctrl Pts',(-0.32175449810873,-6.01427031357918E-5,
-1.34062265507269));
#49991=CARTESIAN_POINT('Origin',(0.,0.,-3.17777734492731));
#49992=CARTESIAN_POINT('',(-0.321922168755166,-0.000227579808175941,-1.61527734492731));
#49993=CARTESIAN_POINT('',(-0.322771138341452,-9.69895275597654E-5,-1.59062265507269));
#49994=CARTESIAN_POINT('',(-0.322275,-1.53308031181269E-15,-3.17777734492731));
#49995=CARTESIAN_POINT('Ctrl Pts',(-0.321922168755166,-0.000227579808175983,
-1.61527734492731));
#49996=CARTESIAN_POINT('Ctrl Pts',(-0.322170091457483,-0.038348893149621,
-1.61292990645995));
#49997=CARTESIAN_POINT('Ctrl Pts',(-0.298262264464941,-0.183713933271471,
-1.60396007567822));
#49998=CARTESIAN_POINT('Ctrl Pts',(-0.0824785577203104,-0.372016388897528,
-1.5883678525821));
#49999=CARTESIAN_POINT('Ctrl Pts',(0.268107811741657,-0.270771319336224,
-1.56850067563896));
#50000=CARTESIAN_POINT('Ctrl Pts',(0.372813523017964,0.0787971011326718,
-1.54863349869582));
#50001=CARTESIAN_POINT('Ctrl Pts',(0.135613365066933,0.35610099874502,-1.52876632175268));
#50002=CARTESIAN_POINT('Ctrl Pts',(-0.218402258481575,0.307855623037052,
-1.50931427049651));
#50003=CARTESIAN_POINT('Ctrl Pts',(-0.322268832511024,0.100017578435714,
-1.49648461155472));
#50004=CARTESIAN_POINT('Ctrl Pts',(-0.322751107179779,-0.000121302661654219,
-1.49027734492731));
#50005=CARTESIAN_POINT('Ctrl Pts',(-0.322771138341452,-9.69895275597966E-5,
-1.59062265507269));
#50006=CARTESIAN_POINT('Ctrl Pts',(-0.32279205568065,-0.00538141795017537,
-1.5902950372368));
#50007=CARTESIAN_POINT('Ctrl Pts',(-0.320277876082452,-0.117463752275654,
-1.58334502708653));
#50008=CARTESIAN_POINT('Ctrl Pts',(-0.190247829186885,-0.330158527530134,
-1.56977262462188));
#50009=CARTESIAN_POINT('Ctrl Pts',(0.174564703217894,-0.338712347282523,
-1.54990544767873));
#50010=CARTESIAN_POINT('Ctrl Pts',(0.379284607793692,-0.0366343568522026,
-1.53003827073559));
#50011=CARTESIAN_POINT('Ctrl Pts',(0.236164035815733,0.299040863425743,
-1.51017109379245));
#50012=CARTESIAN_POINT('Ctrl Pts',(-0.123541678493353,0.360466841035667,
-1.49030391684931));
#50013=CARTESIAN_POINT('Ctrl Pts',(-0.307714925372633,0.159288869904934,
-1.47545443727605));
#50014=CARTESIAN_POINT('Ctrl Pts',(-0.322482500289682,0.0262898853514597,
-1.46722735001718));
#50015=CARTESIAN_POINT('Ctrl Pts',(-0.322244723354561,0.000296369465573685,
-1.46562265507269));
#50016=CARTESIAN_POINT('Origin',(0.,0.,-3.17777734492731));
#50017=CARTESIAN_POINT('',(-0.321923856749615,0.00022841188425891,-1.74027734492731));
#50018=CARTESIAN_POINT('',(-0.321953965388694,-0.000242065591690599,-1.71562265507269));
#50019=CARTESIAN_POINT('',(-0.322275,-1.53308031181269E-15,-3.17777734492731));
#50020=CARTESIAN_POINT('Ctrl Pts',(-0.321923856749615,0.000228411884258914,
-1.74027734492731));
#50021=CARTESIAN_POINT('Ctrl Pts',(-0.321470050673185,-0.0692718503800838,
-1.73599759367957));
#50022=CARTESIAN_POINT('Ctrl Pts',(-0.265230516068486,-0.246984636511405,
-1.72509545011745));
#50023=CARTESIAN_POINT('Ctrl Pts',(0.0278710512479263,-0.380029091773661,
-1.70757091424095));
#50024=CARTESIAN_POINT('Ctrl Pts',(0.334593350165504,-0.182335394580983,
-1.68770373729781));
#50025=CARTESIAN_POINT('Ctrl Pts',(0.334461355547943,0.182577402043658,
-1.66783656035467));
#50026=CARTESIAN_POINT('Ctrl Pts',(0.0275961191588265,0.380049155109377,
-1.64796938341153));
#50027=CARTESIAN_POINT('Ctrl Pts',(-0.265328911815288,0.246829175329326,
-1.63044964493574));
#50028=CARTESIAN_POINT('Ctrl Pts',(-0.321470673167627,0.0691956904453584,
-1.61955229877433));
#50029=CARTESIAN_POINT('Ctrl Pts',(-0.321922168755166,-0.000227579808175983,
-1.61527734492731));
#50030=CARTESIAN_POINT('Ctrl Pts',(-0.321953965388694,-0.000242065591690606,
-1.71562265507269));
#50031=CARTESIAN_POINT('Ctrl Pts',(-0.322209458649345,-0.0369331731931518,
-1.71336272445641));
#50032=CARTESIAN_POINT('Ctrl Pts',(-0.299463487975333,-0.180834904933275,
-1.70448040152576));
#50033=CARTESIAN_POINT('Ctrl Pts',(-0.0873803104607973,-0.370895633777163,
-1.68897568628072));
#50034=CARTESIAN_POINT('Ctrl Pts',(0.264511494039161,-0.27428554342575,
-1.66910850933758));
#50035=CARTESIAN_POINT('Ctrl Pts',(0.373820809690602,0.0738707794290245,
-1.64924133239444));
#50036=CARTESIAN_POINT('Ctrl Pts',(0.140300477324218,0.354280490393961,
-1.6293741554513));
#50037=CARTESIAN_POINT('Ctrl Pts',(-0.215916241007796,0.310514722383114,
-1.60983459634405));
#50038=CARTESIAN_POINT('Ctrl Pts',(-0.322369237350371,0.10143681456936,
-1.59691742955118));
#50039=CARTESIAN_POINT('Ctrl Pts',(-0.322771138341452,-9.69895275597966E-5,
-1.59062265507269));
#50040=CARTESIAN_POINT('Origin',(0.,0.,-3.17777734492731));
#50041=CARTESIAN_POINT('',(-0.3227523074527,0.000119995480296377,-1.86527734492731));
#50042=CARTESIAN_POINT('',(-0.32189411998726,0.000212574305966731,-1.84062265507269));
#50043=CARTESIAN_POINT('',(-0.322275,-1.53308031181269E-15,-3.17777734492731));
#50044=CARTESIAN_POINT('Ctrl Pts',(-0.3227523074527,0.000119995480296356,
-1.86527734492731));
#50045=CARTESIAN_POINT('Ctrl Pts',(-0.322274164449301,-0.1000952891468,
-1.85906528089919));
#50046=CARTESIAN_POINT('Ctrl Pts',(-0.218266807444085,-0.308001705979866,
-1.84623082455668));
#50047=CARTESIAN_POINT('Ctrl Pts',(0.13587094405367,-0.356002798660267,
-1.8267739758998));
#50048=CARTESIAN_POINT('Ctrl Pts',(0.372870429720997,-0.0785273756829916,
-1.80690679895666));
#50049=CARTESIAN_POINT('Ctrl Pts',(0.267911857239273,0.270965205963022,
-1.78703962201352));
#50050=CARTESIAN_POINT('Ctrl Pts',(-0.0827476642965211,0.371956624010715,
-1.76717244507038));
#50051=CARTESIAN_POINT('Ctrl Pts',(-0.298328740556997,0.183556097792722,
-1.75158501937497));
#50052=CARTESIAN_POINT('Ctrl Pts',(-0.322172260147241,0.0382713165060726,
-1.74261998599395));
#50053=CARTESIAN_POINT('Ctrl Pts',(-0.321923856749615,0.000228411884258914,
-1.74027734492731));
#50054=CARTESIAN_POINT('Ctrl Pts',(-0.32189411998726,0.000212574305966721,
-1.84062265507269));
#50055=CARTESIAN_POINT('Ctrl Pts',(-0.321482807742295,-0.067882398119342,
-1.83643041167603));
#50056=CARTESIAN_POINT('Ctrl Pts',(-0.267011798870114,-0.244146878061487,
-1.82561577596499));
#50057=CARTESIAN_POINT('Ctrl Pts',(0.0228539532777633,-0.380363755674442,
-1.80817874793957));
#50058=CARTESIAN_POINT('Ctrl Pts',(0.332158195524763,-0.186734632451837,
-1.78831157099643));
#50059=CARTESIAN_POINT('Ctrl Pts',(0.336841415329915,0.178148114583703,
-1.76844439405329));
#50060=CARTESIAN_POINT('Ctrl Pts',(0.0326086495564207,0.379651900805587,
-1.74857721711014));
#50061=CARTESIAN_POINT('Ctrl Pts',(-0.263520523765027,0.249662771554132,
-1.73096997078328));
#50062=CARTESIAN_POINT('Ctrl Pts',(-0.321460773449221,0.0705846891854826,
-1.71998511677079));
#50063=CARTESIAN_POINT('Ctrl Pts',(-0.321953965388694,-0.000242065591690606,
-1.71562265507269));
#50064=CARTESIAN_POINT('Origin',(0.,0.,-3.17777734492731));
#50065=CARTESIAN_POINT('',(-0.32228538328799,-0.000295626100757004,-1.99027734492731));
#50066=CARTESIAN_POINT('',(-0.322728660521504,0.000143315081735037,-1.96562265507269));
#50067=CARTESIAN_POINT('',(-0.322275,-1.53308031181269E-15,-3.17777734492731));
#50068=CARTESIAN_POINT('Ctrl Pts',(-0.32228538328799,-0.000295626100757031,
-1.99027734492731));
#50069=CARTESIAN_POINT('Ctrl Pts',(-0.32251292564102,-0.0249414224581168,
-1.98875536043318));
#50070=CARTESIAN_POINT('Ctrl Pts',(-0.308665902992896,-0.156571884968343,
-1.98061098362468));
#50071=CARTESIAN_POINT('Ctrl Pts',(-0.128027861842815,-0.358897997603687,
-1.96584421450179));
#50072=CARTESIAN_POINT('Ctrl Pts',(0.232416006884924,-0.301963086875939,
-1.94597703755865));
#50073=CARTESIAN_POINT('Ctrl Pts',(0.37971203641127,0.0319010265725857,
-1.9261098606155));
#50074=CARTESIAN_POINT('Ctrl Pts',(0.178775596218371,0.336508829436531,
-1.90624268367236));
#50075=CARTESIAN_POINT('Ctrl Pts',(-0.18611526581757,0.332505659984359,
-1.88637550672922));
#50076=CARTESIAN_POINT('Ctrl Pts',(-0.319596470562309,0.120162984611006,
-1.8727203938142));
#50077=CARTESIAN_POINT('Ctrl Pts',(-0.322783890449637,0.00673956118529448,
-1.86568767321357));
#50078=CARTESIAN_POINT('Ctrl Pts',(-0.3227523074527,0.000119995480296356,
-1.86527734492731));
#50079=CARTESIAN_POINT('Ctrl Pts',(-0.322728660521503,0.000143315081735021,
-1.96562265507269));
#50080=CARTESIAN_POINT('Ctrl Pts',(-0.32218001068861,-0.0986794523285048,
-1.95949809889565));
#50081=CARTESIAN_POINT('Ctrl Pts',(-0.220722265880929,-0.305331620279144,
-1.94675115040422));
#50082=CARTESIAN_POINT('Ctrl Pts',(0.131161475792397,-0.357764667175434,
-1.92738180959841));
#50083=CARTESIAN_POINT('Ctrl Pts',(0.371801737976828,-0.0834407421383482,
-1.90751463265528));
#50084=CARTESIAN_POINT('Ctrl Pts',(0.271464035161107,0.267406371325063,
-1.88764745571213));
#50085=CARTESIAN_POINT('Ctrl Pts',(-0.0778323056202418,0.373016114950851,
-1.86778027876899));
#50086=CARTESIAN_POINT('Ctrl Pts',(-0.297104761464683,0.18643508125568,
-1.85210534522251));
#50087=CARTESIAN_POINT('Ctrl Pts',(-0.322132548416235,0.0396856935607706,
-1.84305280399041));
#50088=CARTESIAN_POINT('Ctrl Pts',(-0.32189411998726,0.000212574305966721,
-1.84062265507269));
#50089=CARTESIAN_POINT('Origin',(0.,0.,-3.17777734492731));
#50090=CARTESIAN_POINT('',(-0.321748409289639,3.82678754979511E-5,-2.11527734492731));
#50091=CARTESIAN_POINT('',(-0.322328587652096,-0.00029287054778171,-2.09062265507269));
#50092=CARTESIAN_POINT('',(-0.322275,-1.53308031181269E-15,-3.17777734492731));
#50093=CARTESIAN_POINT('Ctrl Pts',(-0.321748409289639,3.82678754979639E-5,
-2.11527734492731));
#50094=CARTESIAN_POINT('Ctrl Pts',(-0.32168899726537,-0.0561337723056524,
-2.1118230476528));
#50095=CARTESIAN_POINT('Ctrl Pts',(-0.280921590087898,-0.220076513828276,
-2.10174635806391));
#50096=CARTESIAN_POINT('Ctrl Pts',(-0.0195268484971016,-0.380549087871386,
-2.08504727616063));
#50097=CARTESIAN_POINT('Ctrl Pts',(0.309366844764242,-0.222465865814493,
-2.06518009921749));
#50098=CARTESIAN_POINT('Ctrl Pts',(0.354541377001136,0.139639958772985,
-2.04531292227435));
#50099=CARTESIAN_POINT('Ctrl Pts',(0.0745673558825864,0.373682506318743,
-2.02544574533121));
#50100=CARTESIAN_POINT('Ctrl Pts',(-0.247104986648104,0.273346487692639,
-2.0071005528822));
#50101=CARTESIAN_POINT('Ctrl Pts',(-0.321522853313923,0.0822962879184196,
-1.99537775274756));
#50102=CARTESIAN_POINT('Ctrl Pts',(-0.32228538328799,-0.000295626100757031,
-1.99027734492731));
#50103=CARTESIAN_POINT('Ctrl Pts',(-0.322328587652096,-0.000292870547781703,
-2.09062265507269));
#50104=CARTESIAN_POINT('Ctrl Pts',(-0.322543800094343,-0.0235136571889884,
-2.08918817842964));
#50105=CARTESIAN_POINT('Ctrl Pts',(-0.309650508248358,-0.153698251766603,
-2.08113130947221));
#50106=CARTESIAN_POINT('Ctrl Pts',(-0.132752542720296,-0.357177340004209,
-2.0664520482004));
#50107=CARTESIAN_POINT('Ctrl Pts',(0.228411208027658,-0.305003622697395,
-2.04658487125726));
#50108=CARTESIAN_POINT('Ctrl Pts',(0.380099905430515,0.0268877612103093,
-2.02671769431412));
#50109=CARTESIAN_POINT('Ctrl Pts',(0.183200419906357,0.334120481200005,
-2.00685051737098));
#50110=CARTESIAN_POINT('Ctrl Pts',(-0.181711476497752,0.334932573990939,
-1.98698334042784));
#50111=CARTESIAN_POINT('Ctrl Pts',(-0.318856304620057,0.123020370421255,
-1.97324071966174));
#50112=CARTESIAN_POINT('Ctrl Pts',(-0.32277325766547,0.0081761493616704,
-1.96612049121003));
#50113=CARTESIAN_POINT('Ctrl Pts',(-0.322728660521503,0.000143315081735021,
-1.96562265507269));
#50114=CARTESIAN_POINT('Origin',(0.,0.,-3.17777734492731));
#50115=CARTESIAN_POINT('',(-0.322426177028279,0.000279078778166078,-2.24027734492731));
#50116=CARTESIAN_POINT('',(-0.321744902911595,1.49008663381245E-5,-2.21562265507269));
#50117=CARTESIAN_POINT('',(-0.322275,-1.53308031181269E-15,-3.17777734492731));
#50118=CARTESIAN_POINT('Ctrl Pts',(-0.322426177028279,0.000279078778166082,
-2.24027734492731));
#50119=CARTESIAN_POINT('Ctrl Pts',(-0.321630768589567,-0.0868495651447256,
-2.23489073487241));
#50120=CARTESIAN_POINT('Ctrl Pts',(-0.240162640512569,-0.282405909728632,
-2.22288173250314));
#50121=CARTESIAN_POINT('Ctrl Pts',(0.090620408871829,-0.370117342997772,
-2.20425033781948));
#50122=CARTESIAN_POINT('Ctrl Pts',(0.360235987022344,-0.124213283290337,
-2.18438316087634));
#50123=CARTESIAN_POINT('Ctrl Pts',(0.299480506547509,0.235606307831963,
-2.1645159839332));
#50124=CARTESIAN_POINT('Ctrl Pts',(-0.0359274116371167,0.379352246843221,
-2.14464880699006));
#50125=CARTESIAN_POINT('Ctrl Pts',(-0.285798019731171,0.210692290217066,
-2.12823592732143));
#50126=CARTESIAN_POINT('Ctrl Pts',(-0.321802898791972,0.0515562316565445,
-2.11844543996718));
#50127=CARTESIAN_POINT('Ctrl Pts',(-0.321748409289639,3.82678754979639E-5,
-2.11527734492731));
#50128=CARTESIAN_POINT('Ctrl Pts',(-0.321744902911595,1.49008663381453E-5,
-2.21562265507269));
#50129=CARTESIAN_POINT('Ctrl Pts',(-0.321722368475626,-0.0547356078121411,
-2.21225586564926));
#50130=CARTESIAN_POINT('Ctrl Pts',(-0.282442567683545,-0.217209365600774,
-2.20226668391144));
#50131=CARTESIAN_POINT('Ctrl Pts',(-0.0245466787495387,-0.380258267988377,
-2.18565510985925));
#50132=CARTESIAN_POINT('Ctrl Pts',(0.306404346658912,-0.226528731422051,
-2.16578793291611));
#50133=CARTESIAN_POINT('Ctrl Pts',(0.356353106829473,0.134949446327866,
-2.14592075597297));
#50134=CARTESIAN_POINT('Ctrl Pts',(0.0794917830842547,0.372665998225311,
-2.12605357902982));
#50135=CARTESIAN_POINT('Ctrl Pts',(-0.245017099497695,0.276125023901044,
-2.10762087872974));
#50136=CARTESIAN_POINT('Ctrl Pts',(-0.321550252217212,0.0836872231681876,
-2.09581057074402));
#50137=CARTESIAN_POINT('Ctrl Pts',(-0.322328587652096,-0.000292870547781703,
-2.09062265507269));
#50138=CARTESIAN_POINT('Origin',(0.,0.,-3.17777734492731));
#50139=CARTESIAN_POINT('',(-0.322662798805829,-0.000191504950135908,-2.36527734492731));
#50140=CARTESIAN_POINT('',(-0.322383419286056,0.000286438788401844,-2.34062265507269));
#50141=CARTESIAN_POINT('',(-0.322275,-1.53308031181269E-15,-3.17777734492731));
#50142=CARTESIAN_POINT('Ctrl Pts',(-0.322662798805829,-0.00019150495013591,
-2.36527734492731));
#50143=CARTESIAN_POINT('Ctrl Pts',(-0.322741850192619,-0.0114364278866111,
-2.36458081440641));
#50144=CARTESIAN_POINT('Ctrl Pts',(-0.317101545247626,-0.129514330580757,
-2.35726189157113));
#50145=CARTESIAN_POINT('Ctrl Pts',(-0.171596042253934,-0.340225960835699,
-2.34332057642147));
#50146=CARTESIAN_POINT('Ctrl Pts',(0.193127759284308,-0.328482228877282,
-2.32345339947833));
#50147=CARTESIAN_POINT('Ctrl Pts',(0.380734824477702,-0.0154886896292257,
-2.30358622253519));
#50148=CARTESIAN_POINT('Ctrl Pts',(0.219171424964897,0.311709468221516,
-2.28371904559205));
#50149=CARTESIAN_POINT('Ctrl Pts',(-0.143393257897354,0.353040053933262,
-2.2638518686489));
#50150=CARTESIAN_POINT('Ctrl Pts',(-0.311805167411146,0.147177520159949,
-2.24937130176066));
#50151=CARTESIAN_POINT('Ctrl Pts',(-0.322608657591674,0.0202679087390474,
-2.24151312718679));
#50152=CARTESIAN_POINT('Ctrl Pts',(-0.322426177028279,0.000279078778166082,
-2.24027734492731));
#50153=CARTESIAN_POINT('Ctrl Pts',(-0.322383419286056,0.000286438788401826,
-2.34062265507269));
#50154=CARTESIAN_POINT('Ctrl Pts',(-0.321592096098541,-0.0854560343740861,
-2.33532355286887));
#50155=CARTESIAN_POINT('Ctrl Pts',(-0.242320152705578,-0.279644670426524,
-2.32340205835068));
#50156=CARTESIAN_POINT('Ctrl Pts',(0.0857286345377398,-0.371280878892406,
-2.3048581715181));
#50157=CARTESIAN_POINT('Ctrl Pts',(0.358565548084728,-0.128955951921072,
-2.28499099457496));
#50158=CARTESIAN_POINT('Ctrl Pts',(0.302563356235795,0.231633989897339,
-2.26512381763181));
#50159=CARTESIAN_POINT('Ctrl Pts',(-0.0309185430950134,0.379793277328495,
-2.24525664068868));
#50160=CARTESIAN_POINT('Ctrl Pts',(-0.284336907323424,0.213563599955149,
-2.22875625316897));
#50161=CARTESIAN_POINT('Ctrl Pts',(-0.321766693159115,0.0529573014494938,
-2.21887825796364));
#50162=CARTESIAN_POINT('Ctrl Pts',(-0.321744902911595,1.49008663381453E-5,
-2.21562265507269));
#50163=CARTESIAN_POINT('Origin',(0.,0.,-3.17777734492731));
#50164=CARTESIAN_POINT('',(-0.321835633176319,-0.000171871078531275,-2.49027734492731));
#50165=CARTESIAN_POINT('',(-0.322693718878697,-0.000171168389977605,-2.46562265507269));
#50166=CARTESIAN_POINT('',(-0.322275,-1.53308031181269E-15,-3.17777734492731));
#50167=CARTESIAN_POINT('Ctrl Pts',(-0.321835633176319,-0.000171871078531286,
-2.49027734492731));
#50168=CARTESIAN_POINT('Ctrl Pts',(-0.322041881997969,-0.042891857212214,
-2.48764850162603));
#50169=CARTESIAN_POINT('Ctrl Pts',(-0.294235300856302,-0.192971292817336,
-2.47839726601036));
#50170=CARTESIAN_POINT('Ctrl Pts',(-0.066622590386437,-0.375180407854742,
-2.46252363808032));
#50171=CARTESIAN_POINT('Ctrl Pts',(0.279353148857915,-0.259153863380453,
-2.44265646113718));
#50172=CARTESIAN_POINT('Ctrl Pts',(0.369135166970047,0.0945417037460469,
-2.42278928419404));
#50173=CARTESIAN_POINT('Ctrl Pts',(0.120384725846265,0.361533434408456,
-2.40292210725089));
#50174=CARTESIAN_POINT('Ctrl Pts',(-0.226178354733955,0.29922797675211,
-2.38375146082865));
#50175=CARTESIAN_POINT('Ctrl Pts',(-0.321990254561689,0.0954767496352355,
-2.37120320672079));
#50176=CARTESIAN_POINT('Ctrl Pts',(-0.322662798805829,-0.00019150495013591,
-2.36527734492731));
#50177=CARTESIAN_POINT('Ctrl Pts',(-0.322693718878697,-0.000171168389977631,
-2.46562265507269));
#50178=CARTESIAN_POINT('Ctrl Pts',(-0.322756909832245,-0.0100008653975118,
-2.46501363240287));
#50179=CARTESIAN_POINT('Ctrl Pts',(-0.317887136349063,-0.126653283447023,
-2.45778221741867));
#50180=CARTESIAN_POINT('Ctrl Pts',(-0.176070541289752,-0.337932026630971,
-2.44392841012009));
#50181=CARTESIAN_POINT('Ctrl Pts',(0.188776450434642,-0.331002026615422,
-2.42406123317694));
#50182=CARTESIAN_POINT('Ctrl Pts',(0.380497273760583,-0.0205113226115502,
-2.40419405623381));
#50183=CARTESIAN_POINT('Ctrl Pts',(0.223265489718655,0.308790237805464,
-2.38432687929066));
#50184=CARTESIAN_POINT('Ctrl Pts',(-0.13872222919299,0.354901441165425,
-2.36445970234752));
#50185=CARTESIAN_POINT('Ctrl Pts',(-0.310869984589673,0.150048604980915,
-2.3498916276082));
#50186=CARTESIAN_POINT('Ctrl Pts',(-0.322581028259807,0.0216980218126806,
-2.34194594518325));
#50187=CARTESIAN_POINT('Ctrl Pts',(-0.322383419286056,0.000286438788401826,
-2.34062265507269));
#50188=CARTESIAN_POINT('Origin',(0.,0.,-3.17777734492731));
#50189=CARTESIAN_POINT('',(-0.322033807694356,0.000269037653784302,-2.61527734492731));
#50190=CARTESIAN_POINT('',(-0.321859793408538,-0.000190557072052594,-2.59062265507269));
#50191=CARTESIAN_POINT('',(-0.322275,-1.53308031181269E-15,-3.17777734492731));
#50192=CARTESIAN_POINT('Ctrl Pts',(-0.322033807694356,0.000269037653784287,
-2.61527734492731));
#50193=CARTESIAN_POINT('Ctrl Pts',(-0.321450758150024,-0.0737374573484295,
-2.61071618884564));
#50194=CARTESIAN_POINT('Ctrl Pts',(-0.259306789923588,-0.256078975821658,
-2.59953264044959));
#50195=CARTESIAN_POINT('Ctrl Pts',(0.0439674142038161,-0.378504723556717,
-2.58172669973917));
#50196=CARTESIAN_POINT('Ctrl Pts',(0.342027290992345,-0.167977046624136,
-2.56185952279602));
#50197=CARTESIAN_POINT('Ctrl Pts',(0.32641489581436,0.196601574673756,-2.54199234585288));
#50198=CARTESIAN_POINT('Ctrl Pts',(0.0114488138936679,0.380877724874727,
-2.52212516890974));
#50199=CARTESIAN_POINT('Ctrl Pts',(-0.270951082513467,0.23768862691842,
-2.50488683526788));
#50200=CARTESIAN_POINT('Ctrl Pts',(-0.321522314851962,0.0647252486472288,
-2.49427089394041));
#50201=CARTESIAN_POINT('Ctrl Pts',(-0.321835633176319,-0.000171871078531286,
-2.49027734492731));
#50202=CARTESIAN_POINT('Ctrl Pts',(-0.321859793408538,-0.000190557072052674,
-2.59062265507269));
#50203=CARTESIAN_POINT('Ctrl Pts',(-0.322081837109745,-0.0414807282665668,
-2.58808131962248));
#50204=CARTESIAN_POINT('Ctrl Pts',(-0.295514570226463,-0.190092842203374,
-2.5789175918579));
#50205=CARTESIAN_POINT('Ctrl Pts',(-0.0715674996361506,-0.374268611298861,
-2.56313147177894));
#50206=CARTESIAN_POINT('Ctrl Pts',(0.275909162196494,-0.262817483673361,
-2.54326429483579));
#50207=CARTESIAN_POINT('Ctrl Pts',(0.370350525192519,0.0896625461742955,
-2.52339711789266));
#50208=CARTESIAN_POINT('Ctrl Pts',(0.125144851946343,0.359913403121745,
-2.5035299409495));
#50209=CARTESIAN_POINT('Ctrl Pts',(-0.223795756394066,0.301922936457637,
-2.4842717866762));
#50210=CARTESIAN_POINT('Ctrl Pts',(-0.322069783874789,0.0968853198647176,
-2.47163602471725));
#50211=CARTESIAN_POINT('Ctrl Pts',(-0.322693718878697,-0.000171168389977631,
-2.46562265507269));
#50212=CARTESIAN_POINT('Origin',(0.,0.,-3.17777734492731));
#50213=CARTESIAN_POINT('',(-0.322809309401469,3.43315038937645E-5,-2.74027734492731));
#50214=CARTESIAN_POINT('',(-0.321998819203686,0.000257793408019194,-2.71562265507269));
#50215=CARTESIAN_POINT('',(-0.322275,-1.53308031181269E-15,-3.17777734492731));
#50216=CARTESIAN_POINT('Ctrl Pts',(-0.322809858836148,3.43668072568986E-5,
-2.74027734492731));
#50217=CARTESIAN_POINT('Ctrl Pts',(-0.322638450561074,-0.104681964129316,
-2.73378387606526));
#50218=CARTESIAN_POINT('Ctrl Pts',(-0.210133729114781,-0.316498876460796,
-2.72066801488882));
#50219=CARTESIAN_POINT('Ctrl Pts',(0.150841923458968,-0.349922901607075,
-2.70092976139801));
#50220=CARTESIAN_POINT('Ctrl Pts',(0.375870812198945,-0.0626363718479885,
-2.68106258445487));
#50221=CARTESIAN_POINT('Ctrl Pts',(0.256173277980071,0.282085432090484,
-2.66119540751173));
#50222=CARTESIAN_POINT('Ctrl Pts',(-0.0984510634044162,0.368112092752765,
-2.64132823056859));
#50223=CARTESIAN_POINT('Ctrl Pts',(-0.302103077194693,0.174298307700632,
-2.62602220970711));
#50224=CARTESIAN_POINT('Ctrl Pts',(-0.322297294149265,0.0337133807596303,
-2.61733858116002));
#50225=CARTESIAN_POINT('Ctrl Pts',(-0.322033807694356,0.000269037653784287,
-2.61527734492731));
#50226=CARTESIAN_POINT('Ctrl Pts',(-0.321998819203686,0.000257793408019166,
-2.71562265507269));
#50227=CARTESIAN_POINT('Ctrl Pts',(-0.321453931795426,-0.072349355039821,
-2.7111490068421));
#50228=CARTESIAN_POINT('Ctrl Pts',(-0.261178988720823,-0.253255718009303,
-2.70005296629713));
#50229=CARTESIAN_POINT('Ctrl Pts',(0.0389678303295289,-0.379052262416539,
-2.68233453343778));
#50230=CARTESIAN_POINT('Ctrl Pts',(0.339781580148665,-0.172475450822871,
-2.66246735649464));
#50231=CARTESIAN_POINT('Ctrl Pts',(0.32898038540163,0.192277148854254,-2.6426001795515));
#50232=CARTESIAN_POINT('Ctrl Pts',(0.0164738552685434,0.380693518847251,
-2.62273300260836));
#50233=CARTESIAN_POINT('Ctrl Pts',(-0.269234143322179,0.240535337111991,
-2.60540716111542));
#50234=CARTESIAN_POINT('Ctrl Pts',(-0.321503219871233,0.0661161308398998,
-2.59470371193687));
#50235=CARTESIAN_POINT('Ctrl Pts',(-0.321859793408538,-0.000190557072052674,
-2.59062265507269));
#50236=CARTESIAN_POINT('Origin',(5.160062080289E-17,2.1385152528819E-17,
-0.04));
#50237=CARTESIAN_POINT('Ctrl Pts',(0.258434353604258,0.193455249693963,
-0.0400000000000002));
#50238=CARTESIAN_POINT('Ctrl Pts',(0.254935552790794,0.199417319786304,
-0.0400000000000001));
#50239=CARTESIAN_POINT('Ctrl Pts',(0.251237159329282,0.205249124536648,
-0.0400000000000005));
#50240=CARTESIAN_POINT('Ctrl Pts',(0.247341514049974,0.21093929920956,-0.0400000000000005));
#50241=CARTESIAN_POINT('Ctrl Pts',(0.238878778768656,0.223300394357799,
-0.0400000000000004));
#50242=CARTESIAN_POINT('Ctrl Pts',(0.229486688116491,0.234993819321299,
-0.0399999999999996));
#50243=CARTESIAN_POINT('Ctrl Pts',(0.219284430274965,0.24599200395083,-0.0399999999999995));
#50244=CARTESIAN_POINT('Ctrl Pts',(0.215221055483291,0.250372381987926,
-0.0399999999999995));
#50245=CARTESIAN_POINT('Ctrl Pts',(0.211028923384398,0.254642373102135,
-0.0399999999999999));
#50246=CARTESIAN_POINT('Ctrl Pts',(0.206714685254849,0.258799772813936,
-0.0399999999999998));
#50247=CARTESIAN_POINT('Ctrl Pts',(0.202264841585829,0.263087848305281,
-0.0399999999999998));
#50248=CARTESIAN_POINT('Ctrl Pts',(0.197691588390428,0.267249800115209,
-0.0400000000000002));
#50249=CARTESIAN_POINT('Ctrl Pts',(0.193005768999244,0.271281678715959,
-0.0400000000000001));
#50250=CARTESIAN_POINT('Ctrl Pts',(0.183472268352816,0.279484708759944,
-0.0400000000000001));
#50251=CARTESIAN_POINT('Ctrl Pts',(0.173470125375889,0.287152749594996,
-0.0399999999999997));
#50252=CARTESIAN_POINT('Ctrl Pts',(0.163063775287283,0.294268502238259,
-0.0399999999999998));
#50253=CARTESIAN_POINT('Ctrl Pts',(0.156857205698134,0.298512489186952,
-0.0399999999999998));
#50254=CARTESIAN_POINT('Ctrl Pts',(0.150506682275409,0.30255992574958,-0.0400000000000011));
#50255=CARTESIAN_POINT('Ctrl Pts',(0.144024608694813,0.306406173056219,
-0.0400000000000014));
#50256=CARTESIAN_POINT('Ctrl Pts',(0.13801492013987,0.309972122768266,-0.0400000000000016));
#50257=CARTESIAN_POINT('Ctrl Pts',(0.131889073078277,0.313366371281921,
-0.0400000000000001));
#50258=CARTESIAN_POINT('Ctrl Pts',(0.125679686933379,0.316573570273351,
-0.0400000000000002));
#50259=CARTESIAN_POINT('Ctrl Pts',(0.107830520217822,0.325792811620591,
-0.0400000000000006));
#50260=CARTESIAN_POINT('Ctrl Pts',(0.0892595211029016,0.333491457102897,
-0.0400000000000009));
#50261=CARTESIAN_POINT('Ctrl Pts',(0.0702059907982684,0.33959923982706,
-0.040000000000001));
#50262=CARTESIAN_POINT('Ctrl Pts',(0.0580714236002871,0.343489085892962,
-0.0400000000000011));
#50263=CARTESIAN_POINT('Ctrl Pts',(0.0457401932381266,0.346733050166134,
-0.0400000000000004));
#50264=CARTESIAN_POINT('Ctrl Pts',(0.0332675301001174,0.349304263700216,
-0.0400000000000004));
#50265=CARTESIAN_POINT('Ctrl Pts',(0.0265485814021288,0.350689360983445,
-0.0400000000000004));
#50266=CARTESIAN_POINT('Ctrl Pts',(0.0197885224519527,0.351879102946484,
-0.0400000000000001));
#50267=CARTESIAN_POINT('Ctrl Pts',(0.0129956579817659,0.352868294018133,
-0.0400000000000001));
#50268=CARTESIAN_POINT('Ctrl Pts',(0.00804678818067408,0.353588958745581,
-0.0400000000000001));
#50269=CARTESIAN_POINT('Ctrl Pts',(0.00308158879209203,0.354202813440212,
-0.0400000000000002));
#50270=CARTESIAN_POINT('Ctrl Pts',(-0.00188381180052424,0.354706990746059,
-0.0400000000000001));
#50271=CARTESIAN_POINT('Ctrl Pts',(-0.0172998207958895,0.356272302897055,
-0.0399999999999999));
#50272=CARTESIAN_POINT('Ctrl Pts',(-0.0327495771761552,0.356786600192842,
-0.0399999999999995));
#50273=CARTESIAN_POINT('Ctrl Pts',(-0.0481326344100983,0.356212876732489,
-0.0399999999999997));
#50274=CARTESIAN_POINT('Ctrl Pts',(-0.0637031171152668,0.355632163088827,
-0.0399999999999999));
#50275=CARTESIAN_POINT('Ctrl Pts',(-0.0792056774455648,0.353937153629172,
-0.0399999999999999));
#50276=CARTESIAN_POINT('Ctrl Pts',(-0.0945633679186374,0.351199965874531,
-0.0399999999999999));
#50277=CARTESIAN_POINT('Ctrl Pts',(-0.101975271573269,0.34987894876212,
-0.04));
#50278=CARTESIAN_POINT('Ctrl Pts',(-0.109353466694925,0.348314883920549,
-0.0400000000000002));
#50279=CARTESIAN_POINT('Ctrl Pts',(-0.116689311574246,0.346514258971721,
-0.0400000000000003));
#50280=CARTESIAN_POINT('Ctrl Pts',(-0.124329759338377,0.344638867508211,
-0.0400000000000004));
#50281=CARTESIAN_POINT('Ctrl Pts',(-0.131930906052299,0.342504388350935,
-0.0399999999999999));
#50282=CARTESIAN_POINT('Ctrl Pts',(-0.139446701840371,0.340129574738105,
-0.0399999999999998));
#50283=CARTESIAN_POINT('Ctrl Pts',(-0.159130311566537,0.333910019863884,
-0.0399999999999996));
#50284=CARTESIAN_POINT('Ctrl Pts',(-0.178265201866502,0.326040008951898,
-0.0399999999999999));
#50285=CARTESIAN_POINT('Ctrl Pts',(-0.196681848896184,0.316683365411485,
-0.0399999999999997));
#50286=CARTESIAN_POINT('Ctrl Pts',(-0.213113725529896,0.308335091585425,
-0.0399999999999996));
#50287=CARTESIAN_POINT('Ctrl Pts',(-0.228974568785446,0.298802296753521,
-0.04));
#50288=CARTESIAN_POINT('Ctrl Pts',(-0.244138579475071,0.288168648000194,
-0.0399999999999999));
#50289=CARTESIAN_POINT('Ctrl Pts',(-0.248431468701942,0.285158291630113,
-0.0399999999999999));
#50290=CARTESIAN_POINT('Ctrl Pts',(-0.252668440607336,0.282059536997446,
-0.0399999999999993));
#50291=CARTESIAN_POINT('Ctrl Pts',(-0.256846437163618,0.278873893021272,
-0.0399999999999991));
#50292=CARTESIAN_POINT('Ctrl Pts',(-0.260954469218941,0.275741595664231,
-0.039999999999999));
#50293=CARTESIAN_POINT('Ctrl Pts',(-0.264998315768473,0.272530722669869,
-0.0399999999999999));
#50294=CARTESIAN_POINT('Ctrl Pts',(-0.268973925848638,0.269244900831608,
-0.0399999999999999));
#50295=CARTESIAN_POINT('Ctrl Pts',(-0.286388122571056,0.254852154376976,
-0.0400000000000002));
#50296=CARTESIAN_POINT('Ctrl Pts',(-0.302504949569424,0.239018084297059,
-0.0400000000000004));
#50297=CARTESIAN_POINT('Ctrl Pts',(-0.317110814018719,0.221907185131117,
-0.0399999999999999));
#50298=CARTESIAN_POINT('Ctrl Pts',(-0.33092057051697,0.205728933459118,
-0.0399999999999994));
#50299=CARTESIAN_POINT('Ctrl Pts',(-0.343380775179789,0.188408133777718,
-0.0400000000000002));
#50300=CARTESIAN_POINT('Ctrl Pts',(-0.354281586312166,0.170043374953611,
-0.0400000000000005));
#50301=CARTESIAN_POINT('Ctrl Pts',(-0.354909998725984,0.168984679203204,
-0.0400000000000005));
#50302=CARTESIAN_POINT('Ctrl Pts',(-0.355533217432698,0.167922504900279,
-0.04));
#50303=CARTESIAN_POINT('Ctrl Pts',(-0.356151197810523,0.166856867698425,
-0.04));
#50304=CARTESIAN_POINT('',(-0.348766791062876,-0.183211156103301,-0.0400000000000003));
#50305=CARTESIAN_POINT('Origin',(0.,0.,-0.04));
#50306=CARTESIAN_POINT('Ctrl Pts',(-0.348771505299647,-0.183214908972786,
-0.0400000000000003));
#50307=CARTESIAN_POINT('Ctrl Pts',(-0.344281860949048,-0.190269236295522,
-0.0400000000000003));
#50308=CARTESIAN_POINT('Ctrl Pts',(-0.339556668524804,-0.197160576599915,
-0.0399999999999999));
#50309=CARTESIAN_POINT('Ctrl Pts',(-0.334595493859032,-0.203875367646479,
-0.0399999999999998));
#50310=CARTESIAN_POINT('Ctrl Pts',(-0.325338386804792,-0.216404565619235,
-0.0399999999999996));
#50311=CARTESIAN_POINT('Ctrl Pts',(-0.315260129136267,-0.228319778085478,
-0.04));
#50312=CARTESIAN_POINT('Ctrl Pts',(-0.304447112191422,-0.239582838373425,
-0.04));
#50313=CARTESIAN_POINT('Ctrl Pts',(-0.297795698249758,-0.246511087594449,
-0.04));
#50314=CARTESIAN_POINT('Ctrl Pts',(-0.29086607385478,-0.253192358646992,
-0.0400000000000009));
#50315=CARTESIAN_POINT('Ctrl Pts',(-0.283677124011411,-0.25961550153745,
-0.0400000000000011));
#50316=CARTESIAN_POINT('Ctrl Pts',(-0.27883471219124,-0.263942072696393,
-0.0400000000000013));
#50317=CARTESIAN_POINT('Ctrl Pts',(-0.273882118054872,-0.26814477485101,
-0.0399999999999996));
#50318=CARTESIAN_POINT('Ctrl Pts',(-0.268826637302453,-0.272220395003461,
-0.0399999999999996));
#50319=CARTESIAN_POINT('Ctrl Pts',(-0.252040976976963,-0.285752634338373,
-0.0399999999999998));
#50320=CARTESIAN_POINT('Ctrl Pts',(-0.234119262469246,-0.29789035047311,
-0.0399999999999999));
#50321=CARTESIAN_POINT('Ctrl Pts',(-0.215283052615073,-0.308512792785733,
-0.04));
#50322=CARTESIAN_POINT('Ctrl Pts',(-0.210201809912688,-0.311378295341735,
-0.04));
#50323=CARTESIAN_POINT('Ctrl Pts',(-0.205051943084034,-0.314134253626617,
-0.0399999999999998));
#50324=CARTESIAN_POINT('Ctrl Pts',(-0.199844116499647,-0.316774415575878,
-0.0399999999999997));
#50325=CARTESIAN_POINT('Ctrl Pts',(-0.181065974193667,-0.326294190474429,
-0.0399999999999996));
#50326=CARTESIAN_POINT('Ctrl Pts',(-0.161610877978346,-0.33427555732133,
-0.0399999999999996));
#50327=CARTESIAN_POINT('Ctrl Pts',(-0.141687478465979,-0.340616307280008,
-0.0399999999999995));
#50328=CARTESIAN_POINT('Ctrl Pts',(-0.122302515671901,-0.346785696292121,
-0.0399999999999994));
#50329=CARTESIAN_POINT('Ctrl Pts',(-0.102472851443113,-0.351402165887278,
-0.0400000000000007));
#50330=CARTESIAN_POINT('Ctrl Pts',(-0.0823890484208069,-0.354323211780531,
-0.0400000000000007));
#50331=CARTESIAN_POINT('Ctrl Pts',(-0.0767749361799088,-0.355139744360905,
-0.0400000000000007));
#50332=CARTESIAN_POINT('Ctrl Pts',(-0.0711410219815515,-0.355823489525933,
-0.0400000000000009));
#50333=CARTESIAN_POINT('Ctrl Pts',(-0.0654916600524661,-0.356370597325589,
-0.0400000000000009));
#50334=CARTESIAN_POINT('Ctrl Pts',(-0.0604220160106905,-0.356861562824268,
-0.0400000000000009));
#50335=CARTESIAN_POINT('Ctrl Pts',(-0.0553499384085825,-0.357241508756984,
-0.0400000000000003));
#50336=CARTESIAN_POINT('Ctrl Pts',(-0.0502793161526174,-0.357508750027682,
-0.0400000000000003));
#50337=CARTESIAN_POINT('Ctrl Pts',(-0.0364167837107168,-0.358239358737591,
-0.0400000000000004));
#50338=CARTESIAN_POINT('Ctrl Pts',(-0.0225628301172705,-0.358128707187053,
-0.0400000000000002));
#50339=CARTESIAN_POINT('Ctrl Pts',(-0.00877966728186113,-0.357135742011749,
-0.0400000000000002));
#50340=CARTESIAN_POINT('Ctrl Pts',(0.0117257534661439,-0.355658492635037,
-0.0400000000000003));
#50341=CARTESIAN_POINT('Ctrl Pts',(0.0320762654196419,-0.35223025391618,
-0.0399999999999998));
#50342=CARTESIAN_POINT('Ctrl Pts',(0.0520546625937477,-0.346973284194516,
-0.0399999999999998));
#50343=CARTESIAN_POINT('Ctrl Pts',(0.057542659920442,-0.345529212604209,
-0.0399999999999998));
#50344=CARTESIAN_POINT('Ctrl Pts',(0.0630024049445004,-0.343946874059417,
-0.0400000000000005));
#50345=CARTESIAN_POINT('Ctrl Pts',(0.0684289356558515,-0.342228230074204,
-0.0400000000000005));
#50346=CARTESIAN_POINT('Ctrl Pts',(0.0736357693981515,-0.34057916661742,
-0.0400000000000005));
#50347=CARTESIAN_POINT('Ctrl Pts',(0.0788044417638721,-0.338806902750585,
-0.0400000000000001));
#50348=CARTESIAN_POINT('Ctrl Pts',(0.0839245765806507,-0.336916643979113,
-0.0400000000000001));
#50349=CARTESIAN_POINT('Ctrl Pts',(0.103108695538129,-0.329834223216773,
-0.0400000000000002));
#50350=CARTESIAN_POINT('Ctrl Pts',(0.121643544170652,-0.321089833264376,
-0.0400000000000006));
#50351=CARTESIAN_POINT('Ctrl Pts',(0.139316889058501,-0.310813500312407,
-0.0400000000000003));
#50352=CARTESIAN_POINT('Ctrl Pts',(0.153758842758092,-0.302416090221918,
-0.0400000000000001));
#50353=CARTESIAN_POINT('Ctrl Pts',(0.167625439375493,-0.292994385994367,
-0.0399999999999986));
#50354=CARTESIAN_POINT('Ctrl Pts',(0.180778458081028,-0.28259993810822,
-0.0399999999999982));
#50355=CARTESIAN_POINT('Ctrl Pts',(0.18501406420843,-0.27925266185604,-0.0399999999999981));
#50356=CARTESIAN_POINT('Ctrl Pts',(0.189176410882292,-0.275803308569567,
-0.0400000000000001));
#50357=CARTESIAN_POINT('Ctrl Pts',(0.193246995837017,-0.27226575337169,
-0.0400000000000001));
#50358=CARTESIAN_POINT('Ctrl Pts',(0.208094771338353,-0.259362245402719,
-0.0399999999999999));
#50359=CARTESIAN_POINT('Ctrl Pts',(0.22176966298894,-0.245254393801563,
-0.0399999999999998));
#50360=CARTESIAN_POINT('Ctrl Pts',(0.234062004541931,-0.23004354120916,
-0.0399999999999999));
#50361=CARTESIAN_POINT('Ctrl Pts',(0.2454650733056,-0.215933097131644,-0.0399999999999999));
#50362=CARTESIAN_POINT('Ctrl Pts',(0.255678773688448,-0.200872367689583,
-0.0400000000000001));
#50363=CARTESIAN_POINT('Ctrl Pts',(0.264490302733435,-0.184924190981102,
-0.0399999999999997));
#50364=CARTESIAN_POINT('Ctrl Pts',(0.265177473281506,-0.18368046616631,
-0.0399999999999997));
#50365=CARTESIAN_POINT('Ctrl Pts',(0.265856090160851,-0.182431338984764,
-0.04));
#50366=CARTESIAN_POINT('Ctrl Pts',(0.266526038810872,-0.181176836987473,
-0.04));
#50367=CARTESIAN_POINT('Ctrl Pts',(0.142815504361805,0.288902937573994,
-2.88100630286919));
#50368=CARTESIAN_POINT('Ctrl Pts',(0.0466461460635961,0.336443040574824,
-2.87438391055481));
#50369=CARTESIAN_POINT('Ctrl Pts',(-0.195237416096998,0.327094963396398,
-2.86113912592605));
#50370=CARTESIAN_POINT('Ctrl Pts',(-0.381101025730574,0.012353614834551,
-2.84127194898291));
#50371=CARTESIAN_POINT('Ctrl Pts',(-0.216533073052069,-0.313416506212782,
-2.82140477203977));
#50372=CARTESIAN_POINT('Ctrl Pts',(0.146152353759915,-0.351899746021385,
-2.80153759509663));
#50373=CARTESIAN_POINT('Ctrl Pts',(0.375042359224723,-0.0675819005554749,
-2.78167041815349));
#50374=CARTESIAN_POINT('Ctrl Pts',(0.259857122798181,0.278675922139343,
-2.76180324121035));
#50375=CARTESIAN_POINT('Ctrl Pts',(-0.0935766607715254,0.369381537016774,
-2.7419360642672));
#50376=CARTESIAN_POINT('Ctrl Pts',(-0.361225822360449,0.121318076485742,
-2.72206888732406));
#50377=CARTESIAN_POINT('Ctrl Pts',(-0.297578297103382,-0.238000159986643,
-2.70220171038092));
#50378=CARTESIAN_POINT('Ctrl Pts',(0.0389678303295289,-0.379052262416539,
-2.68233453343778));
#50379=CARTESIAN_POINT('Ctrl Pts',(0.339781580148665,-0.172475450822871,
-2.66246735649464));
#50380=CARTESIAN_POINT('Ctrl Pts',(0.32898038540163,0.192277148854254,-2.6426001795515));
#50381=CARTESIAN_POINT('Ctrl Pts',(0.0164738552685434,0.380693518847251,
-2.62273300260836));
#50382=CARTESIAN_POINT('Ctrl Pts',(-0.311141479570281,0.219977088554462,
-2.60286582566522));
#50383=CARTESIAN_POINT('Ctrl Pts',(-0.353409779756908,-0.142479382852879,
-2.58299864872207));
#50384=CARTESIAN_POINT('Ctrl Pts',(-0.0715674996361506,-0.374268611298861,
-2.56313147177894));
#50385=CARTESIAN_POINT('Ctrl Pts',(0.275909162196494,-0.262817483673361,
-2.54326429483579));
#50386=CARTESIAN_POINT('Ctrl Pts',(0.370350525192519,0.0896625461742955,
-2.52339711789266));
#50387=CARTESIAN_POINT('Ctrl Pts',(0.125144851946343,0.359913403121745,
-2.5035299409495));
#50388=CARTESIAN_POINT('Ctrl Pts',(-0.234830704909087,0.300089037511211,
-2.48366276400638));
#50389=CARTESIAN_POINT('Ctrl Pts',(-0.379443904784244,-0.034945844948649,
-2.46379558706322));
#50390=CARTESIAN_POINT('Ctrl Pts',(-0.176070541289752,-0.337932026630971,
-2.44392841012009));
#50391=CARTESIAN_POINT('Ctrl Pts',(0.188776450434642,-0.331002026615422,
-2.42406123317694));
#50392=CARTESIAN_POINT('Ctrl Pts',(0.380497273760583,-0.0205113226115502,
-2.40419405623381));
#50393=CARTESIAN_POINT('Ctrl Pts',(0.223265489718655,0.308790237805464,
-2.38432687929066));
#50394=CARTESIAN_POINT('Ctrl Pts',(-0.13872222919299,0.354901441165425,
-2.36445970234752));
#50395=CARTESIAN_POINT('Ctrl Pts',(-0.373488317233333,0.0755338777360533,
-2.34459252540438));
#50396=CARTESIAN_POINT('Ctrl Pts',(-0.265729684906711,-0.27310551876284,
-2.32472534846124));
#50397=CARTESIAN_POINT('Ctrl Pts',(0.0857286345377398,-0.371280878892406,
-2.3048581715181));
#50398=CARTESIAN_POINT('Ctrl Pts',(0.358565548084728,-0.128955951921072,
-2.28499099457496));
#50399=CARTESIAN_POINT('Ctrl Pts',(0.302563356235795,0.231633989897339,
-2.26512381763181));
#50400=CARTESIAN_POINT('Ctrl Pts',(-0.0309185430950134,0.379793277328495,
-2.24525664068868));
#50401=CARTESIAN_POINT('Ctrl Pts',(-0.33604516371248,0.17964558930402,-2.22538946374553));
#50402=CARTESIAN_POINT('Ctrl Pts',(-0.332986038093936,-0.185254387926107,
-2.20552228680239));
#50403=CARTESIAN_POINT('Ctrl Pts',(-0.0245466787495387,-0.380258267988377,
-2.18565510985925));
#50404=CARTESIAN_POINT('Ctrl Pts',(0.306404346658912,-0.226528731422051,
-2.16578793291611));
#50405=CARTESIAN_POINT('Ctrl Pts',(0.356353106829473,0.134949446327866,
-2.14592075597297));
#50406=CARTESIAN_POINT('Ctrl Pts',(0.0794917830842547,0.372665998225311,
-2.12605357902982));
#50407=CARTESIAN_POINT('Ctrl Pts',(-0.270271153702829,0.26861197532375,
-2.10618640208669));
#50408=CARTESIAN_POINT('Ctrl Pts',(-0.372169439589422,-0.0817850722741498,
-2.08631922514355));
#50409=CARTESIAN_POINT('Ctrl Pts',(-0.132752542720296,-0.357177340004209,
-2.0664520482004));
#50410=CARTESIAN_POINT('Ctrl Pts',(0.228411208027658,-0.305003622697395,
-2.04658487125726));
#50411=CARTESIAN_POINT('Ctrl Pts',(0.380099905430515,0.0268877612103093,
-2.02671769431412));
#50412=CARTESIAN_POINT('Ctrl Pts',(0.183200419906357,0.334120481200005,
-2.00685051737098));
#50413=CARTESIAN_POINT('Ctrl Pts',(-0.181711476497752,0.334932573990939,
-1.98698334042784));
#50414=CARTESIAN_POINT('Ctrl Pts',(-0.379976466379767,0.0285792723618732,
-1.9671161634847));
#50415=CARTESIAN_POINT('Ctrl Pts',(-0.229766478820454,-0.303983971652517,
-1.94724898654156));
#50416=CARTESIAN_POINT('Ctrl Pts',(0.131161475792397,-0.357764667175434,
-1.92738180959841));
#50417=CARTESIAN_POINT('Ctrl Pts',(0.371801737976828,-0.0834407421383482,
-1.90751463265528));
#50418=CARTESIAN_POINT('Ctrl Pts',(0.271464035161107,0.267406371325063,
-1.88764745571213));
#50419=CARTESIAN_POINT('Ctrl Pts',(-0.0778323056202418,0.373016114950851,
-1.86778027876899));
#50420=CARTESIAN_POINT('Ctrl Pts',(-0.355748933853518,0.136534193055344,
-1.84791310182585));
#50421=CARTESIAN_POINT('Ctrl Pts',(-0.307409562917938,-0.225162719911157,
-1.82804592488271));
#50422=CARTESIAN_POINT('Ctrl Pts',(0.0228539532777633,-0.380363755674442,
-1.80817874793957));
#50423=CARTESIAN_POINT('Ctrl Pts',(0.332158195524763,-0.186734632451837,
-1.78831157099643));
#50424=CARTESIAN_POINT('Ctrl Pts',(0.336841415329915,0.178148114583703,
-1.76844439405329));
#50425=CARTESIAN_POINT('Ctrl Pts',(0.0326086495564207,0.379651900805587,
-1.74857721711014));
#50426=CARTESIAN_POINT('Ctrl Pts',(-0.301529385158674,0.23297836744432,
-1.72871004016701));
#50427=CARTESIAN_POINT('Ctrl Pts',(-0.359135963354434,-0.127358743856361,
-1.70884286322386));
#50428=CARTESIAN_POINT('Ctrl Pts',(-0.0873803104607973,-0.370895633777163,
-1.68897568628072));
#50429=CARTESIAN_POINT('Ctrl Pts',(0.264511494039161,-0.27428554342575,
-1.66910850933758));
#50430=CARTESIAN_POINT('Ctrl Pts',(0.373820809690602,0.0738707794290245,
-1.64924133239444));
#50431=CARTESIAN_POINT('Ctrl Pts',(0.140300477324218,0.354280490393961,
-1.6293741554513));
#50432=CARTESIAN_POINT('Ctrl Pts',(-0.22188889114426,0.309780906122309,
-1.60950697850816));
#50433=CARTESIAN_POINT('Ctrl Pts',(-0.380584798365858,-0.0188175732762695,
-1.58963980156501));
#50434=CARTESIAN_POINT('Ctrl Pts',(-0.190247829186885,-0.330158527530134,
-1.56977262462188));
#50435=CARTESIAN_POINT('Ctrl Pts',(0.174564703217894,-0.338712347282523,
-1.54990544767873));
#50436=CARTESIAN_POINT('Ctrl Pts',(0.379284607793692,-0.0366343568522026,
-1.53003827073559));
#50437=CARTESIAN_POINT('Ctrl Pts',(0.236164035815733,0.299040863425743,
-1.51017109379245));
#50438=CARTESIAN_POINT('Ctrl Pts',(-0.123541678493353,0.360466841035667,
-1.49030391684931));
#50439=CARTESIAN_POINT('Ctrl Pts',(-0.36994778760266,0.0913100446779361,
-1.47043673990617));
#50440=CARTESIAN_POINT('Ctrl Pts',(-0.277076182574637,-0.261586847645394,
-1.45056956296303));
#50441=CARTESIAN_POINT('Ctrl Pts',(0.0699009395453964,-0.374583433245331,
-1.43070238601989));
#50442=CARTESIAN_POINT('Ctrl Pts',(0.352772174889632,-0.144050971655273,
-1.41083520907674));
#50443=CARTESIAN_POINT('Ctrl Pts',(0.312117385430717,0.218590090175839,
-1.3909680321336));
#50444=CARTESIAN_POINT('Ctrl Pts',(-0.0147790754750554,0.380763008627795,
-1.37110085519046));
#50445=CARTESIAN_POINT('Ctrl Pts',(-0.328121702266199,0.193739614723267,
-1.35123367824732));
#50446=CARTESIAN_POINT('Ctrl Pts',(-0.340545159287118,-0.170961645690779,
-1.33136650130418));
#50447=CARTESIAN_POINT('Ctrl Pts',(-0.040655941181135,-0.378874628680604,
-1.31149932436104));
#50448=CARTESIAN_POINT('Ctrl Pts',(0.296518686521221,-0.239323125407717,
-1.29163214741789));
#50449=CARTESIAN_POINT('Ctrl Pts',(0.361757150437206,0.119710709290111,
-1.27176497047476));
#50450=CARTESIAN_POINT('Ctrl Pts',(0.0952295025228559,0.368958306127452,
-1.25189779353161));
#50451=CARTESIAN_POINT('Ctrl Pts',(-0.258632761294349,0.279835638538854,
-1.23203061658847));
#50452=CARTESIAN_POINT('Ctrl Pts',(-0.375303899786546,-0.0659232327499082,
-1.21216343964533));
#50453=CARTESIAN_POINT('Ctrl Pts',(-0.147785253953922,-0.351224157091969,
-1.19229626270219));
#50454=CARTESIAN_POINT('Ctrl Pts',(0.21526668826523,-0.314418737887087,
-1.17242908575905));
#50455=CARTESIAN_POINT('Ctrl Pts',(0.38089836640381,0.0107389143816884,
-1.15256190881591));
#50456=CARTESIAN_POINT('Ctrl Pts',(0.197209596082445,0.326047948964853,
-1.13269473187277));
#50457=CARTESIAN_POINT('Ctrl Pts',(-0.167339347503859,0.342339645072217,
-1.11282755492962));
#50458=CARTESIAN_POINT('Ctrl Pts',(-0.378422009606898,0.0446729499391543,
-1.09296037798649));
#50459=CARTESIAN_POINT('Ctrl Pts',(-0.242455280684575,-0.293963138300284,
-1.07309320104334));
#50460=CARTESIAN_POINT('Ctrl Pts',(0.115866267398166,-0.363006746342826,
-1.0532260241002));
#50461=CARTESIAN_POINT('Ctrl Pts',(0.367927300711469,-0.0991382428851851,
-1.03335884715706));
#50462=CARTESIAN_POINT('Ctrl Pts',(0.282563600758959,0.255649567449899,
-1.01349167021392));
#50463=CARTESIAN_POINT('Ctrl Pts',(-0.0619381067084859,0.375982128230261,
-0.99362449327078));
#50464=CARTESIAN_POINT('Ctrl Pts',(-0.349636611220657,0.151502903950139,
-0.973757316327636));
#50465=CARTESIAN_POINT('Ctrl Pts',(-0.316684704488649,-0.211919059440451,
-0.953890139384496));
#50466=CARTESIAN_POINT('Ctrl Pts',(0.00669754469093416,-0.380990856460232,
-0.934022962441355));
#50467=CARTESIAN_POINT('Ctrl Pts',(0.323937501014007,-0.200657382739803,
-0.914155785498214));
#50468=CARTESIAN_POINT('Ctrl Pts',(0.34409560267971,0.163698216324051,-0.894288608555072));
#50469=CARTESIAN_POINT('Ctrl Pts',(0.0486849310371447,0.377926801512009,
-0.874421431611931));
#50470=CARTESIAN_POINT('Ctrl Pts',(-0.291374506373835,0.245560149141897,
-0.854554254668789));
#50471=CARTESIAN_POINT('Ctrl Pts',(-0.364215488118362,-0.112008785485316,
-0.834687077725649));
#50472=CARTESIAN_POINT('Ctrl Pts',(-0.103035825860727,-0.366854887387893,
-0.814819900782507));
#50473=CARTESIAN_POINT('Ctrl Pts',(0.25263760185176,-0.285259762219933,
-0.794952723839366));
#50474=CARTESIAN_POINT('Ctrl Pts',(0.376618042246158,0.0579460099220519,
-0.775085546896225));
#50475=CARTESIAN_POINT('Ctrl Pts',(0.15520350324569,0.348009715944001,-0.755218369953084));
#50476=CARTESIAN_POINT('Ctrl Pts',(-0.208547580455982,0.318915030215117,
-0.735351193009942));
#50477=CARTESIAN_POINT('Ctrl Pts',(-0.381040468388129,-0.00265542123362842,
-0.7154840160668));
#50478=CARTESIAN_POINT('Ctrl Pts',(-0.204082586668139,-0.321790595931231,
-0.695616839123661));
#50479=CARTESIAN_POINT('Ctrl Pts',(0.160038661936921,-0.345812834487786,
-0.675749662180518));
#50480=CARTESIAN_POINT('Ctrl Pts',(0.377389060130195,-0.0526914329514625,
-0.655882485237377));
#50481=CARTESIAN_POINT('Ctrl Pts',(0.248637381342986,0.288753082075454,
-0.636015308294237));
#50482=CARTESIAN_POINT('Ctrl Pts',(-0.108138697680715,0.365383239728838,
-0.616148131351095));
#50483=CARTESIAN_POINT('Ctrl Pts',(-0.36574118686201,0.106921812798457,
-0.596280954407954));
#50484=CARTESIAN_POINT('Ctrl Pts',(-0.287923819462959,-0.249597203472902,
-0.576413777464812));
#50485=CARTESIAN_POINT('Ctrl Pts',(0.0539473916324327,-0.377211570275388,
-0.556546600521672));
#50486=CARTESIAN_POINT('Ctrl Pts',(0.346343654442317,-0.158886635343591,
-0.53667942357853));
#50487=CARTESIAN_POINT('Ctrl Pts',(0.321109463897549,0.205152630716595,
-0.516812246635389));
#50488=CARTESIAN_POINT('Ctrl Pts',(0.00138700138049073,0.381047196669113,
-0.496945069692247));
#50489=CARTESIAN_POINT('Ctrl Pts',(-0.319607475922761,0.207484822257589,
-0.477077892749107));
#50490=CARTESIAN_POINT('Ctrl Pts',(-0.347491146111847,-0.156361095963684,
-0.457210715805965));
#50491=CARTESIAN_POINT('Ctrl Pts',(-0.0566920069213143,-0.376808846437738,
-0.437343538862825));
#50492=CARTESIAN_POINT('Ctrl Pts',(0.286099164537831,-0.251686630090085,
-0.417476361919683));
#50493=CARTESIAN_POINT('Ctrl Pts',(0.366509861887374,0.104256437864189,
-0.397609184976542));
#50494=CARTESIAN_POINT('Ctrl Pts',(0.110795781408782,0.364586327678901,
-0.3777420080334));
#50495=CARTESIAN_POINT('Ctrl Pts',(-0.246528743309069,0.290555466529541,
-0.357874831090259));
#50496=CARTESIAN_POINT('Ctrl Pts',(-0.377762590352976,-0.0499426901134978,
-0.338007654147118));
#50497=CARTESIAN_POINT('Ctrl Pts',(-0.162551991338471,-0.344638636705144,
-0.318140477203977));
#50498=CARTESIAN_POINT('Ctrl Pts',(0.201734794471057,-0.323267715522956,
-0.298273300260835));
#50499=CARTESIAN_POINT('Ctrl Pts',(0.381010653528974,-0.00542935060109167,
-0.278406123317695));
#50500=CARTESIAN_POINT('Ctrl Pts',(0.210864447485707,0.317388544423747,
-0.258538946374552));
#50501=CARTESIAN_POINT('Ctrl Pts',(-0.152667350575211,0.34913004670471,
-0.238671769431413));
#50502=CARTESIAN_POINT('Ctrl Pts',(-0.376183510671294,0.0606867807651417,
-0.21880459248827));
#50503=CARTESIAN_POINT('Ctrl Pts',(-0.254712749740312,-0.2834141590357,
-0.19893741554513));
#50504=CARTESIAN_POINT('Ctrl Pts',(0.100372392813672,-0.367593109417031,
-0.179070238601988));
#50505=CARTESIAN_POINT('Ctrl Pts',(0.363371391885224,-0.114661350979993,
-0.159203061658847));
#50506=CARTESIAN_POINT('Ctrl Pts',(0.29319087692976,0.243440329815534,-0.139335884715706));
#50507=CARTESIAN_POINT('Ctrl Pts',(-0.0460022222542214,0.378256179469882,
-0.119468707772565));
#50508=CARTESIAN_POINT('Ctrl Pts',(-0.34276064692937,0.166227606036299,
-0.099601530829423));
#50509=CARTESIAN_POINT('Ctrl Pts',(-0.32565060598116,-0.198348900769526,
-0.0797343538862829));
#50510=CARTESIAN_POINT('Ctrl Pts',(-0.00893422490495668,-0.380826657875824,
-0.0598671769431404));
#50511=CARTESIAN_POINT('Ctrl Pts',(0.206216301921741,-0.269897423691928,
-0.0466223923143805));
#50512=CARTESIAN_POINT('Ctrl Pts',(0.266526038810872,-0.181176836987473,
-0.04));
#50513=CARTESIAN_POINT('Ctrl Pts',(0.153307031988105,0.310126355608481,
-2.86733753524613));
#50514=CARTESIAN_POINT('Ctrl Pts',(0.0500728701596497,0.361158854664061,
-2.86071514293175));
#50515=CARTESIAN_POINT('Ctrl Pts',(-0.209579967725564,0.351124048055182,
-2.84747035830299));
#50516=CARTESIAN_POINT('Ctrl Pts',(-0.409097509429811,0.0132611373889164,
-2.82760318135985));
#50517=CARTESIAN_POINT('Ctrl Pts',(-0.232440048475256,-0.336440742608989,
-2.80773600441671));
#50518=CARTESIAN_POINT('Ctrl Pts',(0.156889013368218,-0.377751042234421,
-2.78786882747356));
#50519=CARTESIAN_POINT('Ctrl Pts',(0.402593760526857,-0.0725466092534843,
-2.76800165053042));
#50520=CARTESIAN_POINT('Ctrl Pts',(0.278946774127782,0.299148042088607,
-2.74813447358728));
#50521=CARTESIAN_POINT('Ctrl Pts',(-0.100450999282939,0.39651708240153,
-2.72826729664414));
#50522=CARTESIAN_POINT('Ctrl Pts',(-0.387762231775959,0.130230357800768,
-2.708400119701));
#50523=CARTESIAN_POINT('Ctrl Pts',(-0.319439025313521,-0.255484152811664,
-2.68853294275786));
#50524=CARTESIAN_POINT('Ctrl Pts',(0.0418304891862556,-0.406898239649373,
-2.66866576581472));
#50525=CARTESIAN_POINT('Ctrl Pts',(0.364742650383773,-0.185145860560615,
-2.64879858887157));
#50526=CARTESIAN_POINT('Ctrl Pts',(0.353147977130382,0.206402233018786,
-2.62893141192844));
#50527=CARTESIAN_POINT('Ctrl Pts',(0.0176840593597166,0.408660066232896,
-2.60906423498529));
#50528=CARTESIAN_POINT('Ctrl Pts',(-0.333998587719615,0.236137068607296,
-2.58919705804216));
#50529=CARTESIAN_POINT('Ctrl Pts',(-0.379372006227298,-0.152946218285481,
-2.56932988109901));
#50530=CARTESIAN_POINT('Ctrl Pts',(-0.0768249988336868,-0.401763171449355,
-2.54946270415587));
#50531=CARTESIAN_POINT('Ctrl Pts',(0.296178030135373,-0.282124609345433,
-2.52959552721273));
#50532=CARTESIAN_POINT('Ctrl Pts',(0.397557254488719,0.0962493455868358,
-2.50972835026959));
#50533=CARTESIAN_POINT('Ctrl Pts',(0.134338256243387,0.386353399456885,
-2.48986117332645));
#50534=CARTESIAN_POINT('Ctrl Pts',(-0.252081862891316,0.322134209997684,
-2.4699939963833));
#50535=CARTESIAN_POINT('Ctrl Pts',(-0.407318652889952,-0.0375130402916304,
-2.45012681944016));
#50536=CARTESIAN_POINT('Ctrl Pts',(-0.189005053942099,-0.362757224770722,
-2.43025964249702));
#50537=CARTESIAN_POINT('Ctrl Pts',(0.202644365923092,-0.355318132363991,
-2.41039246555388));
#50538=CARTESIAN_POINT('Ctrl Pts',(0.408449404568997,-0.0220181275540013,
-2.39052528861074));
#50539=CARTESIAN_POINT('Ctrl Pts',(0.239667042644229,0.331474618784579,
-2.3706581116676));
#50540=CARTESIAN_POINT('Ctrl Pts',(-0.148913056207633,0.380973248223346,
-2.35079093472446));
#50541=CARTESIAN_POINT('Ctrl Pts',(-0.400925555338986,0.0810827554194012,
-2.33092375778132));
#50542=CARTESIAN_POINT('Ctrl Pts',(-0.285250747012572,-0.293168425152445,
-2.31105658083817));
#50543=CARTESIAN_POINT('Ctrl Pts',(0.0920264405192182,-0.398555953930116,
-2.29118940389504));
#50544=CARTESIAN_POINT('Ctrl Pts',(0.384906528151149,-0.138429327645939,
-2.27132222695189));
#50545=CARTESIAN_POINT('Ctrl Pts',(0.32479029738507,0.248650310464616,-2.25145505000875));
#50546=CARTESIAN_POINT('Ctrl Pts',(-0.0331898843649674,0.407693691076853,
-2.23158787306561));
#50547=CARTESIAN_POINT('Ctrl Pts',(-0.360731748929741,0.192842732510204,
-2.21172069612247));
#50548=CARTESIAN_POINT('Ctrl Pts',(-0.357447893502745,-0.198863565287524,
-2.19185351917933));
#50549=CARTESIAN_POINT('Ctrl Pts',(-0.0263499294497031,-0.408192840929575,
-2.17198634223618));
#50550=CARTESIAN_POINT('Ctrl Pts',(0.328913455051278,-0.243170008953405,
-2.15211916529305));
#50551=CARTESIAN_POINT('Ctrl Pts',(0.382531556303331,0.144863116770228,
-2.13225198834991));
#50552=CARTESIAN_POINT('Ctrl Pts',(0.0853314168272379,0.400042827045369,
-2.11238481140676));
#50553=CARTESIAN_POINT('Ctrl Pts',(-0.290125841667811,0.288344776551862,
-2.09251763446363));
#50554=CARTESIAN_POINT('Ctrl Pts',(-0.39950979016666,-0.0877931758691862,
-2.07265045752048));
#50555=CARTESIAN_POINT('Ctrl Pts',(-0.142504823998407,-0.38341633938238,
-2.05278328057734));
#50556=CARTESIAN_POINT('Ctrl Pts',(0.245190776253722,-0.32740983095854,
-2.03291610363419));
#50557=CARTESIAN_POINT('Ctrl Pts',(0.408022844724805,0.0288629927568269,
-2.01304892669106));
#50558=CARTESIAN_POINT('Ctrl Pts',(0.196658708452732,0.358665675187779,
-1.99318174974791));
#50559=CARTESIAN_POINT('Ctrl Pts',(-0.195060384126591,0.359537426024871,
-1.97331457280478));
#50560=CARTESIAN_POINT('Ctrl Pts',(-0.407890337581508,0.0306787658787993,
-1.95344739586163));
#50561=CARTESIAN_POINT('Ctrl Pts',(-0.246645608092269,-0.326315274201189,
-1.93358021891849));
#50562=CARTESIAN_POINT('Ctrl Pts',(0.140796873944239,-0.384046812844128,
-1.91371304197535));
#50563=CARTESIAN_POINT('Ctrl Pts',(0.399115076419467,-0.0895704747273649,
-1.89384586503221));
#50564=CARTESIAN_POINT('Ctrl Pts',(0.29140635470944,0.287050606345219,-1.87397868808907));
#50565=CARTESIAN_POINT('Ctrl Pts',(-0.0835500306549455,0.400418664082683,
-1.85411151114593));
#50566=CARTESIAN_POINT('Ctrl Pts',(-0.381882999508571,0.146564282328745,
-1.83424433420279));
#50567=CARTESIAN_POINT('Ctrl Pts',(-0.329992516613019,-0.241703647360996,
-1.81437715725964));
#50568=CARTESIAN_POINT('Ctrl Pts',(0.0245328528009995,-0.408306077963147,
-1.7945099803165));
#50569=CARTESIAN_POINT('Ctrl Pts',(0.356559235875546,-0.200452551692539,
-1.77464280337336));
#50570=CARTESIAN_POINT('Ctrl Pts',(0.361586494867377,0.191235250144231,
-1.75477562643022));
#50571=CARTESIAN_POINT('Ctrl Pts',(0.0350041496052865,0.407541928736926,
-1.73490844948708));
#50572=CARTESIAN_POINT('Ctrl Pts',(-0.323680368615757,0.250093448816577,
-1.71504127254394));
#50573=CARTESIAN_POINT('Ctrl Pts',(-0.385518847327489,-0.13671478531412,
-1.6951740956008));
#50574=CARTESIAN_POINT('Ctrl Pts',(-0.0937994520329311,-0.398142407897633,
-1.67530691865766));
#50575=CARTESIAN_POINT('Ctrl Pts',(0.28394306527918,-0.294435136911452,
-1.65543974171452));
#50576=CARTESIAN_POINT('Ctrl Pts',(0.401282473392177,0.0792974824093426,
-1.63557256477137));
#50577=CARTESIAN_POINT('Ctrl Pts',(0.150607245769338,0.380306681100895,
-1.61570538782823));
#50578=CARTESIAN_POINT('Ctrl Pts',(-0.238189316240343,0.332538063681678,
-1.59583821088509));
#50579=CARTESIAN_POINT('Ctrl Pts',(-0.408543358916046,-0.0201999518266245,
-1.57597103394195));
#50580=CARTESIAN_POINT('Ctrl Pts',(-0.204223835256235,-0.354412668060041,
-1.55610385699881));
#50581=CARTESIAN_POINT('Ctrl Pts',(0.187388593835173,-0.363594869420182,
-1.53623668005567));
#50582=CARTESIAN_POINT('Ctrl Pts',(0.407147653607099,-0.0393255938345184,
-1.51636950311253));
#50583=CARTESIAN_POINT('Ctrl Pts',(0.253513143093484,0.321009034837128,
-1.49650232616938));
#50584=CARTESIAN_POINT('Ctrl Pts',(-0.132617310293307,0.386947494085143,
-1.47663514922625));
#50585=CARTESIAN_POINT('Ctrl Pts',(-0.397124930947607,0.0980178727991059,
-1.4567679722831));
#50586=CARTESIAN_POINT('Ctrl Pts',(-0.297430782287474,-0.280803568203938,
-1.43690079533996));
#50587=CARTESIAN_POINT('Ctrl Pts',(0.0750360097299817,-0.402101120878822,
-1.41703361839682));
#50588=CARTESIAN_POINT('Ctrl Pts',(0.378687561564093,-0.154633259310036,
-1.39716644145368));
#50589=CARTESIAN_POINT('Ctrl Pts',(0.335046185679176,0.234648178407669,
-1.37729926451054));
#50590=CARTESIAN_POINT('Ctrl Pts',(-0.015864777474503,0.408734660879019,
-1.3574320875674));
#50591=CARTESIAN_POINT('Ctrl Pts',(-0.352226213323998,0.207972134709531,
-1.33756491062425));
#50592=CARTESIAN_POINT('Ctrl Pts',(-0.365562323653335,-0.183520848116438,
-1.31769773368112));
#50593=CARTESIAN_POINT('Ctrl Pts',(-0.0436426122150763,-0.406707556565216,
-1.29783055673797));
#50594=CARTESIAN_POINT('Ctrl Pts',(0.318301573507149,-0.256904306057869,
-1.27796337979483));
#50595=CARTESIAN_POINT('Ctrl Pts',(0.388332592331863,0.128504910026883,
-1.25809620285169));
#50596=CARTESIAN_POINT('Ctrl Pts',(0.102225262269124,0.396062760080031,
-1.23822902590855));
#50597=CARTESIAN_POINT('Ctrl Pts',(-0.277632468450175,0.300392953696429,
-1.21836184896541));
#50598=CARTESIAN_POINT('Ctrl Pts',(-0.402874514408985,-0.0707660922188523,
-1.19849467202227));
#50599=CARTESIAN_POINT('Ctrl Pts',(-0.158641869848295,-0.377025823119903,
-1.17862749507913));
#50600=CARTESIAN_POINT('Ctrl Pts',(0.231080632395799,-0.337516600332132,
-1.15876031813598));
#50601=CARTESIAN_POINT('Ctrl Pts',(0.408879962322234,0.0115278176412847,
-1.13889314119284));
#50602=CARTESIAN_POINT('Ctrl Pts',(0.211697028204861,0.350000117739169,
-1.1190259642497));
#50603=CARTESIAN_POINT('Ctrl Pts',(-0.179632448278519,0.367488636142218,
-1.09915878730656));
#50604=CARTESIAN_POINT('Ctrl Pts',(-0.406221687141436,0.0479547188936482,
-1.07929161036342));
#50605=CARTESIAN_POINT('Ctrl Pts',(-0.260266556055632,-0.315558289333592,
-1.05942443342028));
#50606=CARTESIAN_POINT('Ctrl Pts',(0.12437804733968,-0.389673986183541,
-1.03955725647714));
#50607=CARTESIAN_POINT('Ctrl Pts',(0.394956014835567,-0.106421146927716,
-1.019690079534));
#50608=CARTESIAN_POINT('Ctrl Pts',(0.303321317764523,0.274430122905259,
-0.999822902590855));
#50609=CARTESIAN_POINT('Ctrl Pts',(-0.0664882104283629,0.40360256694208,
-0.979955725647714));
#50610=CARTESIAN_POINT('Ctrl Pts',(-0.375321652786552,0.162632626240169,
-0.960088548704573));
#50611=CARTESIAN_POINT('Ctrl Pts',(-0.339949029610886,-0.227487079709639,
-0.94022137176143));
#50612=CARTESIAN_POINT('Ctrl Pts',(0.00718956042457087,-0.408979246892924,
-0.920354194818291));
#50613=CARTESIAN_POINT('Ctrl Pts',(0.347734631838634,-0.215398096528849,
-0.900487017875149));
#50614=CARTESIAN_POINT('Ctrl Pts',(0.369373590092455,0.175723831936406,
-0.880619840932009));
#50615=CARTESIAN_POINT('Ctrl Pts',(0.0522614285697006,0.405690100017313,
-0.860752663988866));
#50616=CARTESIAN_POINT('Ctrl Pts',(-0.312779491055863,0.263599514686647,
-0.840885487045725));
#50617=CARTESIAN_POINT('Ctrl Pts',(-0.390971524674726,-0.120237186684183,
-0.821018310102585));
#50618=CARTESIAN_POINT('Ctrl Pts',(-0.110605054554397,-0.393804819771442,
-0.801151133159443));
#50619=CARTESIAN_POINT('Ctrl Pts',(0.271196891973055,-0.306215544922771,
-0.781283956216301));
#50620=CARTESIAN_POINT('Ctrl Pts',(0.404285196540403,0.0622028458072574,
-0.761416779273161));
#50621=CARTESIAN_POINT('Ctrl Pts',(0.166605079351009,0.373575242357697,
-0.741549602330019));
#50622=CARTESIAN_POINT('Ctrl Pts',(-0.223867924780845,0.342343199760824,
-0.721682425386878));
#50623=CARTESIAN_POINT('Ctrl Pts',(-0.409032503417495,-0.00285049406802788,
-0.701815248443737));
#50624=CARTESIAN_POINT('Ctrl Pts',(-0.219074923148997,-0.345430010588501,
-0.681948071500596));
#50625=CARTESIAN_POINT('Ctrl Pts',(0.171795438979374,-0.371216973364516,
-0.662080894557454));
#50626=CARTESIAN_POINT('Ctrl Pts',(0.40511285502146,-0.0565622565497122,
-0.642213717614313));
#50627=CARTESIAN_POINT('Ctrl Pts',(0.266902806843863,0.30996549140952,-0.622346540671173));
#50628=CARTESIAN_POINT('Ctrl Pts',(-0.116082794081587,0.392225061777027,
-0.60247936372803));
#50629=CARTESIAN_POINT('Ctrl Pts',(-0.392609304460204,0.114776514273916,
-0.58261218678489));
#50630=CARTESIAN_POINT('Ctrl Pts',(-0.309075309419628,-0.267933139528199,
-0.562745009841748));
#50631=CARTESIAN_POINT('Ctrl Pts',(0.0579104805996126,-0.404922326388242,
-0.542877832898608));
#50632=CARTESIAN_POINT('Ctrl Pts',(0.371786788470466,-0.170558782087086,
-0.523010655955466));
#50633=CARTESIAN_POINT('Ctrl Pts',(0.344698841161608,0.220223574886063,
-0.503143479012324));
#50634=CARTESIAN_POINT('Ctrl Pts',(0.00148889342201763,0.409039725972165,
-0.483276302069184));
#50635=CARTESIAN_POINT('Ctrl Pts',(-0.343086513987988,0.222727094127726,
-0.463409125126042));
#50636=CARTESIAN_POINT('Ctrl Pts',(-0.373018577293906,-0.167847711267199,
-0.443541948182901));
#50637=CARTESIAN_POINT('Ctrl Pts',(-0.0608567211059766,-0.404490017609605,
-0.42367477123976));
#50638=CARTESIAN_POINT('Ctrl Pts',(0.307116611502172,-0.270176059823644,
-0.403807594296618));
#50639=CARTESIAN_POINT('Ctrl Pts',(0.393434447971258,0.111915335285443,
-0.383940417353478));
#50640=CARTESIAN_POINT('Ctrl Pts',(0.118935072774395,0.391369606890128,
-0.364073240410336));
#50641=CARTESIAN_POINT('Ctrl Pts',(-0.264639263820565,0.311900282820246,
-0.344206063467195));
#50642=CARTESIAN_POINT('Ctrl Pts',(-0.405513825560816,-0.0536115852758187,
-0.324338886524054));
#50643=CARTESIAN_POINT('Ctrl Pts',(-0.174493402850188,-0.36995651654067,
-0.304471709580912));
#50644=CARTESIAN_POINT('Ctrl Pts',(0.216554657194204,-0.347015642495281,
-0.284604532637771));
#50645=CARTESIAN_POINT('Ctrl Pts',(0.409000498296016,-0.00582820212690324,
-0.26473735569463));
#50646=CARTESIAN_POINT('Ctrl Pts',(0.226354993740378,0.340704575109441,
-0.244870178751488));
#50647=CARTESIAN_POINT('Ctrl Pts',(-0.163882615565881,0.374777874974771,
-0.225003001808348));
#50648=CARTESIAN_POINT('Ctrl Pts',(-0.40381874336121,0.0651449594467487,
-0.205135824865206));
#50649=CARTESIAN_POINT('Ctrl Pts',(-0.273424484594403,-0.304234359842993,
-0.185268647922065));
#50650=CARTESIAN_POINT('Ctrl Pts',(0.107745960108261,-0.394597273145052,
-0.165401470978924));
#50651=CARTESIAN_POINT('Ctrl Pts',(0.390065419355187,-0.123084615224664,
-0.145534294035782));
#50652=CARTESIAN_POINT('Ctrl Pts',(0.314729296016912,0.261323968969618,
-0.125667117092642));
#50653=CARTESIAN_POINT('Ctrl Pts',(-0.0493816423515566,0.406043674773425,
-0.1057999401495));
#50654=CARTESIAN_POINT('Ctrl Pts',(-0.367940565682151,0.178439035942154,
-0.0859327632063587));
#50655=CARTESIAN_POINT('Ctrl Pts',(-0.349573585103351,-0.212920028612885,
-0.0660655862632184));
#50656=CARTESIAN_POINT('Ctrl Pts',(-0.00959055187609898,-0.408802985934812,
-0.0461984093200761));
#50657=CARTESIAN_POINT('Ctrl Pts',(0.221365385617334,-0.289724656663478,
-0.0329536246913161));
#50658=CARTESIAN_POINT('Ctrl Pts',(0.286105602751133,-0.194486468872287,
-0.0263312323769356));
#50659=CARTESIAN_POINT('Ctrl Pts',(0.163798559614405,0.331349773642968,
-2.85366876762306));
#50660=CARTESIAN_POINT('Ctrl Pts',(0.0534995942557033,0.385874668753298,
-2.84704637530868));
#50661=CARTESIAN_POINT('Ctrl Pts',(-0.223922519354131,0.375153132713966,
-2.83380159067992));
#50662=CARTESIAN_POINT('Ctrl Pts',(-0.437093993129047,0.0141686599432813,
-2.81393441373678));
#50663=CARTESIAN_POINT('Ctrl Pts',(-0.248347023898443,-0.359464979005196,
-2.79406723679364));
#50664=CARTESIAN_POINT('Ctrl Pts',(0.167625672976521,-0.403602338447458,
-2.7742000598505));
#50665=CARTESIAN_POINT('Ctrl Pts',(0.430145161828992,-0.0775113179514932,
-2.75433288290736));
#50666=CARTESIAN_POINT('Ctrl Pts',(0.298036425457382,0.31962016203787,-2.73446570596421));
#50667=CARTESIAN_POINT('Ctrl Pts',(-0.107325337794352,0.423652627786286,
-2.71459852902108));
#50668=CARTESIAN_POINT('Ctrl Pts',(-0.41429864119147,0.139142639115794,
-2.69473135207794));
#50669=CARTESIAN_POINT('Ctrl Pts',(-0.34129975352366,-0.272968145636686,
-2.67486417513479));
#50670=CARTESIAN_POINT('Ctrl Pts',(0.0446931480429821,-0.434744216882207,
-2.65499699819165));
#50671=CARTESIAN_POINT('Ctrl Pts',(0.389703720618882,-0.197816270298359,
-2.63512982124851));
#50672=CARTESIAN_POINT('Ctrl Pts',(0.377315568859134,0.220527317183318,
-2.61526264430537));
#50673=CARTESIAN_POINT('Ctrl Pts',(0.0188942634508897,0.43662661361854,
-2.59539546736223));
#50674=CARTESIAN_POINT('Ctrl Pts',(-0.356855695868948,0.252297048660129,
-2.57552829041909));
#50675=CARTESIAN_POINT('Ctrl Pts',(-0.405334232697688,-0.163413053718083,
-2.55566111347595));
#50676=CARTESIAN_POINT('Ctrl Pts',(-0.0820824980312227,-0.42925773159985,
-2.5357939365328));
#50677=CARTESIAN_POINT('Ctrl Pts',(0.316446898074251,-0.301431735017504,
-2.51592675958967));
#50678=CARTESIAN_POINT('Ctrl Pts',(0.424763983784919,0.102836144999376,
-2.49605958264652));
#50679=CARTESIAN_POINT('Ctrl Pts',(0.14353166054043,0.412793395792026,-2.47619240570339));
#50680=CARTESIAN_POINT('Ctrl Pts',(-0.269333020873544,0.344179382484156,
-2.45632522876024));
#50681=CARTESIAN_POINT('Ctrl Pts',(-0.43519340099566,-0.0400802356346113,
-2.4364580518171));
#50682=CARTESIAN_POINT('Ctrl Pts',(-0.201939566594445,-0.387582422910473,
-2.41659087487396));
#50683=CARTESIAN_POINT('Ctrl Pts',(0.216512281411541,-0.379634238112561,
-2.39672369793082));
#50684=CARTESIAN_POINT('Ctrl Pts',(0.436401535377412,-0.0235249324964524,
-2.37685652098768));
#50685=CARTESIAN_POINT('Ctrl Pts',(0.256068595569802,0.354158999763693,
-2.35698934404454));
#50686=CARTESIAN_POINT('Ctrl Pts',(-0.159103883222276,0.407045055281267,
-2.33712216710139));
#50687=CARTESIAN_POINT('Ctrl Pts',(-0.428362793444638,0.0866316331027495,
-2.31725499015825));
#50688=CARTESIAN_POINT('Ctrl Pts',(-0.304771809118433,-0.31323133154205,
-2.29738781321512));
#50689=CARTESIAN_POINT('Ctrl Pts',(0.0983242465006967,-0.425831028967825,
-2.27752063627196));
#50690=CARTESIAN_POINT('Ctrl Pts',(0.41124750821757,-0.147902703370805,
-2.25765345932883));
#50691=CARTESIAN_POINT('Ctrl Pts',(0.347017238534345,0.265666631031894,
-2.23778628238569));
#50692=CARTESIAN_POINT('Ctrl Pts',(-0.0354612256349216,0.435594104825211,
-2.21791910544254));
#50693=CARTESIAN_POINT('Ctrl Pts',(-0.385418334147002,0.206039875716387,
-2.19805192849941));
#50694=CARTESIAN_POINT('Ctrl Pts',(-0.381909748911555,-0.21247274264894,
-2.17818475155626));
#50695=CARTESIAN_POINT('Ctrl Pts',(-0.0281531801498664,-0.436127413870774,
-2.15831757461312));
#50696=CARTESIAN_POINT('Ctrl Pts',(0.351422563443643,-0.259811286484759,
-2.13845039766998));
#50697=CARTESIAN_POINT('Ctrl Pts',(0.40871000577719,0.15477678721259,-2.11858322072684));
#50698=CARTESIAN_POINT('Ctrl Pts',(0.0911710505702201,0.427419655865427,
-2.0987160437837));
#50699=CARTESIAN_POINT('Ctrl Pts',(-0.309980529632792,0.308077577779974,
-2.07884886684056));
#50700=CARTESIAN_POINT('Ctrl Pts',(-0.4268501407439,-0.0938012794642228,
-2.05898168989742));
#50701=CARTESIAN_POINT('Ctrl Pts',(-0.152257105276517,-0.409655338760549,
-2.03911451295427));
#50702=CARTESIAN_POINT('Ctrl Pts',(0.261970344479786,-0.349816039219687,
-2.01924733601114));
#50703=CARTESIAN_POINT('Ctrl Pts',(0.435945784019096,0.0308382243033446,
-1.99938015906799));
#50704=CARTESIAN_POINT('Ctrl Pts',(0.210116996999107,0.383210869175555,
-1.97951298212485));
#50705=CARTESIAN_POINT('Ctrl Pts',(-0.20840929175543,0.384142278058803,
-1.95964580518171));
#50706=CARTESIAN_POINT('Ctrl Pts',(-0.435804208783249,0.0327782593957259,
-1.93977862823857));
#50707=CARTESIAN_POINT('Ctrl Pts',(-0.263524737364084,-0.348646576749862,
-1.91991145129543));
#50708=CARTESIAN_POINT('Ctrl Pts',(0.150432272096081,-0.410328958512822,
-1.90004427435229));
#50709=CARTESIAN_POINT('Ctrl Pts',(0.426428414862106,-0.0957002073163822,
-1.88017709740915));
#50710=CARTESIAN_POINT('Ctrl Pts',(0.311348674257774,0.306694841365375,
-1.860309920466));
#50711=CARTESIAN_POINT('Ctrl Pts',(-0.0892677556896494,0.427821213214516,
-1.84044274352286));
#50712=CARTESIAN_POINT('Ctrl Pts',(-0.408017065163623,0.156594371602146,
-1.82057556657972));
#50713=CARTESIAN_POINT('Ctrl Pts',(-0.3525754703081,-0.258244574810834,
-1.80070838963658));
#50714=CARTESIAN_POINT('Ctrl Pts',(0.026211752324236,-0.436248400251852,
-1.78084121269344));
#50715=CARTESIAN_POINT('Ctrl Pts',(0.380960276226329,-0.214170470933241,
-1.7609740357503));
#50716=CARTESIAN_POINT('Ctrl Pts',(0.38633157440484,0.204322385704759,-1.74110685880715));
#50717=CARTESIAN_POINT('Ctrl Pts',(0.0373996496541524,0.435431956668264,
-1.72123968186402));
#50718=CARTESIAN_POINT('Ctrl Pts',(-0.34583135207284,0.267208530188836,
-1.70137250492087));
#50719=CARTESIAN_POINT('Ctrl Pts',(-0.411901731300545,-0.14607082677188,
-1.68150532797773));
#50720=CARTESIAN_POINT('Ctrl Pts',(-0.100218593605065,-0.425389182018102,
-1.66163815103459));
#50721=CARTESIAN_POINT('Ctrl Pts',(0.303374636519199,-0.314584730397155,
-1.64177097409145));
#50722=CARTESIAN_POINT('Ctrl Pts',(0.428744137093751,0.0847241853896615,
-1.62190379714831));
#50723=CARTESIAN_POINT('Ctrl Pts',(0.160914014214458,0.406332871807828,
-1.60203662020517));
#50724=CARTESIAN_POINT('Ctrl Pts',(-0.254489741336427,0.355295221241048,
-1.58216944326203));
#50725=CARTESIAN_POINT('Ctrl Pts',(-0.436501919466233,-0.0215823303769795,
-1.56230226631889));
#50726=CARTESIAN_POINT('Ctrl Pts',(-0.218199841325584,-0.378666808589948,
-1.54243508937574));
#50727=CARTESIAN_POINT('Ctrl Pts',(0.200212484452452,-0.38847739155784,
-1.5225679124326));
#50728=CARTESIAN_POINT('Ctrl Pts',(0.435010699420506,-0.0420168308168348,
-1.50270073548946));
#50729=CARTESIAN_POINT('Ctrl Pts',(0.270862250371236,0.342977206248515,
-1.48283355854632));
#50730=CARTESIAN_POINT('Ctrl Pts',(-0.14169294209326,0.413428147134617,
-1.46296638160318));
#50731=CARTESIAN_POINT('Ctrl Pts',(-0.424302074292555,0.104725700920277,
-1.44309920466004));
#50732=CARTESIAN_POINT('Ctrl Pts',(-0.317785382000311,-0.300020288762482,
-1.4232320277169));
#50733=CARTESIAN_POINT('Ctrl Pts',(0.0801710799145669,-0.429618808512312,
-1.40336485077376));
#50734=CARTESIAN_POINT('Ctrl Pts',(0.404602948238555,-0.165215546964798,
-1.38349767383061));
#50735=CARTESIAN_POINT('Ctrl Pts',(0.357974985927635,0.250706266639499,
-1.36363049688747));
#50736=CARTESIAN_POINT('Ctrl Pts',(-0.0169504794739499,0.436706313130243,
-1.34376331994433));
#50737=CARTESIAN_POINT('Ctrl Pts',(-0.376330724381798,0.222204654695795,
-1.32389614300119));
#50738=CARTESIAN_POINT('Ctrl Pts',(-0.390579488019552,-0.196080050542096,
-1.30402896605805));
#50739=CARTESIAN_POINT('Ctrl Pts',(-0.0466292832490179,-0.434540484449828,
-1.28416178911491));
#50740=CARTESIAN_POINT('Ctrl Pts',(0.340084460493077,-0.274485486708021,
-1.26429461217177));
#50741=CARTESIAN_POINT('Ctrl Pts',(0.414908034226521,0.137299110763656,
-1.24442743522863));
#50742=CARTESIAN_POINT('Ctrl Pts',(0.109221022015393,0.42316721403261,-1.22456025828548));
#50743=CARTESIAN_POINT('Ctrl Pts',(-0.296632175606001,0.320950268854004,
-1.20469308134235));
#50744=CARTESIAN_POINT('Ctrl Pts',(-0.430445129031423,-0.0756089516877968,
-1.1848259043992));
#50745=CARTESIAN_POINT('Ctrl Pts',(-0.169498485742669,-0.402827489147836,
-1.16495872745606));
#50746=CARTESIAN_POINT('Ctrl Pts',(0.246894576526369,-0.360614462777177,
-1.14509155051292));
#50747=CARTESIAN_POINT('Ctrl Pts',(0.436861558240658,0.0123167209008815,
-1.12522437356978));
#50748=CARTESIAN_POINT('Ctrl Pts',(0.226184460327279,0.373952286513485,
-1.10535719662664));
#50749=CARTESIAN_POINT('Ctrl Pts',(-0.19192554905318,0.39263762721222,-1.0854900196835));
#50750=CARTESIAN_POINT('Ctrl Pts',(-0.434021364675974,0.051236487848142,
-1.06562284274036));
#50751=CARTESIAN_POINT('Ctrl Pts',(-0.278077831426689,-0.337153440366899,
-1.04575566579721));
#50752=CARTESIAN_POINT('Ctrl Pts',(0.132889827281194,-0.416341226024256,
-1.02588848885407));
#50753=CARTESIAN_POINT('Ctrl Pts',(0.421984728959667,-0.113704050970247,
-1.00602131191093));
#50754=CARTESIAN_POINT('Ctrl Pts',(0.324079034770088,0.293210678360619,
-0.986154134967789));
#50755=CARTESIAN_POINT('Ctrl Pts',(-0.0710383141482399,0.431223005653899,
-0.966286958024651));
#50756=CARTESIAN_POINT('Ctrl Pts',(-0.401006694352448,0.173762348530199,
-0.946419781081507));
#50757=CARTESIAN_POINT('Ctrl Pts',(-0.363213354733123,-0.243055099978827,
-0.926552604138367));
#50758=CARTESIAN_POINT('Ctrl Pts',(0.00768157615820771,-0.436967637325617,
-0.906685427195226));
#50759=CARTESIAN_POINT('Ctrl Pts',(0.371531762663261,-0.230138810317896,
-0.886818250252084));
#50760=CARTESIAN_POINT('Ctrl Pts',(0.394651577505199,0.187749447548761,
-0.866951073308945));
#50761=CARTESIAN_POINT('Ctrl Pts',(0.0558379261022568,0.433453398522617,
-0.847083896365802));
#50762=CARTESIAN_POINT('Ctrl Pts',(-0.334184475737891,0.281638880231398,
-0.82721671942266));
#50763=CARTESIAN_POINT('Ctrl Pts',(-0.41772756123109,-0.128465587883049,
-0.80734954247952));
#50764=CARTESIAN_POINT('Ctrl Pts',(-0.118174283248069,-0.420754752154992,
-0.787482365536378));
#50765=CARTESIAN_POINT('Ctrl Pts',(0.289756182094351,-0.327171327625608,
-0.767615188593237));
#50766=CARTESIAN_POINT('Ctrl Pts',(0.431952350834647,0.0664596816924623,
-0.747748011650097));
#50767=CARTESIAN_POINT('Ctrl Pts',(0.178006655456329,0.399140768771395,
-0.727880834706954));
#50768=CARTESIAN_POINT('Ctrl Pts',(-0.239188269105709,0.365771369306532,
-0.708013657763814));
#50769=CARTESIAN_POINT('Ctrl Pts',(-0.437024538446861,-0.00304556690242747,
-0.688146480820672));
#50770=CARTESIAN_POINT('Ctrl Pts',(-0.234067259629854,-0.369069425245772,
-0.668279303877532));
#50771=CARTESIAN_POINT('Ctrl Pts',(0.183552216021828,-0.396621112241247,
-0.64841212693439));
#50772=CARTESIAN_POINT('Ctrl Pts',(0.432836649912724,-0.0604330801479618,
-0.628544949991249));
#50773=CARTESIAN_POINT('Ctrl Pts',(0.28516823234474,0.331177900743587,-0.608677773048107));
#50774=CARTESIAN_POINT('Ctrl Pts',(-0.124026890482458,0.419066883825217,
-0.588810596104966));
#50775=CARTESIAN_POINT('Ctrl Pts',(-0.419477422058399,0.122631215749375,
-0.568943419161825));
#50776=CARTESIAN_POINT('Ctrl Pts',(-0.330226799376297,-0.286269075583497,
-0.549076242218684));
#50777=CARTESIAN_POINT('Ctrl Pts',(0.0618735695667918,-0.432633082501095,
-0.529209065275543));
#50778=CARTESIAN_POINT('Ctrl Pts',(0.397229922498616,-0.18223092883058,
-0.509341888332401));
#50779=CARTESIAN_POINT('Ctrl Pts',(0.368288218425666,0.235294519055531,
-0.489474711389261));
#50780=CARTESIAN_POINT('Ctrl Pts',(0.0015907854635455,0.437032255275218,
-0.469607534446119));
#50781=CARTESIAN_POINT('Ctrl Pts',(-0.366565552053217,0.237969365997863,
-0.449740357502978));
#50782=CARTESIAN_POINT('Ctrl Pts',(-0.398546008475964,-0.179334326570714,
-0.429873180559836));
#50783=CARTESIAN_POINT('Ctrl Pts',(-0.0650214352906394,-0.432171188781472,
-0.410006003616696));
#50784=CARTESIAN_POINT('Ctrl Pts',(0.328134058466513,-0.288665489557203,
-0.390138826673554));
#50785=CARTESIAN_POINT('Ctrl Pts',(0.420359034055142,0.119574232706697,
-0.370271649730413));
#50786=CARTESIAN_POINT('Ctrl Pts',(0.127074364140008,0.418152886101354,
-0.350404472787272));
#50787=CARTESIAN_POINT('Ctrl Pts',(-0.28274978433206,0.33324509911095,-0.33053729584413));
#50788=CARTESIAN_POINT('Ctrl Pts',(-0.433265060768657,-0.0572804804381396,
-0.31067011890099));
#50789=CARTESIAN_POINT('Ctrl Pts',(-0.186434814361904,-0.395274396376197,
-0.290802941957848));
#50790=CARTESIAN_POINT('Ctrl Pts',(0.231374519917352,-0.370763569467605,
-0.270935765014707));
#50791=CARTESIAN_POINT('Ctrl Pts',(0.436990343063058,-0.00622705365271487,
-0.251068588071566));
#50792=CARTESIAN_POINT('Ctrl Pts',(0.241845539995049,0.364020605795136,
-0.231201411128424));
#50793=CARTESIAN_POINT('Ctrl Pts',(-0.17509788055655,0.400425703244833,
-0.211334234185283));
#50794=CARTESIAN_POINT('Ctrl Pts',(-0.431453976051128,0.0696031381283553,
-0.191467057242142));
#50795=CARTESIAN_POINT('Ctrl Pts',(-0.292136219448492,-0.325054560650286,
-0.171599880299));
#50796=CARTESIAN_POINT('Ctrl Pts',(0.11511952740285,-0.421601436873074,
-0.15173270335586));
#50797=CARTESIAN_POINT('Ctrl Pts',(0.416759446825152,-0.131507879469335,
-0.131865526412718));
#50798=CARTESIAN_POINT('Ctrl Pts',(0.336267715104065,0.279207608123703,
-0.111998349469577));
#50799=CARTESIAN_POINT('Ctrl Pts',(-0.0527610624488913,0.433831170076969,
-0.0921311725264359));
#50800=CARTESIAN_POINT('Ctrl Pts',(-0.393120484434934,0.190650465848009,
-0.0722639955832943));
#50801=CARTESIAN_POINT('Ctrl Pts',(-0.373496564225541,-0.227491156456244,
-0.052396818640154));
#50802=CARTESIAN_POINT('Ctrl Pts',(-0.0102468788472413,-0.436779313993799,
-0.0325296416970117));
#50803=CARTESIAN_POINT('Ctrl Pts',(0.236514469312927,-0.309551889635029,
-0.0192848570682517));
#50804=CARTESIAN_POINT('Ctrl Pts',(0.305685166691393,-0.207796100757101,
-0.0126624647538713));
#50805=CARTESIAN_POINT('Ctrl Pts',(0.174290087240704,0.352573191677455,
-2.84));
#50806=CARTESIAN_POINT('Ctrl Pts',(0.0569263183517569,0.410590482842535,
-2.83337760768562));
#50807=CARTESIAN_POINT('Ctrl Pts',(-0.238265070982699,0.399182217372751,
-2.82013282305686));
#50808=CARTESIAN_POINT('Ctrl Pts',(-0.465090476828282,0.0150761824976466,
-2.80026564611372));
#50809=CARTESIAN_POINT('Ctrl Pts',(-0.264253999321632,-0.382489215401403,
-2.78039846917058));
#50810=CARTESIAN_POINT('Ctrl Pts',(0.178362332584825,-0.429453634660495,
-2.76053129222743));
#50811=CARTESIAN_POINT('Ctrl Pts',(0.457696563131125,-0.0824760266495024,
-2.74066411528429));
#50812=CARTESIAN_POINT('Ctrl Pts',(0.317126076786983,0.340092281987134,
-2.72079693834115));
#50813=CARTESIAN_POINT('Ctrl Pts',(-0.114199676305766,0.450788173171041,
-2.70092976139801));
#50814=CARTESIAN_POINT('Ctrl Pts',(-0.440835050606981,0.14805492043082,
-2.68106258445487));
#50815=CARTESIAN_POINT('Ctrl Pts',(-0.363160481733799,-0.290452138461707,
-2.66119540751173));
#50816=CARTESIAN_POINT('Ctrl Pts',(0.0475558068997083,-0.462590194115042,
-2.64132823056859));
#50817=CARTESIAN_POINT('Ctrl Pts',(0.414664790853991,-0.210486680036103,
-2.62146105362544));
#50818=CARTESIAN_POINT('Ctrl Pts',(0.401483160587886,0.234652401347849,
-2.60159387668231));
#50819=CARTESIAN_POINT('Ctrl Pts',(0.0201044675420631,0.464593161004185,
-2.58172669973916));
#50820=CARTESIAN_POINT('Ctrl Pts',(-0.379712804018282,0.268457028712963,
-2.56185952279602));
#50821=CARTESIAN_POINT('Ctrl Pts',(-0.431296459168077,-0.173879889150686,
-2.54199234585288));
#50822=CARTESIAN_POINT('Ctrl Pts',(-0.0873399972287587,-0.456752291750344,
-2.52212516890974));
#50823=CARTESIAN_POINT('Ctrl Pts',(0.336715766013129,-0.320738860689576,
-2.5022579919666));
#50824=CARTESIAN_POINT('Ctrl Pts',(0.451970713081119,0.109422944411916,
-2.48239081502346));
#50825=CARTESIAN_POINT('Ctrl Pts',(0.152725064837474,0.439233392127166,
-2.46252363808032));
#50826=CARTESIAN_POINT('Ctrl Pts',(-0.286584178855772,0.366224554970629,
-2.44265646113718));
#50827=CARTESIAN_POINT('Ctrl Pts',(-0.463068149101368,-0.0426474309775924,
-2.42278928419403));
#50828=CARTESIAN_POINT('Ctrl Pts',(-0.214874079246792,-0.412407621050223,
-2.40292210725089));
#50829=CARTESIAN_POINT('Ctrl Pts',(0.230380196899991,-0.40395034386113,
-2.38305493030775));
#50830=CARTESIAN_POINT('Ctrl Pts',(0.464353666185826,-0.0250317374389039,
-2.36318775336461));
#50831=CARTESIAN_POINT('Ctrl Pts',(0.272470148495376,0.376843380742809,
-2.34332057642147));
#50832=CARTESIAN_POINT('Ctrl Pts',(-0.169294710236919,0.433116862339188,
-2.32345339947833));
#50833=CARTESIAN_POINT('Ctrl Pts',(-0.45580003155029,0.092180510786098,
-2.30358622253519));
#50834=CARTESIAN_POINT('Ctrl Pts',(-0.324292871224294,-0.333294237931656,
-2.28371904559205));
#50835=CARTESIAN_POINT('Ctrl Pts',(0.104622052482175,-0.453106104005534,
-2.2638518686489));
#50836=CARTESIAN_POINT('Ctrl Pts',(0.437588488283992,-0.157376079095672,
-2.24398469170577));
#50837=CARTESIAN_POINT('Ctrl Pts',(0.369244179683619,0.282682951599172,
-2.22411751476262));
#50838=CARTESIAN_POINT('Ctrl Pts',(-0.0377325669048753,0.463494518573569,
-2.20425033781949));
#50839=CARTESIAN_POINT('Ctrl Pts',(-0.410104919364264,0.21923701892257,
-2.18438316087634));
#50840=CARTESIAN_POINT('Ctrl Pts',(-0.406371604320363,-0.226081920010357,
-2.1645159839332));
#50841=CARTESIAN_POINT('Ctrl Pts',(-0.0299564308500308,-0.464061986811973,
-2.14464880699006));
#50842=CARTESIAN_POINT('Ctrl Pts',(0.373931671836009,-0.276452564016112,
-2.12478163004692));
#50843=CARTESIAN_POINT('Ctrl Pts',(0.434888455251049,0.164690457654952,
-2.10491445310378));
#50844=CARTESIAN_POINT('Ctrl Pts',(0.0970106843132033,0.454796484685485,
-2.08504727616063));
#50845=CARTESIAN_POINT('Ctrl Pts',(-0.329835217597774,0.327810379008085,
-2.0651800992175));
#50846=CARTESIAN_POINT('Ctrl Pts',(-0.454190491321138,-0.0998093830592591,
-2.04531292227435));
#50847=CARTESIAN_POINT('Ctrl Pts',(-0.162009386554628,-0.43589433813872,
-2.02544574533121));
#50848=CARTESIAN_POINT('Ctrl Pts',(0.27874991270585,-0.372222247480832,
-2.00557856838807));
#50849=CARTESIAN_POINT('Ctrl Pts',(0.463868723313386,0.0328134558498621,
-1.98571139144493));
#50850=CARTESIAN_POINT('Ctrl Pts',(0.223575285545482,0.40775606316333,-1.96584421450179));
#50851=CARTESIAN_POINT('Ctrl Pts',(-0.22175819938427,0.408747130092735,
-1.94597703755865));
#50852=CARTESIAN_POINT('Ctrl Pts',(-0.463718079984989,0.0348777529126524,
-1.9261098606155));
#50853=CARTESIAN_POINT('Ctrl Pts',(-0.2804038666359,-0.370977879298534,
-1.90624268367236));
#50854=CARTESIAN_POINT('Ctrl Pts',(0.160067670247924,-0.436611104181516,
-1.88637550672922));
#50855=CARTESIAN_POINT('Ctrl Pts',(0.453741753304744,-0.101829939905399,
-1.86650832978608));
#50856=CARTESIAN_POINT('Ctrl Pts',(0.331290993806108,0.326339076385531,
-1.84664115284294));
#50857=CARTESIAN_POINT('Ctrl Pts',(-0.0949854807243538,0.455223762346349,
-1.8267739758998));
#50858=CARTESIAN_POINT('Ctrl Pts',(-0.434151130818675,0.166624460875547,
-1.80690679895666));
#50859=CARTESIAN_POINT('Ctrl Pts',(-0.375158424003181,-0.274785502260672,
-1.78703962201352));
#50860=CARTESIAN_POINT('Ctrl Pts',(0.0278906518474728,-0.464190722540557,
-1.76717244507037));
#50861=CARTESIAN_POINT('Ctrl Pts',(0.405361316577113,-0.227888390173943,
-1.74730526812723));
#50862=CARTESIAN_POINT('Ctrl Pts',(0.411076653942302,0.217409521265286,
-1.72743809118409));
#50863=CARTESIAN_POINT('Ctrl Pts',(0.0397951497030185,0.463321984599604,
-1.70757091424095));
#50864=CARTESIAN_POINT('Ctrl Pts',(-0.367982335529924,0.284323611561093,
-1.68770373729781));
#50865=CARTESIAN_POINT('Ctrl Pts',(-0.438284615273599,-0.155426868229639,
-1.66783656035467));
#50866=CARTESIAN_POINT('Ctrl Pts',(-0.106637735177198,-0.452635956138572,
-1.64796938341153));
#50867=CARTESIAN_POINT('Ctrl Pts',(0.322806207759218,-0.334734323882857,
-1.62810220646839));
#50868=CARTESIAN_POINT('Ctrl Pts',(0.456205800795326,0.0901508883699798,
-1.60823502952524));
#50869=CARTESIAN_POINT('Ctrl Pts',(0.171220782659577,0.432359062514762,
-1.5883678525821));
#50870=CARTESIAN_POINT('Ctrl Pts',(-0.27079016643251,0.378052378800417,
-1.56850067563896));
#50871=CARTESIAN_POINT('Ctrl Pts',(-0.464460480016421,-0.0229647089273341,
-1.54863349869582));
#50872=CARTESIAN_POINT('Ctrl Pts',(-0.232175847394933,-0.402920949119856,
-1.52876632175268));
#50873=CARTESIAN_POINT('Ctrl Pts',(0.213036375069731,-0.413359913695497,
-1.50889914480954));
#50874=CARTESIAN_POINT('Ctrl Pts',(0.462873745233912,-0.0447080677991511,
-1.4890319678664));
#50875=CARTESIAN_POINT('Ctrl Pts',(0.288211357648988,0.364945377659901,
-1.46916479092326));
#50876=CARTESIAN_POINT('Ctrl Pts',(-0.150768573893214,0.439908800184091,
-1.44929761398012));
#50877=CARTESIAN_POINT('Ctrl Pts',(-0.451479217637502,0.111433529041447,
-1.42943043703697));
#50878=CARTESIAN_POINT('Ctrl Pts',(-0.338139981713148,-0.319237009321025,
-1.40956326009383));
#50879=CARTESIAN_POINT('Ctrl Pts',(0.0853061500991524,-0.457136496145803,
-1.38969608315069));
#50880=CARTESIAN_POINT('Ctrl Pts',(0.430518334913016,-0.175797834619561,
-1.36982890620755));
#50881=CARTESIAN_POINT('Ctrl Pts',(0.380903786176095,0.266764354871328,
-1.34996172926441));
#50882=CARTESIAN_POINT('Ctrl Pts',(-0.0180361814733977,0.464677965381466,
-1.33009455232127));
#50883=CARTESIAN_POINT('Ctrl Pts',(-0.400435235439597,0.23643717468206,
-1.31022737537813));
#50884=CARTESIAN_POINT('Ctrl Pts',(-0.415596652385769,-0.208639252967755,
-1.29036019843499));
#50885=CARTESIAN_POINT('Ctrl Pts',(-0.0496159542829584,-0.46237341233444,
-1.27049302149184));
#50886=CARTESIAN_POINT('Ctrl Pts',(0.361867347479004,-0.292066667358173,
-1.2506258445487));
#50887=CARTESIAN_POINT('Ctrl Pts',(0.441483476121179,0.146093311500428,
-1.23075866760556));
#50888=CARTESIAN_POINT('Ctrl Pts',(0.116216781761661,0.450271667985189,
-1.21089149066242));
#50889=CARTESIAN_POINT('Ctrl Pts',(-0.315631882761826,0.341507584011579,
-1.19102431371928));
#50890=CARTESIAN_POINT('Ctrl Pts',(-0.458015743653862,-0.0804518111567413,
-1.17115713677614));
#50891=CARTESIAN_POINT('Ctrl Pts',(-0.180355101637042,-0.42862915517577,
-1.151289959833));
#50892=CARTESIAN_POINT('Ctrl Pts',(0.262708520656938,-0.383712325222222,
-1.13142278288986));
#50893=CARTESIAN_POINT('Ctrl Pts',(0.464843154159083,0.0131056241604778,
-1.11155560594671));
#50894=CARTESIAN_POINT('Ctrl Pts',(0.240671892449695,0.397904455287802,
-1.09168842900357));
#50895=CARTESIAN_POINT('Ctrl Pts',(-0.204218649827841,0.417786618282221,
-1.07182125206043));
#50896=CARTESIAN_POINT('Ctrl Pts',(-0.461821042210512,0.054518256802636,
-1.05195407511729));
#50897=CARTESIAN_POINT('Ctrl Pts',(-0.295889106797746,-0.358748591400207,
-1.03208689817415));
#50898=CARTESIAN_POINT('Ctrl Pts',(0.141401607222709,-0.443008465864971,
-1.01221972123101));
#50899=CARTESIAN_POINT('Ctrl Pts',(0.449013443083765,-0.120986955012779,
-0.992352544287866));
#50900=CARTESIAN_POINT('Ctrl Pts',(0.344836751775652,0.31199123381598,-0.972485367344727));
#50901=CARTESIAN_POINT('Ctrl Pts',(-0.0755884178681167,0.458843444365718,
-0.952618190401585));
#50902=CARTESIAN_POINT('Ctrl Pts',(-0.426691735918344,0.184892070820229,
-0.932751013458443));
#50903=CARTESIAN_POINT('Ctrl Pts',(-0.386477679855359,-0.258623120248015,
-0.912883836515303));
#50904=CARTESIAN_POINT('Ctrl Pts',(0.00817359189184459,-0.46495602775831,
-0.893016659572161));
#50905=CARTESIAN_POINT('Ctrl Pts',(0.395328893487888,-0.244879524106942,
-0.87314948262902));
#50906=CARTESIAN_POINT('Ctrl Pts',(0.419929564917943,0.199775063161117,
-0.85328230568588));
#50907=CARTESIAN_POINT('Ctrl Pts',(0.0594144236348126,0.461216697027921,
-0.833415128742737));
#50908=CARTESIAN_POINT('Ctrl Pts',(-0.355589460419919,0.299678245776149,
-0.813547951799597));
#50909=CARTESIAN_POINT('Ctrl Pts',(-0.444483597787454,-0.136693989081916,
-0.793680774856456));
#50910=CARTESIAN_POINT('Ctrl Pts',(-0.125743511941739,-0.447704684538541,
-0.773813597913313));
#50911=CARTESIAN_POINT('Ctrl Pts',(0.308315472215645,-0.348127110328446,
-0.753946420970174));
#50912=CARTESIAN_POINT('Ctrl Pts',(0.459619505128892,0.0707165175776674,
-0.734079244027031));
#50913=CARTESIAN_POINT('Ctrl Pts',(0.189408231561648,0.424706295185092,
-0.714212067083891));
#50914=CARTESIAN_POINT('Ctrl Pts',(-0.254508613430572,0.389199538852239,
-0.694344890140749));
#50915=CARTESIAN_POINT('Ctrl Pts',(-0.465016573476227,-0.00324063973682662,
-0.674477713197608));
#50916=CARTESIAN_POINT('Ctrl Pts',(-0.249059596110711,-0.392708839903043,
-0.654610536254467));
#50917=CARTESIAN_POINT('Ctrl Pts',(0.195308993064281,-0.422025251117977,
-0.634743359311326));
#50918=CARTESIAN_POINT('Ctrl Pts',(0.460560444803989,-0.0643039037462118,
-0.614876182368184));
#50919=CARTESIAN_POINT('Ctrl Pts',(0.303433657845617,0.352390310077654,
-0.595009005425044));
#50920=CARTESIAN_POINT('Ctrl Pts',(-0.13197098688333,0.445908705873406,
-0.575141828481902));
#50921=CARTESIAN_POINT('Ctrl Pts',(-0.446345539656594,0.130485917224834,
-0.555274651538761));
#50922=CARTESIAN_POINT('Ctrl Pts',(-0.351378289332966,-0.304605011638794,
-0.535407474595619));
#50923=CARTESIAN_POINT('Ctrl Pts',(0.0658366585339714,-0.460343838613949,
-0.515540297652478));
#50924=CARTESIAN_POINT('Ctrl Pts',(0.422673056526765,-0.193903075574074,
-0.495673120709337));
#50925=CARTESIAN_POINT('Ctrl Pts',(0.391877595689725,0.250365463225,-0.475805943766196));
#50926=CARTESIAN_POINT('Ctrl Pts',(0.00169267750507216,0.46502478457827,
-0.455938766823055));
#50927=CARTESIAN_POINT('Ctrl Pts',(-0.390044590118444,0.253211637868,-0.436071589879914));
#50928=CARTESIAN_POINT('Ctrl Pts',(-0.424073439658023,-0.190820941874228,
-0.416204412936772));
#50929=CARTESIAN_POINT('Ctrl Pts',(-0.0691861494753018,-0.459852359953339,
-0.396337235993632));
#50930=CARTESIAN_POINT('Ctrl Pts',(0.349151505430854,-0.307154919290763,
-0.376470059050489));
#50931=CARTESIAN_POINT('Ctrl Pts',(0.447283620139026,0.127233130127951,
-0.356602882107349));
#50932=CARTESIAN_POINT('Ctrl Pts',(0.135213655505621,0.44493616531258,-0.336735705164207));
#50933=CARTESIAN_POINT('Ctrl Pts',(-0.300860304843555,0.354589915401655,
-0.316868528221066));
#50934=CARTESIAN_POINT('Ctrl Pts',(-0.461016295976497,-0.0609493756004606,
-0.297001351277925));
#50935=CARTESIAN_POINT('Ctrl Pts',(-0.19837622587362,-0.420592276211723,
-0.277134174334784));
#50936=CARTESIAN_POINT('Ctrl Pts',(0.246194382640499,-0.39451149643993,
-0.257266997391642));
#50937=CARTESIAN_POINT('Ctrl Pts',(0.4649801878301,-0.00662590517852661,
-0.237399820448502));
#50938=CARTESIAN_POINT('Ctrl Pts',(0.25733608624972,0.387336636480831,-0.217532643505359));
#50939=CARTESIAN_POINT('Ctrl Pts',(-0.18631314554722,0.426073531514894,
-0.197665466562219));
#50940=CARTESIAN_POINT('Ctrl Pts',(-0.459089208741044,0.0740613168099621,
-0.177798289619077));
#50941=CARTESIAN_POINT('Ctrl Pts',(-0.310847954302583,-0.345874761457578,
-0.157931112675936));
#50942=CARTESIAN_POINT('Ctrl Pts',(0.122493094697439,-0.448605600601096,
-0.138063935732795));
#50943=CARTESIAN_POINT('Ctrl Pts',(0.443453474295116,-0.139931143714006,
-0.118196758789654));
#50944=CARTESIAN_POINT('Ctrl Pts',(0.357806134191217,0.297091247277788,
-0.0983295818465128));
#50945=CARTESIAN_POINT('Ctrl Pts',(-0.0561404825462262,0.461618665380512,
-0.0784624049033717));
#50946=CARTESIAN_POINT('Ctrl Pts',(-0.418300403187716,0.202861895753863,
-0.0585952279602298));
#50947=CARTESIAN_POINT('Ctrl Pts',(-0.397419543347731,-0.242062284299603,
-0.0387280510170898));
#50948=CARTESIAN_POINT('Ctrl Pts',(-0.010903205818384,-0.464755642052786,
-0.0188608740739473));
#50949=CARTESIAN_POINT('Ctrl Pts',(0.25166355300852,-0.329379122606579,
-0.00561608944518735));
#50950=CARTESIAN_POINT('Ctrl Pts',(0.325264730631653,-0.221105732641915,
0.00100630286919312));
#50951=CARTESIAN_POINT('Ctrl Pts',(-0.39272888104496,9.19390291685468E-5,
-0.0496163522034977));
#50952=CARTESIAN_POINT('Ctrl Pts',(-0.392616526570956,-0.0635210754266735,
-0.0464109014689986));
#50953=CARTESIAN_POINT('Ctrl Pts',(-0.377854412170386,-0.1271963235368,
-0.0432054507344995));
#50954=CARTESIAN_POINT('Ctrl Pts',(-0.348771505299647,-0.183214908972786,
-0.0400000000000003));
#50955=CARTESIAN_POINT('',(-0.322117167679667,-0.010084934854993,-2.84));
#50956=CARTESIAN_POINT('Ctrl Pts',(-0.322665937590337,-0.00999768482676959,
-2.84));
#50957=CARTESIAN_POINT('Ctrl Pts',(-0.323650211264442,-0.00315523629261327,
-2.84));
#50958=CARTESIAN_POINT('Ctrl Pts',(-0.324397225861028,0.00370989634134569,
-2.84));
#50959=CARTESIAN_POINT('Ctrl Pts',(-0.324901721971083,0.0105873702227374,
-2.84));
#50960=CARTESIAN_POINT('Ctrl Pts',(-0.325997667963835,0.0255277033399459,
-2.84));
#50961=CARTESIAN_POINT('Ctrl Pts',(-0.325950748451652,0.0405258873091143,
-2.84));
#50962=CARTESIAN_POINT('Ctrl Pts',(-0.324836924795275,0.0554860263150083,
-2.84));
#50963=CARTESIAN_POINT('Ctrl Pts',(-0.324393308343733,0.0614443876250565,
-2.84));
#50964=CARTESIAN_POINT('Ctrl Pts',(-0.323780197469711,0.0673967849520013,
-2.84));
#50965=CARTESIAN_POINT('Ctrl Pts',(-0.323001415813532,0.0733373463202781,
-2.84));
#50966=CARTESIAN_POINT('Ctrl Pts',(-0.322198157543006,0.0794646157709396,
-2.84));
#50967=CARTESIAN_POINT('Ctrl Pts',(-0.321219769535019,0.0855702854614099,
-2.84));
#50968=CARTESIAN_POINT('Ctrl Pts',(-0.320072263419342,0.09164450471336,
-2.84));
#50969=CARTESIAN_POINT('Ctrl Pts',(-0.317737578918981,0.104002944764868,
-2.84));
#50970=CARTESIAN_POINT('Ctrl Pts',(-0.314702870444172,0.116235555905157,
-2.84));
#50971=CARTESIAN_POINT('Ctrl Pts',(-0.311007712210463,0.128288621791672,
-2.84));
#50972=CARTESIAN_POINT('Ctrl Pts',(-0.30880376108375,0.135477588125667,
-2.84));
#50973=CARTESIAN_POINT('Ctrl Pts',(-0.306364669022593,0.142602716913589,
-2.84));
#50974=CARTESIAN_POINT('Ctrl Pts',(-0.303697238249508,0.149652643556526,
-2.84));
#50975=CARTESIAN_POINT('Ctrl Pts',(-0.301224487679456,0.156188037202371,
-2.84));
#50976=CARTESIAN_POINT('Ctrl Pts',(-0.298553872096886,0.162661690838749,
-2.84));
#50977=CARTESIAN_POINT('Ctrl Pts',(-0.295701310709281,0.169041266471786,
-2.84));
#50978=CARTESIAN_POINT('Ctrl Pts',(-0.287500937396955,0.187380889938761,
-2.84));
#50979=CARTESIAN_POINT('Ctrl Pts',(-0.277787872339422,0.204982261003147,
-2.84));
#50980=CARTESIAN_POINT('Ctrl Pts',(-0.26670532546941,0.221641187990873,
-2.84));
#50981=CARTESIAN_POINT('Ctrl Pts',(-0.259647208511552,0.232250721742538,
-2.84));
#50982=CARTESIAN_POINT('Ctrl Pts',(-0.25203249560377,0.242478100323189,
-2.84));
#50983=CARTESIAN_POINT('Ctrl Pts',(-0.24388759544458,0.252267871100332,
-2.84));
#50984=CARTESIAN_POINT('Ctrl Pts',(-0.239499894383172,0.257541672717328,
-2.84));
#50985=CARTESIAN_POINT('Ctrl Pts',(-0.234958197800991,0.262688420481687,
-2.84));
#50986=CARTESIAN_POINT('Ctrl Pts',(-0.230265756133984,0.267698872564867,
-2.84));
#50987=CARTESIAN_POINT('Ctrl Pts',(-0.226847227029321,0.271349078041964,
-2.84));
#50988=CARTESIAN_POINT('Ctrl Pts',(-0.223349311713903,0.274925985807238,
-2.84));
#50989=CARTESIAN_POINT('Ctrl Pts',(-0.219782826738047,0.278417295395633,
-2.84));
#50990=CARTESIAN_POINT('Ctrl Pts',(-0.208710072844623,0.289256654624611,
-2.84));
#50991=CARTESIAN_POINT('Ctrl Pts',(-0.196955369123494,0.299295600355571,
-2.84));
#50992=CARTESIAN_POINT('Ctrl Pts',(-0.184574140330731,0.308442555718213,
-2.84));
#50993=CARTESIAN_POINT('Ctrl Pts',(-0.172041900670708,0.317701074293621,
-2.84));
#50994=CARTESIAN_POINT('Ctrl Pts',(-0.158867686557205,0.326046279965927,
-2.84));
#50995=CARTESIAN_POINT('Ctrl Pts',(-0.145156625066643,0.333486543488778,
-2.84));
#50996=CARTESIAN_POINT('Ctrl Pts',(-0.138539413076319,0.337077352342525,
-2.84));
#50997=CARTESIAN_POINT('Ctrl Pts',(-0.131796942169486,0.340457166247357,
-2.84));
#50998=CARTESIAN_POINT('Ctrl Pts',(-0.12494001352005,0.343625665611372,
-2.84));
#50999=CARTESIAN_POINT('Ctrl Pts',(-0.117798371987087,0.346925727171306,
-2.84));
#51000=CARTESIAN_POINT('Ctrl Pts',(-0.110525837567219,0.349998768671215,
-2.84));
#51001=CARTESIAN_POINT('Ctrl Pts',(-0.103170100809649,0.352830723345205,
-2.84));
#51002=CARTESIAN_POINT('Ctrl Pts',(-0.0839056785772351,0.360247515487291,
-2.84));
#51003=CARTESIAN_POINT('Ctrl Pts',(-0.0640406356108989,0.366032022011569,
-2.84));
#51004=CARTESIAN_POINT('Ctrl Pts',(-0.0438096601120564,0.37020654613364,
-2.84));
#51005=CARTESIAN_POINT('Ctrl Pts',(-0.0257589803203683,0.373931181073486,
-2.84));
#51006=CARTESIAN_POINT('Ctrl Pts',(-0.00741575563267887,0.376373790742814,
-2.84));
#51007=CARTESIAN_POINT('Ctrl Pts',(0.0110694999116937,0.377521301223216,
-2.84));
#51008=CARTESIAN_POINT('Ctrl Pts',(0.0163026119130628,0.377846157477016,
-2.84));
#51009=CARTESIAN_POINT('Ctrl Pts',(0.0215471587080905,0.37806704191005,
-2.84));
#51010=CARTESIAN_POINT('Ctrl Pts',(0.0267998089378223,0.378183226427262,
-2.84));
#51011=CARTESIAN_POINT('Ctrl Pts',(0.0319645250457776,0.378297465910437,
-2.84));
#51012=CARTESIAN_POINT('Ctrl Pts',(0.03712808659929,0.37831025253997,-2.84));
#51013=CARTESIAN_POINT('Ctrl Pts',(0.0422850648456711,0.378221894196039,
-2.84));
#51014=CARTESIAN_POINT('Ctrl Pts',(0.0648738954569795,0.377834862960147,
-2.84));
#51015=CARTESIAN_POINT('Ctrl Pts',(0.0873477481761387,0.375512022714285,
-2.84));
#51016=CARTESIAN_POINT('Ctrl Pts',(0.10943707149879,0.371248712598134,-2.84));
#51017=CARTESIAN_POINT('Ctrl Pts',(0.130322404520726,0.367217776464374,
-2.84));
#51018=CARTESIAN_POINT('Ctrl Pts',(0.150865606811995,0.361452006559849,
-2.84));
#51019=CARTESIAN_POINT('Ctrl Pts',(0.170841168278706,0.353897569143461,
-2.84));
#51020=CARTESIAN_POINT('Ctrl Pts',(0.171992712390165,0.353462073603737,
-2.84));
#51021=CARTESIAN_POINT('Ctrl Pts',(0.173142366923995,0.353020619647747,
-2.84));
#51022=CARTESIAN_POINT('Ctrl Pts',(0.174290087240704,0.352573191677455,
-2.84));
#51023=CARTESIAN_POINT('Ctrl Pts',(-0.322665937590337,-0.00999768482676161,
-2.84));
#51024=CARTESIAN_POINT('Ctrl Pts',(-0.319085648514224,-0.109944606251347,
-2.83380159067993));
#51025=CARTESIAN_POINT('Ctrl Pts',(-0.208793047698186,-0.314237772328811,
-2.82098078904546));
#51026=CARTESIAN_POINT('Ctrl Pts',(0.146152353759915,-0.351899746021385,
-2.80153759509663));
#51027=CARTESIAN_POINT('Ctrl Pts',(0.375042359224723,-0.0675819005554749,
-2.78167041815349));
#51028=CARTESIAN_POINT('Ctrl Pts',(0.259857122798181,0.278675922139343,
-2.76180324121035));
#51029=CARTESIAN_POINT('Ctrl Pts',(-0.0935766607715254,0.369381537016774,
-2.7419360642672));
#51030=CARTESIAN_POINT('Ctrl Pts',(-0.3009571590477,0.17717647370315,-2.72654253555465));
#51031=CARTESIAN_POINT('Ctrl Pts',(-0.322260534817986,0.0351318319167836,
-2.71777139915648));
#51032=CARTESIAN_POINT('Ctrl Pts',(-0.321998819203686,0.000257793408019166,
-2.71562265507269));
#51033=CARTESIAN_POINT('Origin',(-5.160062080289E-17,2.1385152528819E-17,
-2.84));
#51034=CARTESIAN_POINT('',(-0.0953060101009199,-0.307860260611277,-2.84));
#51035=CARTESIAN_POINT('Ctrl Pts',(0.386886490162194,0.0743511351644874,
-2.84));
#51036=CARTESIAN_POINT('Ctrl Pts',(0.387777631536103,0.0660369131998544,
-2.84));
#51037=CARTESIAN_POINT('Ctrl Pts',(0.388383000500425,0.0577031558050302,
-2.84));
#51038=CARTESIAN_POINT('Ctrl Pts',(0.388693798011576,0.0493601925761383,
-2.84));
#51039=CARTESIAN_POINT('Ctrl Pts',(0.389273718297948,0.0337929713105256,
-2.84));
#51040=CARTESIAN_POINT('Ctrl Pts',(0.388828835948466,0.0181934386380921,
-2.84));
#51041=CARTESIAN_POINT('Ctrl Pts',(0.387402867595623,0.00264531365779935,
-2.84));
#51042=CARTESIAN_POINT('Ctrl Pts',(0.386525710712122,-0.00691881504449793,
-2.84));
#51043=CARTESIAN_POINT('Ctrl Pts',(0.385277044495428,-0.0164634425160969,
-2.84));
#51044=CARTESIAN_POINT('Ctrl Pts',(0.38366467452966,-0.0259680740313437,
-2.84));
#51045=CARTESIAN_POINT('Ctrl Pts',(0.382578597842544,-0.0323703011426751,
-2.84));
#51046=CARTESIAN_POINT('Ctrl Pts',(0.381329136230223,-0.0387444395247865,
-2.84));
#51047=CARTESIAN_POINT('Ctrl Pts',(0.379919987860161,-0.0450834271490292,
-2.84));
#51048=CARTESIAN_POINT('Ctrl Pts',(0.375241205020874,-0.0661307115549059,
-2.84));
#51049=CARTESIAN_POINT('Ctrl Pts',(0.368804611897396,-0.086796661047342,
-2.84));
#51050=CARTESIAN_POINT('Ctrl Pts',(0.36070805921707,-0.106848695813115,
-2.84));
#51051=CARTESIAN_POINT('Ctrl Pts',(0.358523938385156,-0.112257919785758,
-2.84));
#51052=CARTESIAN_POINT('Ctrl Pts',(0.356217849874627,-0.117624328792278,
-2.84));
#51053=CARTESIAN_POINT('Ctrl Pts',(0.353794229194997,-0.122936384035782,
-2.84));
#51054=CARTESIAN_POINT('Ctrl Pts',(0.345055249932482,-0.142090346949399,
-2.84));
#51055=CARTESIAN_POINT('Ctrl Pts',(0.33482754435563,-0.160464142324307,
-2.84));
#51056=CARTESIAN_POINT('Ctrl Pts',(0.323210439908307,-0.177847734349123,
-2.84));
#51057=CARTESIAN_POINT('Ctrl Pts',(0.311907287961945,-0.194761534420477,
-2.84));
#51058=CARTESIAN_POINT('Ctrl Pts',(0.299287886823657,-0.21073895330334,
-2.84));
#51059=CARTESIAN_POINT('Ctrl Pts',(0.285412291186548,-0.225549742408173,
-2.84));
#51060=CARTESIAN_POINT('Ctrl Pts',(0.281533606021401,-0.229689844893676,
-2.84));
#51061=CARTESIAN_POINT('Ctrl Pts',(0.277556615451261,-0.233738512703413,
-2.84));
#51062=CARTESIAN_POINT('Ctrl Pts',(0.273482321259015,-0.237690020765659,
-2.84));
#51063=CARTESIAN_POINT('Ctrl Pts',(0.269826094885338,-0.241236060229495,
-2.84));
#51064=CARTESIAN_POINT('Ctrl Pts',(0.266098715359341,-0.244696844003723,
-2.84));
#51065=CARTESIAN_POINT('Ctrl Pts',(0.262302171233473,-0.248068629162198,
-2.84));
#51066=CARTESIAN_POINT('Ctrl Pts',(0.251922843610169,-0.257286713207833,
-2.84));
#51067=CARTESIAN_POINT('Ctrl Pts',(0.241025467094922,-0.265841912499015,
-2.84));
#51068=CARTESIAN_POINT('Ctrl Pts',(0.229633058917296,-0.273663333948482,
-2.84));
#51069=CARTESIAN_POINT('Ctrl Pts',(0.212684455368641,-0.285299343584647,
-2.84));
#51070=CARTESIAN_POINT('Ctrl Pts',(0.194639964930078,-0.29531383338317,
-2.84));
#51071=CARTESIAN_POINT('Ctrl Pts',(0.175745617012724,-0.303666873318378,
-2.84));
#51072=CARTESIAN_POINT('Ctrl Pts',(0.170555727357543,-0.305961281981682,
-2.84));
#51073=CARTESIAN_POINT('Ctrl Pts',(0.165301681301442,-0.308130013924166,
-2.84));
#51074=CARTESIAN_POINT('Ctrl Pts',(0.159988579735579,-0.310171507406792,
-2.84));
#51075=CARTESIAN_POINT('Ctrl Pts',(0.154889918181581,-0.312130604970348,
-2.84));
#51076=CARTESIAN_POINT('Ctrl Pts',(0.149744225546196,-0.313969589980248,
-2.84));
#51077=CARTESIAN_POINT('Ctrl Pts',(0.144562864921253,-0.315686056767363,
-2.84));
#51078=CARTESIAN_POINT('Ctrl Pts',(0.12515058641648,-0.322116902587143,
-2.84));
#51079=CARTESIAN_POINT('Ctrl Pts',(0.105209092186283,-0.326843744021275,
-2.84));
#51080=CARTESIAN_POINT('Ctrl Pts',(0.0849853735125539,-0.329835823811007,
-2.84));
#51081=CARTESIAN_POINT('Ctrl Pts',(0.0684594127471476,-0.332280823863164,
-2.84));
#51082=CARTESIAN_POINT('Ctrl Pts',(0.0517442313050582,-0.333566343194817,
-2.84));
#51083=CARTESIAN_POINT('Ctrl Pts',(0.0349800186612873,-0.333646455380123,
-2.84));
#51084=CARTESIAN_POINT('Ctrl Pts',(0.0295813726058093,-0.333672254225699,
-2.84));
#51085=CARTESIAN_POINT('Ctrl Pts',(0.0241763134870444,-0.333572565689335,
-2.84));
#51086=CARTESIAN_POINT('Ctrl Pts',(0.0187879591158384,-0.333346693379246,
-2.84));
#51087=CARTESIAN_POINT('Ctrl Pts',(-0.000865993468952917,-0.332522827061838,
-2.84));
#51088=CARTESIAN_POINT('Ctrl Pts',(-0.0203544443771316,-0.330026027060492,
-2.84));
#51089=CARTESIAN_POINT('Ctrl Pts',(-0.0394503020694342,-0.325804718223723,
-2.84));
#51090=CARTESIAN_POINT('Ctrl Pts',(-0.057164691519548,-0.321888795203734,
-2.84));
#51091=CARTESIAN_POINT('Ctrl Pts',(-0.0745422208533479,-0.316488228952411,
-2.84));
#51092=CARTESIAN_POINT('Ctrl Pts',(-0.0913773650560324,-0.30951939268376,
-2.84));
#51093=CARTESIAN_POINT('Ctrl Pts',(-0.0926902647827869,-0.308975923431418,
-2.84));
#51094=CARTESIAN_POINT('Ctrl Pts',(-0.0939998487070982,-0.308422896049449,
-2.84));
#51095=CARTESIAN_POINT('Ctrl Pts',(-0.0953060101009229,-0.307860260611276,
-2.84));
#51096=CARTESIAN_POINT('Origin',(0.,0.,-2.84));
#51097=CARTESIAN_POINT('Origin',(0.,0.,-3.17777734492731));
#51098=CARTESIAN_POINT('Ctrl Pts',(-0.0953060101009229,-0.307860260611276,
-2.84));
#51099=CARTESIAN_POINT('Ctrl Pts',(0.00717381913557572,-0.339585510310479,
-2.83337760768562));
#51100=CARTESIAN_POINT('Ctrl Pts',(0.244531614604281,-0.292083776802967,
-2.82013282305686));
#51101=CARTESIAN_POINT('Ctrl Pts',(0.378255106318521,0.0481000370439281,
-2.80026564611372));
#51102=CARTESIAN_POINT('Ctrl Pts',(0.164216515677071,0.34372885516354,-2.78039846917058));
#51103=CARTESIAN_POINT('Ctrl Pts',(-0.199989402997138,0.324342678219355,
-2.76053129222744));
#51104=CARTESIAN_POINT('Ctrl Pts',(-0.321845227690632,0.110984795593872,
-2.74715758414635));
#51105=CARTESIAN_POINT('Ctrl Pts',(-0.322813262032044,0.00211343905450969,
-2.74040626837964));
#51106=CARTESIAN_POINT('Ctrl Pts',(-0.322809858836148,3.43668072568986E-5,
-2.74027734492731));
#51107=CARTESIAN_POINT('Ctrl Pts',(-0.116310150563007,-0.375708449300798,
-2.88100630286919));
#51108=CARTESIAN_POINT('Ctrl Pts',(0.00875483070676231,-0.414425509906482,
-2.87438391055481));
#51109=CARTESIAN_POINT('Ctrl Pts',(0.298423036300873,-0.356455044346,-2.86113912592605));
#51110=CARTESIAN_POINT('Ctrl Pts',(0.461617355721276,0.0587006270091591,
-2.84127194898291));
#51111=CARTESIAN_POINT('Ctrl Pts',(0.200407588599154,0.419481991267769,
-2.82140477203977));
#51112=CARTESIAN_POINT('Ctrl Pts',(-0.244064330769604,0.395823366204863,
-2.80153759509663));
#51113=CARTESIAN_POINT('Ctrl Pts',(-0.464980723451366,0.00901991303881209,
-2.78167041815349));
#51114=CARTESIAN_POINT('Ctrl Pts',(-0.259321715654258,-0.385984470229777,
-2.76180324121035));
#51115=CARTESIAN_POINT('Ctrl Pts',(0.184085419273639,-0.427041120788341,
-2.7419360642672));
#51116=CARTESIAN_POINT('Ctrl Pts',(0.458707595804344,-0.07644057108933,
-2.72206888732406));
#51117=CARTESIAN_POINT('Ctrl Pts',(0.312630362980567,0.344253201275889,
-2.70220171038092));
#51118=CARTESIAN_POINT('Ctrl Pts',(-0.120148330577789,0.449238960762277,
-2.68233453343778));
#51119=CARTESIAN_POINT('Ctrl Pts',(-0.442745013212915,0.142226606977436,
-2.66246735649464));
#51120=CARTESIAN_POINT('Ctrl Pts',(-0.359299014024003,-0.295219785168938,
-2.6426001795515));
#51121=CARTESIAN_POINT('Ctrl Pts',(0.0536572306457554,-0.461921985183017,
-2.62273300260836));
#51122=CARTESIAN_POINT('Ctrl Pts',(0.417405425637388,-0.204996889107976,
-2.60286582566521));
#51123=CARTESIAN_POINT('Ctrl Pts',(0.398352272201653,0.239929871442676,
-2.58299864872208));
#51124=CARTESIAN_POINT('Ctrl Pts',(0.0139719758106573,0.464817963519448,
-2.56313147177893));
#51125=CARTESIAN_POINT('Ctrl Pts',(-0.383222079658351,0.263423206510685,
-2.5432642948358));
#51126=CARTESIAN_POINT('Ctrl Pts',(-0.42896455902559,-0.179555945670809,
-2.52339711789265));
#51127=CARTESIAN_POINT('Ctrl Pts',(-0.0813052976463755,-0.457865035790148,
-2.50352994094951));
#51128=CARTESIAN_POINT('Ctrl Pts',(0.340918760207331,-0.316267828616965,
-2.48366276400637));
#51129=CARTESIAN_POINT('Ctrl Pts',(0.450487506537335,0.115377401546258,
-2.46379558706323));
#51130=CARTESIAN_POINT('Ctrl Pts',(0.14691587208234,0.441210456141015,-2.44392841012008));
#51131=CARTESIAN_POINT('Ctrl Pts',(-0.291391754232848,0.362411072184382,
-2.42406123317695));
#51132=CARTESIAN_POINT('Ctrl Pts',(-0.462465105737489,-0.0487541321641203,
-2.4041940562338));
#51133=CARTESIAN_POINT('Ctrl Pts',(-0.209413461852369,-0.415207106963557,
-2.38432687929066));
#51134=CARTESIAN_POINT('Ctrl Pts',(0.235690474676962,-0.400875217182329,
-2.36445970234752));
#51135=CARTESIAN_POINT('Ctrl Pts',(0.464643569830363,-0.0189021848768118,
-2.34459252540438));
#51136=CARTESIAN_POINT('Ctrl Pts',(0.26747380789293,0.380405969595911,-2.32472534846124));
#51137=CARTESIAN_POINT('Ctrl Pts',(-0.174995169749528,0.430845250832214,
-2.3048581715181));
#51138=CARTESIAN_POINT('Ctrl Pts',(-0.456976740313732,0.0861579851791214,
-2.28499099457496));
#51139=CARTESIAN_POINT('Ctrl Pts',(-0.31986667400783,-0.337544442202628,
-2.26512381763182));
#51140=CARTESIAN_POINT('Ctrl Pts',(0.110591906940626,-0.451686140721507,
-2.24525664068867));
#51141=CARTESIAN_POINT('Ctrl Pts',(0.439627069105229,-0.151588191197238,
-2.22538946374554));
#51142=CARTESIAN_POINT('Ctrl Pts',(0.365481912109643,0.287530714049526,
-2.20552228680239));
#51143=CARTESIAN_POINT('Ctrl Pts',(-0.043845321532473,0.462956291004388,
-2.18565510985925));
#51144=CARTESIAN_POINT('Ctrl Pts',(-0.412962176943286,0.213806407797088,
-2.16578793291611));
#51145=CARTESIAN_POINT('Ctrl Pts',(-0.403352984750648,-0.231424521807137,
-2.14592075597297));
#51146=CARTESIAN_POINT('Ctrl Pts',(-0.0238302987011413,-0.464416899417628,
-2.12605357902982));
#51147=CARTESIAN_POINT('Ctrl Pts',(0.377547063985032,-0.271494298424763,
-2.10618640208669));
#51148=CARTESIAN_POINT('Ctrl Pts',(0.432677444960194,0.170414694858164,
-2.08631922514354));
#51149=CARTESIAN_POINT('Ctrl Pts',(0.0910009807419794,0.456037017252848,
-2.0664520482004));
#51150=CARTESIAN_POINT('Ctrl Pts',(-0.33413213807732,0.323429519222901,
-2.04658487125727));
#51151=CARTESIAN_POINT('Ctrl Pts',(-0.452833939219847,-0.105793965288736,
-2.02671769431412));
#51152=CARTESIAN_POINT('Ctrl Pts',(-0.15624345066412,-0.437994205127701,
-2.00685051737098));
#51153=CARTESIAN_POINT('Ctrl Pts',(0.283637314429727,-0.368511619170916,
-1.98698334042784));
#51154=CARTESIAN_POINT('Ctrl Pts',(0.463395373269886,0.0389315762966344,
-1.9671161634847));
#51155=CARTESIAN_POINT('Ctrl Pts',(0.2181752912658,0.41067077066911,-1.94724898654156));
#51156=CARTESIAN_POINT('Ctrl Pts',(-0.227132523608876,0.405785357448913,
-1.92738180959842));
#51157=CARTESIAN_POINT('Ctrl Pts',(-0.464137961773493,0.0287557305875891,
-1.90751463265527));
#51158=CARTESIAN_POINT('Ctrl Pts',(-0.275484233991155,-0.374645667829196,
-1.88764745571213));
#51159=CARTESIAN_POINT('Ctrl Pts',(0.165815040869781,-0.434460943954955,
-1.86778027876899));
#51160=CARTESIAN_POINT('Ctrl Pts',(0.455045970085387,-0.0958337347176189,
-1.84791310182585));
#51161=CARTESIAN_POINT('Ctrl Pts',(0.326955964478182,0.330682229478725,
-1.82804592488271));
#51162=CARTESIAN_POINT('Ctrl Pts',(-0.100984117191286,0.453930774101045,
-1.80817874793956));
#51163=CARTESIAN_POINT('Ctrl Pts',(-0.436312047651907,0.160881125911892,
-1.78831157099643));
#51164=CARTESIAN_POINT('Ctrl Pts',(-0.371499852563495,-0.279711993211197,
-1.76844439405328));
#51165=CARTESIAN_POINT('Ctrl Pts',(0.0340134495564639,-0.463782303295574,
-1.74857721711015));
#51166=CARTESIAN_POINT('Ctrl Pts',(0.408333145978101,-0.222519620475373,
-1.728710040167));
#51167=CARTESIAN_POINT('Ctrl Pts',(0.408172061553041,0.222814963071199,
-1.70884286322386));
#51168=CARTESIAN_POINT('Ctrl Pts',(0.0336779261970881,0.463806788315934,
-1.68897568628072));
#51169=CARTESIAN_POINT('Ctrl Pts',(-0.371702107655723,0.279443165536699,
-1.66910850933758));
#51170=CARTESIAN_POINT('Ctrl Pts',(-0.436195547098329,-0.161196725439652,
-1.64924133239443));
#51171=CARTESIAN_POINT('Ctrl Pts',(-0.100655703208124,-0.45400371035109,
-1.6293741554513));
#51172=CARTESIAN_POINT('Ctrl Pts',(0.327195104671456,-0.33044561289252,
-1.60950697850816));
#51173=CARTESIAN_POINT('Ctrl Pts',(0.454976521923715,0.0961629039654941,
-1.58963980156502));
#51174=CARTESIAN_POINT('Ctrl Pts',(0.165500694999069,0.434580785994621,
-1.56977262462187));
#51175=CARTESIAN_POINT('Ctrl Pts',(-0.275755192164056,0.374446275980204,
-1.54990544767873));
#51176=CARTESIAN_POINT('Ctrl Pts',(-0.464117037534976,-0.0290914948161029,
-1.53003827073559));
#51177=CARTESIAN_POINT('Ctrl Pts',(-0.226838906498796,-0.405949565955315,
-1.51017109379245));
#51178=CARTESIAN_POINT('Ctrl Pts',(0.218472326108414,-0.41051282845443,
-1.49030391684931));
#51179=CARTESIAN_POINT('Ctrl Pts',(0.463423416316454,-0.0385963315674505,
-1.47043673990617));
#51180=CARTESIAN_POINT('Ctrl Pts',(0.283370647508505,0.368716714743839,
-1.45056956296303));
#51181=CARTESIAN_POINT('Ctrl Pts',(-0.156560268330182,0.437881059171619,
-1.43070238601989));
#51182=CARTESIAN_POINT('Ctrl Pts',(-0.452910355349746,0.105466343531221,
-1.41083520907674));
#51183=CARTESIAN_POINT('Ctrl Pts',(-0.333898071727896,-0.323671156109517,
-1.3909680321336));
#51184=CARTESIAN_POINT('Ctrl Pts',(0.0913308682086396,-0.455971064995503,
-1.37110085519046));
#51185=CARTESIAN_POINT('Ctrl Pts',(0.432800614998476,-0.17010163802215,
-1.35123367824732));
#51186=CARTESIAN_POINT('Ctrl Pts',(0.377350557819586,0.271767356601424,
-1.33136650130418));
#51187=CARTESIAN_POINT('Ctrl Pts',(-0.0241662660106598,0.464399538315856,
-1.31149932436104));
#51188=CARTESIAN_POINT('Ctrl Pts',(-0.403520298857715,0.231132663227545,
-1.2916321474179));
#51189=CARTESIAN_POINT('Ctrl Pts',(-0.412807394714464,-0.21410510145705,
-1.27176497047476));
#51190=CARTESIAN_POINT('Ctrl Pts',(-0.0435103931630265,-0.462987888921166,
-1.25189779353161));
#51191=CARTESIAN_POINT('Ctrl Pts',(0.365689825080772,-0.28726623789313,
-1.23203061658847));
#51192=CARTESIAN_POINT('Ctrl Pts',(0.439517290481023,0.151906191345506,
-1.21216343964533));
#51193=CARTESIAN_POINT('Ctrl Pts',(0.110265114279544,0.451766028131595,
-1.19229626270219));
#51194=CARTESIAN_POINT('Ctrl Pts',(-0.320110780391191,0.337312952431746,
-1.17242908575905));
#51195=CARTESIAN_POINT('Ctrl Pts',(-0.456914291386833,-0.0864885537360078,
-1.15256190881591));
#51196=CARTESIAN_POINT('Ctrl Pts',(-0.17468343717389,-0.430971735010537,
-1.13269473187277));
#51197=CARTESIAN_POINT('Ctrl Pts',(0.267748935329152,-0.380212371222958,
-1.11282755492963));
#51198=CARTESIAN_POINT('Ctrl Pts',(0.464629773844524,0.0192383174437102,
-1.09296037798648));
#51199=CARTESIAN_POINT('Ctrl Pts',(0.235400407426262,0.401045618084062,
-1.07309320104334));
#51200=CARTESIAN_POINT('Ctrl Pts',(-0.20971378062082,0.415055502094117,
-1.0532260241002));
#51201=CARTESIAN_POINT('Ctrl Pts',(-0.462500255145941,0.0484195579370409,
-1.03335884715706));
#51202=CARTESIAN_POINT('Ctrl Pts',(-0.29112949826634,-0.36262177932395,
-1.01349167021392));
#51203=CARTESIAN_POINT('Ctrl Pts',(0.147235018272768,-0.441104056878981,
-0.993624493270776));
#51204=CARTESIAN_POINT('Ctrl Pts',(0.450570857483482,-0.115051475381576,
-0.97375731632764));
#51205=CARTESIAN_POINT('Ctrl Pts',(0.340689870680686,0.316514378214412,
-0.953890139384495));
#51206=CARTESIAN_POINT('Ctrl Pts',(-0.0816365055196882,0.457806094943495,
-0.934022962441356));
#51207=CARTESIAN_POINT('Ctrl Pts',(-0.429094351859766,0.179245576801561,
-0.914155785498213));
#51208=CARTESIAN_POINT('Ctrl Pts',(-0.383031394111188,-0.263700380595324,
-0.894288608555073));
#51209=CARTESIAN_POINT('Ctrl Pts',(0.0143082037249251,-0.464807718209417,
-0.874421431611931));
#51210=CARTESIAN_POINT('Ctrl Pts',(0.398525802144136,-0.239641658787132,
-0.85455425466879));
#51211=CARTESIAN_POINT('Ctrl Pts',(0.417256897583025,0.205298857815313,
-0.834687077725648));
#51212=CARTESIAN_POINT('Ctrl Pts',(0.0533232733938106,0.461960569870896,
-0.814819900782508));
#51213=CARTESIAN_POINT('Ctrl Pts',(-0.359512922762638,0.294959993842442,
-0.794952723839367));
#51214=CARTESIAN_POINT('Ctrl Pts',(-0.442641179784937,-0.142547274823183,
-0.775085546896225));
#51215=CARTESIAN_POINT('Ctrl Pts',(-0.119824888162353,-0.44932497791433,
-0.755218369953084));
#51216=CARTESIAN_POINT('Ctrl Pts',(0.312882354331519,-0.344028446423828,
-0.735351193009943));
#51217=CARTESIAN_POINT('Ctrl Pts',(0.458646375298876,0.076775269627352,
-0.715484016066801));
#51218=CARTESIAN_POINT('Ctrl Pts',(0.183787543464457,0.42716867683364,-0.69561683912366));
#51219=CARTESIAN_POINT('Ctrl Pts',(-0.259622148038332,0.385807309221348,
-0.67574966218052));
#51220=CARTESIAN_POINT('Ctrl Pts',(-0.464933351385975,-0.00937647970841039,
-0.655882485237378));
#51221=CARTESIAN_POINT('Ctrl Pts',(-0.243855939980186,-0.395961134625949,
-0.636015308294237));
#51222=CARTESIAN_POINT('Ctrl Pts',(0.200860829905182,-0.419411333430728,
-0.616148131351095));
#51223=CARTESIAN_POINT('Ctrl Pts',(0.461368893847993,-0.0582209876456167,
-0.596280954407956));
#51224=CARTESIAN_POINT('Ctrl Pts',(0.298757293496838,0.356363605268922,
-0.576413777464811));
#51225=CARTESIAN_POINT('Ctrl Pts',(-0.13784348852236,0.444128486224894,
-0.556546600521672));
#51226=CARTESIAN_POINT('Ctrl Pts',(-0.44802852973673,0.124584815366827,
-0.53667942357853));
#51227=CARTESIAN_POINT('Ctrl Pts',(-0.347328303740341,-0.30921511743238,
-0.516812246635389));
#51228=CARTESIAN_POINT('Ctrl Pts',(0.071905392806198,-0.459435038021824,
-0.496945069692248));
#51229=CARTESIAN_POINT('Ctrl Pts',(0.425194927333323,-0.1883088257302,-0.477077892749107));
#51230=CARTESIAN_POINT('Ctrl Pts',(0.388539802842457,0.255514696134952,
-0.457210715805966));
#51231=CARTESIAN_POINT('Ctrl Pts',(-0.00444369794125631,0.465006660197467,
-0.437343538862825));
#51232=CARTESIAN_POINT('Ctrl Pts',(-0.393351908929444,0.248042774871675,
-0.417476361919683));
#51233=CARTESIAN_POINT('Ctrl Pts',(-0.421518558049922,-0.196400192834101,
-0.397609184976542));
#51234=CARTESIAN_POINT('Ctrl Pts',(-0.0631121669455817,-0.460725300422581,
-0.377742008033401));
#51235=CARTESIAN_POINT('Ctrl Pts',(0.353174214709179,-0.302520956931872,
-0.35787483109026));
#51236=CARTESIAN_POINT('Ctrl Pts',(0.445565744803263,0.133124163984721,
-0.338007654147118));
#51237=CARTESIAN_POINT('Ctrl Pts',(0.129330843850922,0.446681706278964,
-0.318140477203977));
#51238=CARTESIAN_POINT('Ctrl Pts',(-0.305513314896439,0.350588980455718,
-0.298273300260836));
#51239=CARTESIAN_POINT('Ctrl Pts',(-0.460171545064611,-0.0670272492846139,
-0.278406123317694));
#51240=CARTESIAN_POINT('Ctrl Pts',(-0.192809775000032,-0.423173658350396,
-0.258538946374554));
#51241=CARTESIAN_POINT('Ctrl Pts',(0.251380134241884,-0.391227930132719,
-0.238671769431412));
#51242=CARTESIAN_POINT('Ctrl Pts',(0.465024482747802,-0.000490806679507694,
-0.218804592488271));
#51243=CARTESIAN_POINT('Ctrl Pts',(0.252207730484799,0.39070075510648,-0.19893741554513));
#51244=CARTESIAN_POINT('Ctrl Pts',(-0.191929009959531,0.423573860819181,
-0.179070238601988));
#51245=CARTESIAN_POINT('Ctrl Pts',(-0.460007725025938,0.0680048261882178,
-0.159203061658848));
#51246=CARTESIAN_POINT('Ctrl Pts',(-0.306292952616749,-0.349961511012139,
-0.139335884715706));
#51247=CARTESIAN_POINT('Ctrl Pts',(0.128471060887831,-0.446921381567406,
-0.119468707772565));
#51248=CARTESIAN_POINT('Ctrl Pts',(0.445128579067042,-0.134122670208492,
-0.099601530829424));
#51249=CARTESIAN_POINT('Ctrl Pts',(0.354113939546637,0.301893465535662,
-0.0797343538862821));
#51250=CARTESIAN_POINT('Ctrl Pts',(-0.0627678983065788,0.460626419321466,
-0.0598671769431416));
#51251=CARTESIAN_POINT('Ctrl Pts',(-0.300608260002571,0.285411675199489,
-0.0466223923143805));
#51252=CARTESIAN_POINT('Ctrl Pts',(-0.356151197810523,0.166856867698425,
-0.04));
#51253=CARTESIAN_POINT('Ctrl Pts',(-0.109308770408979,-0.353092386404291,
-2.86733753524613));
#51254=CARTESIAN_POINT('Ctrl Pts',(0.00822782684970018,-0.389478843374481,
-2.86071514293175));
#51255=CARTESIAN_POINT('Ctrl Pts',(0.280459229068676,-0.334997955164989,
-2.84747035830299));
#51256=CARTESIAN_POINT('Ctrl Pts',(0.433829939253691,0.0551670970207491,
-2.82760318135984));
#51257=CARTESIAN_POINT('Ctrl Pts',(0.188343897625126,0.394230945899693,
-2.80773600441671));
#51258=CARTESIAN_POINT('Ctrl Pts',(-0.229372688178782,0.371996470209694,
-2.78786882747356));
#51259=CARTESIAN_POINT('Ctrl Pts',(-0.436990846442185,0.00847695234419238,
-2.76800165053043));
#51260=CARTESIAN_POINT('Ctrl Pts',(-0.243711642890173,-0.362749834245313,
-2.74813447358728));
#51261=CARTESIAN_POINT('Ctrl Pts',(0.173004254002082,-0.401335047727919,
-2.72826729664414));
#51262=CARTESIAN_POINT('Ctrl Pts',(0.431095334602544,-0.0718391713422158,
-2.708400119701));
#51263=CARTESIAN_POINT('Ctrl Pts',(0.293811334647068,0.32353061154742,-2.68853294275786));
#51264=CARTESIAN_POINT('Ctrl Pts',(-0.112915908186665,0.422196671425773,
-2.66866576581472));
#51265=CARTESIAN_POINT('Ctrl Pts',(-0.4160936321099,0.13366516553276,-2.64879858887158));
#51266=CARTESIAN_POINT('Ctrl Pts',(-0.337670729871909,-0.277448800134932,
-2.62893141192843));
#51267=CARTESIAN_POINT('Ctrl Pts',(0.0504272918317754,-0.434116231307584,
-2.6090642349853));
#51268=CARTESIAN_POINT('Ctrl Pts',(0.392279380755707,-0.192656941613362,
-2.58919705804215));
#51269=CARTESIAN_POINT('Ctrl Pts',(0.374373146739222,0.225487105853035,
-2.56932988109901));
#51270=CARTESIAN_POINT('Ctrl Pts',(0.0131309218383279,0.436837883971209,
-2.54946270415587));
#51271=CARTESIAN_POINT('Ctrl Pts',(-0.360153727927074,0.247566241308192,
-2.52959552721272));
#51272=CARTESIAN_POINT('Ctrl Pts',(-0.403142703101535,-0.168747435592608,
-2.50972835026959));
#51273=CARTESIAN_POINT('Ctrl Pts',(-0.0764110618930625,-0.430303493145013,
-2.48986117332644));
#51274=CARTESIAN_POINT('Ctrl Pts',(0.320396889757525,-0.297229840204795,
-2.46999399638331));
#51275=CARTESIAN_POINT('Ctrl Pts',(0.423370060014906,0.108432168946187,
-2.45012681944016));
#51276=CARTESIAN_POINT('Ctrl Pts',(0.138072156670315,0.414651448896828,
-2.43025964249702));
#51277=CARTESIAN_POINT('Ctrl Pts',(-0.273851200504237,0.340595455266087,
-2.41039246555388));
#51278=CARTESIAN_POINT('Ctrl Pts',(-0.434626658297024,-0.0458193391842438,
-2.39052528861074));
#51279=CARTESIAN_POINT('Ctrl Pts',(-0.196807655319557,-0.390213391587604,
-2.37065811166759));
#51280=CARTESIAN_POINT('Ctrl Pts',(0.22150290287941,-0.376744221080646,
-2.35079093472446));
#51281=CARTESIAN_POINT('Ctrl Pts',(0.436673988046143,-0.0177643531276166,
-2.33092375778131));
#51282=CARTESIAN_POINT('Ctrl Pts',(0.251373013583586,0.357507135804446,
-2.31105658083818));
#51283=CARTESIAN_POINT('Ctrl Pts',(-0.164461199132137,0.40491018519923,
-2.29118940389503));
#51284=CARTESIAN_POINT('Ctrl Pts',(-0.429468669307051,0.0809716381180591,
-2.27132222695189));
#51285=CARTESIAN_POINT('Ctrl Pts',(-0.300612050292764,-0.317225691454733,
-2.25145505000875));
#51286=CARTESIAN_POINT('Ctrl Pts',(0.103934740917693,-0.424496541480263,
-2.23158787306561));
#51287=CARTESIAN_POINT('Ctrl Pts',(0.413163375077601,-0.142463221894937,
-2.21172069612247));
#51288=CARTESIAN_POINT('Ctrl Pts',(0.343481443588932,0.270222578643672,
-2.19185351917933));
#51289=CARTESIAN_POINT('Ctrl Pts',(-0.0412060182340209,0.435088276283999,
-2.17198634223619));
#51290=CARTESIAN_POINT('Ctrl Pts',(-0.388103596879385,0.200936164459697,
-2.15211916529305));
#51291=CARTESIAN_POINT('Ctrl Pts',(-0.379072837499258,-0.217493742367056,
-2.1322519883499));
#51292=CARTESIAN_POINT('Ctrl Pts',(-0.0223958152997948,-0.436460962235547,
-2.11238481140677));
#51293=CARTESIAN_POINT('Ctrl Pts',(0.354820324244769,-0.255151487554673,
-2.09251763446362));
#51294=CARTESIAN_POINT('Ctrl Pts',(0.406632088973841,0.160156449496438,
-2.07265045752049));
#51295=CARTESIAN_POINT('Ctrl Pts',(0.0855231057888487,0.428585513608147,
-2.05278328057734));
#51296=CARTESIAN_POINT('Ctrl Pts',(-0.314018793635468,0.303960427263576,
-2.0329161036342));
#51297=CARTESIAN_POINT('Ctrl Pts',(-0.425575247353511,-0.0994256151025911,
-2.01304892669105));
#51298=CARTESIAN_POINT('Ctrl Pts',(-0.146838254390352,-0.411628802619697,
-1.99318174974792));
#51299=CARTESIAN_POINT('Ctrl Pts',(0.266563545248126,-0.34632877507259,
-1.97331457280477));
#51300=CARTESIAN_POINT('Ctrl Pts',(0.435500927650348,0.0365880597219514,
-1.95344739586163));
#51301=CARTESIAN_POINT('Ctrl Pts',(0.205042059583323,0.385950123591584,
-1.93358021891849));
#51302=CARTESIAN_POINT('Ctrl Pts',(-0.213460104345107,0.381358791627395,
-1.91371304197535));
#51303=CARTESIAN_POINT('Ctrl Pts',(-0.436198815460278,0.0270247569754325,
-1.89384586503221));
#51304=CARTESIAN_POINT('Ctrl Pts',(-0.258901245840276,-0.3520935798916,
-1.87397868808907));
#51305=CARTESIAN_POINT('Ctrl Pts',(0.15583367526441,-0.408308228856726,
-1.85411151114593));
#51306=CARTESIAN_POINT('Ctrl Pts',(0.427654123297258,-0.090064948372743,
-1.83424433420278));
#51307=CARTESIAN_POINT('Ctrl Pts',(0.307274595398546,0.310776554973491,
-1.81437715725965));
#51308=CARTESIAN_POINT('Ctrl Pts',(-0.0949052995596975,0.426606057404268,
-1.7945099803165));
#51309=CARTESIAN_POINT('Ctrl Pts',(-0.410047903924069,0.151196761162428,
-1.77464280337336));
#51310=CARTESIAN_POINT('Ctrl Pts',(-0.349137129427362,-0.262874511799361,
-1.75477562643022));
#51311=CARTESIAN_POINT('Ctrl Pts',(0.0319659834536178,-0.435864566121603,
-1.73490844948708));
#51312=CARTESIAN_POINT('Ctrl Pts',(0.383753214040569,-0.209124878510576,
-1.71504127254394));
#51313=CARTESIAN_POINT('Ctrl Pts',(0.383601826218008,0.209402442728685,
-1.6951740956008));
#51314=CARTESIAN_POINT('Ctrl Pts',(0.0316506571843346,0.435887577247082,
-1.67530691865766));
#51315=CARTESIAN_POINT('Ctrl Pts',(-0.349327209616696,0.262621866416228,
-1.65543974171451));
#51316=CARTESIAN_POINT('Ctrl Pts',(-0.409938416212103,-0.151493362930668,
-1.63557256477137));
#51317=CARTESIAN_POINT('Ctrl Pts',(-0.0945966547121861,-0.426674603199902,
-1.61570538782823));
#51318=CARTESIAN_POINT('Ctrl Pts',(0.307499340361523,-0.310554181707088,
-1.59583821088509));
#51319=CARTESIAN_POINT('Ctrl Pts',(0.427588855621798,0.0903743030212203,
-1.57597103394195));
#51320=CARTESIAN_POINT('Ctrl Pts',(0.155538251688356,0.408420856911421,
-1.55610385699881));
#51321=CARTESIAN_POINT('Ctrl Pts',(-0.259155893474801,0.351906190590346,
-1.53623668005567));
#51322=CARTESIAN_POINT('Ctrl Pts',(-0.436179150772605,-0.0273403096145494,
-1.51636950311253));
#51323=CARTESIAN_POINT('Ctrl Pts',(-0.213184161745785,-0.381513115474785,
-1.49650232616938));
#51324=CARTESIAN_POINT('Ctrl Pts',(0.205321214182107,-0.385801688831601,
-1.47663514922625));
#51325=CARTESIAN_POINT('Ctrl Pts',(0.435527282623873,-0.0362729953104975,
-1.4567679722831));
#51326=CARTESIAN_POINT('Ctrl Pts',(0.266312930550041,0.346521524757669,
-1.43690079533996));
#51327=CARTESIAN_POINT('Ctrl Pts',(-0.147136000970108,0.411522467572615,
-1.41703361839682));
#51328=CARTESIAN_POINT('Ctrl Pts',(-0.425647063554919,0.0991177147920855,
-1.39716644145368));
#51329=CARTESIAN_POINT('Ctrl Pts',(-0.313798817092356,-0.304187518629494,
-1.37729926451054));
#51330=CARTESIAN_POINT('Ctrl Pts',(0.085833135422371,-0.42852353139833,
-1.3574320875674));
#51331=CARTESIAN_POINT('Ctrl Pts',(0.406747844695681,-0.159862237360634,
-1.33756491062426));
#51332=CARTESIAN_POINT('Ctrl Pts',(0.35463564692109,0.255408108781595,-1.31769773368111));
#51333=CARTESIAN_POINT('Ctrl Pts',(-0.0227115587952971,0.436444646198827,
-1.29783055673797));
#51334=CARTESIAN_POINT('Ctrl Pts',(-0.379230080003261,0.217219452442108,
-1.27796337979483));
#51335=CARTESIAN_POINT('Ctrl Pts',(-0.38795813188745,-0.201216878022024,
-1.25809620285169));
#51336=CARTESIAN_POINT('Ctrl Pts',(-0.0408912511387834,-0.435117972139552,
-1.23822902590855));
#51337=CARTESIAN_POINT('Ctrl Pts',(0.343676841076736,-0.269974022835617,
-1.21836184896541));
#51338=CARTESIAN_POINT('Ctrl Pts',(0.41306020466323,0.142762079776462,-1.19849467202227));
#51339=CARTESIAN_POINT('Ctrl Pts',(0.103627619795515,0.424571620005444,
-1.17862749507913));
#51340=CARTESIAN_POINT('Ctrl Pts',(-0.300841462502146,0.317008136391009,
-1.15876031813598));
#51341=CARTESIAN_POINT('Ctrl Pts',(-0.429409979541973,-0.0812823078430504,
-1.13889314119285));
#51342=CARTESIAN_POINT('Ctrl Pts',(-0.164168231541823,-0.40502905556387,
-1.1190259642497));
#51343=CARTESIAN_POINT('Ctrl Pts',(0.251631579509376,-0.357325191236424,
-1.09915878730656));
#51344=CARTESIAN_POINT('Ctrl Pts',(0.436661022520423,0.0180802519327009,
-1.07929161036342));
#51345=CARTESIAN_POINT('Ctrl Pts',(0.221230296452916,0.376904364567306,
-1.05942443342028));
#51346=CARTESIAN_POINT('Ctrl Pts',(-0.197089896165702,0.390070912691426,
-1.03955725647714));
#51347=CARTESIAN_POINT('Ctrl Pts',(-0.434659691859441,0.0455049049134983,
-1.019690079534));
#51348=CARTESIAN_POINT('Ctrl Pts',(-0.27360473124001,-0.340793478725185,
-0.999822902590856));
#51349=CARTESIAN_POINT('Ctrl Pts',(0.138372091607098,-0.414551454421289,
-0.979955725647713));
#51350=CARTESIAN_POINT('Ctrl Pts',(0.423448393585894,-0.108125862160985,
-0.960088548704574));
#51351=CARTESIAN_POINT('Ctrl Pts',(0.320181778414311,0.297461548557087,
-0.940221371761431));
#51352=CARTESIAN_POINT('Ctrl Pts',(-0.0767223324503298,0.430248100288556,
-0.920354194818291));
#51353=CARTESIAN_POINT('Ctrl Pts',(-0.40326468295491,0.168455749619316,
-0.900487017875149));
#51354=CARTESIAN_POINT('Ctrl Pts',(-0.359974520845024,-0.247826730682804,
-0.880619840932009));
#51355=CARTESIAN_POINT('Ctrl Pts',(0.0134469102512725,-0.436828255385598,
-0.860752663988866));
#51356=CARTESIAN_POINT('Ctrl Pts',(0.374536230911585,-0.225216242382897,
-0.840885487045726));
#51357=CARTESIAN_POINT('Ctrl Pts',(0.392139793463325,0.192940733079036,
-0.821018310102584));
#51358=CARTESIAN_POINT('Ctrl Pts',(0.0501134373968655,0.434152493360106,
-0.801151133159443));
#51359=CARTESIAN_POINT('Ctrl Pts',(-0.337871762207323,0.277204647149791,
-0.781283956216302));
#51360=CARTESIAN_POINT('Ctrl Pts',(-0.415996049016037,-0.133966530527635,
-0.76141677927316));
#51361=CARTESIAN_POINT('Ctrl Pts',(-0.112611935639486,-0.422277510708325,
-0.74154960233002));
#51362=CARTESIAN_POINT('Ctrl Pts',(0.294048157182272,-0.323319385988831,
-0.721682425386878));
#51363=CARTESIAN_POINT('Ctrl Pts',(0.431037799313113,0.0721537224409103,
-0.701815248443737));
#51364=CARTESIAN_POINT('Ctrl Pts',(0.172724309059369,0.401454925437667,
-0.681948071500596));
#51365=CARTESIAN_POINT('Ctrl Pts',(-0.243993990512759,0.362583337581848,
-0.662080894557455));
#51366=CARTESIAN_POINT('Ctrl Pts',(-0.436946325975187,-0.00881205520524107,
-0.642213717614313));
#51367=CARTESIAN_POINT('Ctrl Pts',(-0.229176841635333,-0.372125945553308,
-0.622346540671172));
#51368=CARTESIAN_POINT('Ctrl Pts',(0.188769855717525,-0.394164541366216,
-0.602479363728031));
#51369=CARTESIAN_POINT('Ctrl Pts',(0.433596433736497,-0.0547163299224792,
-0.58261218678489));
#51370=CARTESIAN_POINT('Ctrl Pts',(0.280773365392242,0.334912020334415,
-0.562745009841748));
#51371=CARTESIAN_POINT('Ctrl Pts',(-0.129545892308867,0.417393825885778,
-0.542877832898608));
#51372=CARTESIAN_POINT('Ctrl Pts',(-0.421059103239103,0.117085335316459,
-0.523010655955466));
#51373=CARTESIAN_POINT('Ctrl Pts',(-0.326420605822587,-0.290601672466167,
-0.503143479012325));
#51374=CARTESIAN_POINT('Ctrl Pts',(0.0675769916501168,-0.431778987868845,
-0.483276302069183));
#51375=CARTESIAN_POINT('Ctrl Pts',(0.39959998732667,-0.176973429215675,
-0.463409125126043));
#51376=CARTESIAN_POINT('Ctrl Pts',(0.365151346619992,0.240133789877654,
-0.443541948182901));
#51377=CARTESIAN_POINT('Ctrl Pts',(-0.00417620608069359,0.437015221905641,
-0.42367477123976));
#51378=CARTESIAN_POINT('Ctrl Pts',(-0.369673784230984,0.233111646737714,
-0.403807594296618));
#51379=CARTESIAN_POINT('Ctrl Pts',(-0.39614491995729,-0.184577730171128,
-0.383940417353478));
#51380=CARTESIAN_POINT('Ctrl Pts',(-0.0593130808727705,-0.432991581918882,
-0.364073240410336));
#51381=CARTESIAN_POINT('Ctrl Pts',(0.331914617624918,-0.284310472173769,
-0.344206063467196));
#51382=CARTESIAN_POINT('Ctrl Pts',(0.418744567563962,0.125110651189557,
-0.324338886524053));
#51383=CARTESIAN_POINT('Ctrl Pts',(0.121545672917358,0.41979335286896,-0.304471709580913));
#51384=CARTESIAN_POINT('Ctrl Pts',(-0.287122702818704,0.329485003562026,
-0.284604532637771));
#51385=CARTESIAN_POINT('Ctrl Pts',(-0.43247116029623,-0.0629924917793682,
-0.26473735569463));
#51386=CARTESIAN_POINT('Ctrl Pts',(-0.181203440336604,-0.397700390205352,
-0.244870178751489));
#51387=CARTESIAN_POINT('Ctrl Pts',(0.236248111159817,-0.367677659993151,
-0.225003001808348));
#51388=CARTESIAN_POINT('Ctrl Pts',(0.43703197161367,-0.00046126218894694,
-0.205135824865206));
#51389=CARTESIAN_POINT('Ctrl Pts',(0.237025889601942,0.367182218678445,
-0.185268647922066));
#51390=CARTESIAN_POINT('Ctrl Pts',(-0.1803756936341,0.398076502174651,-0.165401470978924));
#51391=CARTESIAN_POINT('Ctrl Pts',(-0.432317201532449,0.0639112226794298,
-0.145534294035783));
#51392=CARTESIAN_POINT('Ctrl Pts',(-0.287855409638866,-0.328895305130591,
-0.125667117092642));
#51393=CARTESIAN_POINT('Ctrl Pts',(0.120737645259763,-0.420018600716635,
-0.1057999401495));
#51394=CARTESIAN_POINT('Ctrl Pts',(0.418333717359917,-0.126049051553048,
-0.0859327632063595));
#51395=CARTESIAN_POINT('Ctrl Pts',(0.332797774993454,0.28372075311116,-0.0660655862632178));
#51396=CARTESIAN_POINT('Ctrl Pts',(-0.0589895357527821,0.432898653042708,
-0.0461984093200771));
#51397=CARTESIAN_POINT('Ctrl Pts',(-0.282512911526698,0.268231096988586,
-0.0329536246913161));
#51398=CARTESIAN_POINT('Ctrl Pts',(-0.334712398908504,0.156812788515205,
-0.0263312323769356));
#51399=CARTESIAN_POINT('Ctrl Pts',(-0.102307390254951,-0.330476323507783,
-2.85366876762306));
#51400=CARTESIAN_POINT('Ctrl Pts',(0.0077008229926378,-0.36453217684248,
-2.84704637530868));
#51401=CARTESIAN_POINT('Ctrl Pts',(0.262495421836479,-0.313540865983978,
-2.83380159067992));
#51402=CARTESIAN_POINT('Ctrl Pts',(0.406042522786106,0.0516335670323386,
-2.81393441373678));
#51403=CARTESIAN_POINT('Ctrl Pts',(0.176280206651099,0.368979900531617,
-2.79406723679364));
#51404=CARTESIAN_POINT('Ctrl Pts',(-0.21468104558796,0.348169574214524,
-2.7742000598505));
#51405=CARTESIAN_POINT('Ctrl Pts',(-0.409000969433003,0.00793399164957273,
-2.75433288290736));
#51406=CARTESIAN_POINT('Ctrl Pts',(-0.228101570126088,-0.339515198260848,
-2.73446570596422));
#51407=CARTESIAN_POINT('Ctrl Pts',(0.161923088730525,-0.375628974667497,
-2.71459852902108));
#51408=CARTESIAN_POINT('Ctrl Pts',(0.403483073400745,-0.0672377715951021,
-2.69473135207793));
#51409=CARTESIAN_POINT('Ctrl Pts',(0.27499230631357,0.302808021818952,-2.6748641751348));
#51410=CARTESIAN_POINT('Ctrl Pts',(-0.105683485795541,0.395154382089269,
-2.65499699819165));
#51411=CARTESIAN_POINT('Ctrl Pts',(-0.389442251006885,0.125103724088085,
-2.63512982124851));
#51412=CARTESIAN_POINT('Ctrl Pts',(-0.316042445719816,-0.259677815100926,
-2.61526264430537));
#51413=CARTESIAN_POINT('Ctrl Pts',(0.0471973530177957,-0.406310477432151,
-2.59539546736223));
#51414=CARTESIAN_POINT('Ctrl Pts',(0.367153335874026,-0.180316994118749,
-2.57552829041909));
#51415=CARTESIAN_POINT('Ctrl Pts',(0.350394021276791,0.211044340263396,
-2.55566111347595));
#51416=CARTESIAN_POINT('Ctrl Pts',(0.0122898678659977,0.408857804422968,
-2.5357939365328));
#51417=CARTESIAN_POINT('Ctrl Pts',(-0.337085376195796,0.231709276105699,
-2.51592675958967));
#51418=CARTESIAN_POINT('Ctrl Pts',(-0.37732084717748,-0.157938925514407,
-2.49605958264652));
#51419=CARTESIAN_POINT('Ctrl Pts',(-0.0715168261397497,-0.402741950499878,
-2.47619240570338));
#51420=CARTESIAN_POINT('Ctrl Pts',(0.29987501930772,-0.278191851792624,
-2.45632522876024));
#51421=CARTESIAN_POINT('Ctrl Pts',(0.396252613492476,0.101486936346117,
-2.4364580518171));
#51422=CARTESIAN_POINT('Ctrl Pts',(0.12922844125829,0.388092441652642,-2.41659087487395));
#51423=CARTESIAN_POINT('Ctrl Pts',(-0.256310646775627,0.318779838347793,
-2.39672369793082));
#51424=CARTESIAN_POINT('Ctrl Pts',(-0.406788210856558,-0.042884546204367,
-2.37685652098767));
#51425=CARTESIAN_POINT('Ctrl Pts',(-0.184201848786746,-0.365219676211651,
-2.35698934404454));
#51426=CARTESIAN_POINT('Ctrl Pts',(0.207315331081859,-0.352613224978964,
-2.33712216710139));
#51427=CARTESIAN_POINT('Ctrl Pts',(0.408704406261923,-0.016626521378421,
-2.31725499015826));
#51428=CARTESIAN_POINT('Ctrl Pts',(0.235272219274242,0.334608302012981,
-2.29738781321511));
#51429=CARTESIAN_POINT('Ctrl Pts',(-0.153927228514745,0.378975119566246,
-2.27752063627197));
#51430=CARTESIAN_POINT('Ctrl Pts',(-0.40196059830037,0.0757852910569974,
-2.25765345932882));
#51431=CARTESIAN_POINT('Ctrl Pts',(-0.281357426577698,-0.296906940706838,
-2.23778628238569));
#51432=CARTESIAN_POINT('Ctrl Pts',(0.0972775748947614,-0.397306942239017,
-2.21791910544254));
#51433=CARTESIAN_POINT('Ctrl Pts',(0.386699681049972,-0.133338252592638,
-2.19805192849941));
#51434=CARTESIAN_POINT('Ctrl Pts',(0.32148097506822,0.252914443237818,-2.17818475155626));
#51435=CARTESIAN_POINT('Ctrl Pts',(-0.038566714935569,0.40722026156361,
-2.15831757461312));
#51436=CARTESIAN_POINT('Ctrl Pts',(-0.363245016815483,0.188065921122305,
-2.13845039766998));
#51437=CARTESIAN_POINT('Ctrl Pts',(-0.354792690247869,-0.203562962926974,
-2.11858322072684));
#51438=CARTESIAN_POINT('Ctrl Pts',(-0.0209613318984479,-0.408505025053466,
-2.0987160437837));
#51439=CARTESIAN_POINT('Ctrl Pts',(0.332093584504505,-0.238808676684583,
-2.07884886684056));
#51440=CARTESIAN_POINT('Ctrl Pts',(0.380586732987488,0.149898204134711,
-2.05898168989742));
#51441=CARTESIAN_POINT('Ctrl Pts',(0.0800452308357175,0.401134009963445,
-2.03911451295428));
#51442=CARTESIAN_POINT('Ctrl Pts',(-0.293905449193615,0.284491335304253,
-2.01924733601113));
#51443=CARTESIAN_POINT('Ctrl Pts',(-0.398316555487175,-0.0930572649164465,
-1.99938015906799));
#51444=CARTESIAN_POINT('Ctrl Pts',(-0.137433058116583,-0.385263400111692,
-1.97951298212485));
#51445=CARTESIAN_POINT('Ctrl Pts',(0.249489776066525,-0.324145930974265,
-1.95964580518171));
#51446=CARTESIAN_POINT('Ctrl Pts',(0.407606482030808,0.0342445431472686,
-1.93977862823857));
#51447=CARTESIAN_POINT('Ctrl Pts',(0.191908827900848,0.361229476514057,
-1.91991145129543));
#51448=CARTESIAN_POINT('Ctrl Pts',(-0.199787685081339,0.356932225805877,
-1.90004427435229));
#51449=CARTESIAN_POINT('Ctrl Pts',(-0.408259669147063,0.025293783363276,
-1.88017709740914));
#51450=CARTESIAN_POINT('Ctrl Pts',(-0.242318257689397,-0.329541491954005,
-1.860309920466));
#51451=CARTESIAN_POINT('Ctrl Pts',(0.14585230965904,-0.382155513758496,
-1.84044274352286));
#51452=CARTESIAN_POINT('Ctrl Pts',(0.400262276509128,-0.0842961620278672,
-1.82057556657972));
#51453=CARTESIAN_POINT('Ctrl Pts',(0.287593226318909,0.290870880468256,
-1.80070838963658));
#51454=CARTESIAN_POINT('Ctrl Pts',(-0.0888264819281091,0.399281340707492,
-1.78084121269344));
#51455=CARTESIAN_POINT('Ctrl Pts',(-0.38378376019623,0.141512396412965,
-1.7609740357503));
#51456=CARTESIAN_POINT('Ctrl Pts',(-0.32677440629123,-0.246037030387525,
-1.74110685880716));
#51457=CARTESIAN_POINT('Ctrl Pts',(0.0299185173507721,-0.407946828947632,
-1.72123968186402));
#51458=CARTESIAN_POINT('Ctrl Pts',(0.359173282103036,-0.19573013654578,
-1.70137250492087));
#51459=CARTESIAN_POINT('Ctrl Pts',(0.359031590882975,0.195989922386171,
-1.68150532797773));
#51460=CARTESIAN_POINT('Ctrl Pts',(0.0296233881715808,0.407968366178229,
-1.66163815103459));
#51461=CARTESIAN_POINT('Ctrl Pts',(-0.326952311577669,0.245800567295756,
-1.64177097409145));
#51462=CARTESIAN_POINT('Ctrl Pts',(-0.383681285325876,-0.141790000421682,
-1.62190379714831));
#51463=CARTESIAN_POINT('Ctrl Pts',(-0.0885376062162486,-0.399345496048715,
-1.60203662020517));
#51464=CARTESIAN_POINT('Ctrl Pts',(0.28780357605159,-0.290662750521656,
-1.58216944326203));
#51465=CARTESIAN_POINT('Ctrl Pts',(0.400201189319881,0.0845857020769455,
-1.56230226631889));
#51466=CARTESIAN_POINT('Ctrl Pts',(0.145575808377645,0.382260927828221,
-1.54243508937574));
#51467=CARTESIAN_POINT('Ctrl Pts',(-0.242556594785546,0.329366105200487,
-1.5225679124326));
#51468=CARTESIAN_POINT('Ctrl Pts',(-0.408241264010235,-0.0255891244129948,
-1.50270073548946));
#51469=CARTESIAN_POINT('Ctrl Pts',(-0.199529416992774,-0.357076664994257,
-1.48283355854632));
#51470=CARTESIAN_POINT('Ctrl Pts',(0.192170102255799,-0.361090549208772,
-1.46296638160318));
#51471=CARTESIAN_POINT('Ctrl Pts',(0.407631148931293,-0.0339496590535454,
-1.44309920466004));
#51472=CARTESIAN_POINT('Ctrl Pts',(0.249255213591577,0.3243263347715,-1.4232320277169));
#51473=CARTESIAN_POINT('Ctrl Pts',(-0.137711733610034,0.385163875973612,
-1.40336485077376));
#51474=CARTESIAN_POINT('Ctrl Pts',(-0.398383771760093,0.092769086052951,
-1.38349767383061));
#51475=CARTESIAN_POINT('Ctrl Pts',(-0.293699562456816,-0.284703881149472,
-1.36363049688748));
#51476=CARTESIAN_POINT('Ctrl Pts',(0.0803354026361021,-0.401075997801155,
-1.34376331994433));
#51477=CARTESIAN_POINT('Ctrl Pts',(0.380695074392888,-0.149622836699118,
-1.32389614300119));
#51478=CARTESIAN_POINT('Ctrl Pts',(0.331920736022593,0.239048860961766,
-1.30402896605805));
#51479=CARTESIAN_POINT('Ctrl Pts',(-0.0212568515799336,0.408489754081796,
-1.28416178911491));
#51480=CARTESIAN_POINT('Ctrl Pts',(-0.354939861148809,0.203306241656672,
-1.26429461217177));
#51481=CARTESIAN_POINT('Ctrl Pts',(-0.363108869060434,-0.188328654586999,
-1.24442743522863));
#51482=CARTESIAN_POINT('Ctrl Pts',(-0.0382721091145412,-0.407248055357939,
-1.22456025828549));
#51483=CARTESIAN_POINT('Ctrl Pts',(0.321663857072701,-0.252681807778104,
-1.20469308134234));
#51484=CARTESIAN_POINT('Ctrl Pts',(0.386603118845436,0.133617968207419,
-1.1848259043992));
#51485=CARTESIAN_POINT('Ctrl Pts',(0.0969901253114878,0.397377211879292,
-1.16495872745606));
#51486=CARTESIAN_POINT('Ctrl Pts',(-0.281572144613101,0.296703320350273,
-1.14509155051292));
#51487=CARTESIAN_POINT('Ctrl Pts',(-0.401905667697113,-0.0760760619500936,
-1.12522437356978));
#51488=CARTESIAN_POINT('Ctrl Pts',(-0.153653025909756,-0.379086376117202,
-1.10535719662664));
#51489=CARTESIAN_POINT('Ctrl Pts',(0.235514223689601,-0.334438011249891,
-1.0854900196835));
#51490=CARTESIAN_POINT('Ctrl Pts',(0.408692271196321,0.0169221864216921,
-1.06562284274035));
#51491=CARTESIAN_POINT('Ctrl Pts',(0.207060185479571,0.35276311105055,-1.04575566579722));
#51492=CARTESIAN_POINT('Ctrl Pts',(-0.184466011710584,0.365086323288736,
-1.02588848885407));
#51493=CARTESIAN_POINT('Ctrl Pts',(-0.406819128572942,0.0425902518899552,
-1.00602131191093));
#51494=CARTESIAN_POINT('Ctrl Pts',(-0.25607996421368,-0.31896517812642,
-0.986154134967791));
#51495=CARTESIAN_POINT('Ctrl Pts',(0.129509164941429,-0.387998851963599,
-0.966286958024649));
#51496=CARTESIAN_POINT('Ctrl Pts',(0.396325929688306,-0.101200248940393,
-0.946419781081509));
#51497=CARTESIAN_POINT('Ctrl Pts',(0.299673686147936,0.278408718899761,
-0.926552604138367));
#51498=CARTESIAN_POINT('Ctrl Pts',(-0.0718081593809718,0.402690105633617,
-0.906685427195226));
#51499=CARTESIAN_POINT('Ctrl Pts',(-0.377435014050053,0.157665922437071,
-0.886818250252085));
#51500=CARTESIAN_POINT('Ctrl Pts',(-0.33691764757886,-0.231953080770283,
-0.866951073308944));
#51501=CARTESIAN_POINT('Ctrl Pts',(0.0125856167776199,-0.408848792561779,
-0.847083896365802));
#51502=CARTESIAN_POINT('Ctrl Pts',(0.350546659679034,-0.210790825978663,
-0.827216719422662));
#51503=CARTESIAN_POINT('Ctrl Pts',(0.367022689343624,0.18058260834276,-0.80734954247952));
#51504=CARTESIAN_POINT('Ctrl Pts',(0.0469036013999205,0.406344416849317,
-0.787482365536379));
#51505=CARTESIAN_POINT('Ctrl Pts',(-0.316230601652008,0.259449300457139,
-0.767615188593238));
#51506=CARTESIAN_POINT('Ctrl Pts',(-0.389350918247137,-0.125385786232088,
-0.747748011650096));
#51507=CARTESIAN_POINT('Ctrl Pts',(-0.105398983116618,-0.39523004350232,
-0.727880834706955));
#51508=CARTESIAN_POINT('Ctrl Pts',(0.275213960033025,-0.302610325553834,
-0.708013657763814));
#51509=CARTESIAN_POINT('Ctrl Pts',(0.403429223327349,0.0675321752544685,
-0.688146480820672));
#51510=CARTESIAN_POINT('Ctrl Pts',(0.161661074654281,0.375741174041693,
-0.668279303877532));
#51511=CARTESIAN_POINT('Ctrl Pts',(-0.228365832987187,0.339359365942348,
-0.64841212693439));
#51512=CARTESIAN_POINT('Ctrl Pts',(-0.408959300564399,-0.00824763070207162,
-0.628544949991249));
#51513=CARTESIAN_POINT('Ctrl Pts',(-0.214497743290479,-0.348290756480668,
-0.608677773048107));
#51514=CARTESIAN_POINT('Ctrl Pts',(0.176678881529869,-0.368917749301704,
-0.588810596104967));
#51515=CARTESIAN_POINT('Ctrl Pts',(0.405823973625002,-0.0512116721993414,
-0.568943419161826));
#51516=CARTESIAN_POINT('Ctrl Pts',(0.262789437287646,0.313460435399907,
-0.549076242218683));
#51517=CARTESIAN_POINT('Ctrl Pts',(-0.121248296095373,0.390659165546662,
-0.529209065275544));
#51518=CARTESIAN_POINT('Ctrl Pts',(-0.394089676741475,0.109585855266091,
-0.509341888332401));
#51519=CARTESIAN_POINT('Ctrl Pts',(-0.305512907904833,-0.271988227499954,
-0.48947471138926));
#51520=CARTESIAN_POINT('Ctrl Pts',(0.0632485904940357,-0.404122937715866,
-0.469607534446119));
#51521=CARTESIAN_POINT('Ctrl Pts',(0.374005047320018,-0.165638032701151,
-0.449740357502979));
#51522=CARTESIAN_POINT('Ctrl Pts',(0.341762890397528,0.224752883620358,
-0.429873180559837));
#51523=CARTESIAN_POINT('Ctrl Pts',(-0.00390871422013135,0.409023783613815,
-0.410006003616696));
#51524=CARTESIAN_POINT('Ctrl Pts',(-0.345995659532523,0.218180518603753,
-0.390138826673554));
#51525=CARTESIAN_POINT('Ctrl Pts',(-0.370771281864659,-0.172755267508155,
-0.370271649730414));
#51526=CARTESIAN_POINT('Ctrl Pts',(-0.0555139947999592,-0.405257863415184,
-0.350404472787271));
#51527=CARTESIAN_POINT('Ctrl Pts',(0.310655020540657,-0.266099987415665,
-0.330537295844131));
#51528=CARTESIAN_POINT('Ctrl Pts',(0.39192339032466,0.117097138394392,-0.310670118900989));
#51529=CARTESIAN_POINT('Ctrl Pts',(0.113760501983795,0.392904999458956,
-0.290802941957848));
#51530=CARTESIAN_POINT('Ctrl Pts',(-0.268732090740969,0.308381026668334,
-0.270935765014708));
#51531=CARTESIAN_POINT('Ctrl Pts',(-0.404770775527847,-0.0589577342741226,
-0.251068588071565));
#51532=CARTESIAN_POINT('Ctrl Pts',(-0.169597105673178,-0.372227122060309,
-0.231201411128425));
#51533=CARTESIAN_POINT('Ctrl Pts',(0.221116088077751,-0.344127389853583,
-0.211334234185283));
#51534=CARTESIAN_POINT('Ctrl Pts',(0.409039460479538,-0.000431717698386653,
-0.191467057242142));
#51535=CARTESIAN_POINT('Ctrl Pts',(0.221844048719085,0.343663682250411,
-0.171599880299001));
#51536=CARTESIAN_POINT('Ctrl Pts',(-0.168822377308669,0.372579143530119,
-0.151732703355859));
#51537=CARTESIAN_POINT('Ctrl Pts',(-0.404626678038961,0.0598176191706426,
-0.131865526412719));
#51538=CARTESIAN_POINT('Ctrl Pts',(-0.269417866660982,-0.307829099249045,
-0.111998349469577));
#51539=CARTESIAN_POINT('Ctrl Pts',(0.113004229631694,-0.393115819865864,
-0.0921311725264359));
#51540=CARTESIAN_POINT('Ctrl Pts',(0.391538855652792,-0.117975432897604,
-0.0722639955832951));
#51541=CARTESIAN_POINT('Ctrl Pts',(0.311481610440272,0.265548040686658,
-0.0523968186401534));
#51542=CARTESIAN_POINT('Ctrl Pts',(-0.0552111731989857,0.405170886763949,
-0.0325296416970127));
#51543=CARTESIAN_POINT('Ctrl Pts',(-0.264417563050825,0.251050518777684,
-0.0192848570682517));
#51544=CARTESIAN_POINT('Ctrl Pts',(-0.313273600006485,0.146768709331986,
-0.0126624647538713));
#51545=CARTESIAN_POINT('Ctrl Pts',(-0.0953060101009229,-0.307860260611276,
-2.84));
#51546=CARTESIAN_POINT('Ctrl Pts',(0.00717381913557572,-0.339585510310479,
-2.83337760768562));
#51547=CARTESIAN_POINT('Ctrl Pts',(0.244531614604281,-0.292083776802967,
-2.82013282305686));
#51548=CARTESIAN_POINT('Ctrl Pts',(0.378255106318521,0.0481000370439281,
-2.80026564611372));
#51549=CARTESIAN_POINT('Ctrl Pts',(0.164216515677071,0.34372885516354,-2.78039846917058));
#51550=CARTESIAN_POINT('Ctrl Pts',(-0.199989402997138,0.324342678219355,
-2.76053129222744));
#51551=CARTESIAN_POINT('Ctrl Pts',(-0.381011092423822,0.00739103095495322,
-2.74066411528429));
#51552=CARTESIAN_POINT('Ctrl Pts',(-0.212491497362003,-0.316280562276384,
-2.72079693834115));
#51553=CARTESIAN_POINT('Ctrl Pts',(0.150841923458968,-0.349922901607075,
-2.70092976139801));
#51554=CARTESIAN_POINT('Ctrl Pts',(0.375870812198945,-0.0626363718479885,
-2.68106258445487));
#51555=CARTESIAN_POINT('Ctrl Pts',(0.256173277980071,0.282085432090484,
-2.66119540751173));
#51556=CARTESIAN_POINT('Ctrl Pts',(-0.0984510634044162,0.368112092752765,
-2.64132823056859));
#51557=CARTESIAN_POINT('Ctrl Pts',(-0.36279086990387,0.11654228264341,-2.62146105362545));
#51558=CARTESIAN_POINT('Ctrl Pts',(-0.294414161567723,-0.24190683006692,
-2.60159387668231));
#51559=CARTESIAN_POINT('Ctrl Pts',(0.0439674142038161,-0.378504723556717,
-2.58172669973917));
#51560=CARTESIAN_POINT('Ctrl Pts',(0.342027290992345,-0.167977046624136,
-2.56185952279602));
#51561=CARTESIAN_POINT('Ctrl Pts',(0.32641489581436,0.196601574673756,-2.54199234585288));
#51562=CARTESIAN_POINT('Ctrl Pts',(0.0114488138936679,0.380877724874727,
-2.52212516890974));
#51563=CARTESIAN_POINT('Ctrl Pts',(-0.314017024464519,0.215852310903206,
-2.5022579919666));
#51564=CARTESIAN_POINT('Ctrl Pts',(-0.351498991253425,-0.147130415436207,
-2.48239081502346));
#51565=CARTESIAN_POINT('Ctrl Pts',(-0.066622590386437,-0.375180407854742,
-2.46252363808032));
#51566=CARTESIAN_POINT('Ctrl Pts',(0.279353148857915,-0.259153863380453,
-2.44265646113718));
#51567=CARTESIAN_POINT('Ctrl Pts',(0.369135166970047,0.0945417037460469,
-2.42278928419404));
#51568=CARTESIAN_POINT('Ctrl Pts',(0.120384725846265,0.361533434408456,
-2.40292210725089));
#51569=CARTESIAN_POINT('Ctrl Pts',(-0.238770093047016,0.296964221429498,
-2.38305493030775));
#51570=CARTESIAN_POINT('Ctrl Pts',(-0.378949763416092,-0.0399497532244903,
-2.36318775336461));
#51571=CARTESIAN_POINT('Ctrl Pts',(-0.171596042253934,-0.340225960835699,
-2.34332057642147));
#51572=CARTESIAN_POINT('Ctrl Pts',(0.193127759284308,-0.328482228877282,
-2.32345339947833));
#51573=CARTESIAN_POINT('Ctrl Pts',(0.380734824477702,-0.0154886896292257,
-2.30358622253519));
#51574=CARTESIAN_POINT('Ctrl Pts',(0.219171424964897,0.311709468221516,
-2.28371904559205));
#51575=CARTESIAN_POINT('Ctrl Pts',(-0.143393257897354,0.353040053933262,
-2.2638518686489));
#51576=CARTESIAN_POINT('Ctrl Pts',(-0.374452527293689,0.0705989439959352,
-2.24398469170576));
#51577=CARTESIAN_POINT('Ctrl Pts',(-0.262102802862633,-0.276588189958943,
-2.22411751476262));
#51578=CARTESIAN_POINT('Ctrl Pts',(0.090620408871829,-0.370117342997772,
-2.20425033781948));
#51579=CARTESIAN_POINT('Ctrl Pts',(0.360235987022344,-0.124213283290337,
-2.18438316087634));
#51580=CARTESIAN_POINT('Ctrl Pts',(0.299480506547509,0.235606307831963,
-2.1645159839332));
#51581=CARTESIAN_POINT('Ctrl Pts',(-0.0359274116371167,0.379352246843221,
-2.14464880699006));
#51582=CARTESIAN_POINT('Ctrl Pts',(-0.338386436751582,0.175195677784914,
-2.12478163004692));
#51583=CARTESIAN_POINT('Ctrl Pts',(-0.330512542996479,-0.189632183486893,
-2.10491445310378));
#51584=CARTESIAN_POINT('Ctrl Pts',(-0.0195268484971016,-0.380549087871386,
-2.08504727616063));
#51585=CARTESIAN_POINT('Ctrl Pts',(0.309366844764242,-0.222465865814493,
-2.06518009921749));
#51586=CARTESIAN_POINT('Ctrl Pts',(0.354541377001136,0.139639958772985,
-2.04531292227435));
#51587=CARTESIAN_POINT('Ctrl Pts',(0.0745673558825864,0.373682506318743,
-2.02544574533121));
#51588=CARTESIAN_POINT('Ctrl Pts',(-0.273792104751763,0.265022243344928,
-2.00557856838807));
#51589=CARTESIAN_POINT('Ctrl Pts',(-0.371057863620839,-0.0866889147303015,
-1.98571139144493));
#51590=CARTESIAN_POINT('Ctrl Pts',(-0.128027861842815,-0.358897997603687,
-1.96584421450179));
#51591=CARTESIAN_POINT('Ctrl Pts',(0.232416006884924,-0.301963086875939,
-1.94597703755865));
#51592=CARTESIAN_POINT('Ctrl Pts',(0.37971203641127,0.0319010265725857,
-1.9261098606155));
#51593=CARTESIAN_POINT('Ctrl Pts',(0.178775596218371,0.336508829436531,
-1.90624268367236));
#51594=CARTESIAN_POINT('Ctrl Pts',(-0.18611526581757,0.332505659984359,
-1.88637550672922));
#51595=CARTESIAN_POINT('Ctrl Pts',(-0.380320522833848,0.0235628097511194,
-1.86650832978608));
#51596=CARTESIAN_POINT('Ctrl Pts',(-0.225735269538518,-0.306989404016411,
-1.84664115284294));
#51597=CARTESIAN_POINT('Ctrl Pts',(0.13587094405367,-0.356002798660267,
-1.8267739758998));
#51598=CARTESIAN_POINT('Ctrl Pts',(0.372870429720997,-0.0785273756829916,
-1.80690679895666));
#51599=CARTESIAN_POINT('Ctrl Pts',(0.267911857239273,0.270965205963022,
-1.78703962201352));
#51600=CARTESIAN_POINT('Ctrl Pts',(-0.0827476642965211,0.371956624010715,
-1.76717244507038));
#51601=CARTESIAN_POINT('Ctrl Pts',(-0.357519616468391,0.131828031663501,
-1.74730526812723));
#51602=CARTESIAN_POINT('Ctrl Pts',(-0.304411683155098,-0.229199548975689,
-1.72743809118409));
#51603=CARTESIAN_POINT('Ctrl Pts',(0.0278710512479263,-0.380029091773661,
-1.70757091424095));
#51604=CARTESIAN_POINT('Ctrl Pts',(0.334593350165504,-0.182335394580983,
-1.68770373729781));
#51605=CARTESIAN_POINT('Ctrl Pts',(0.334461355547943,0.182577402043658,
-1.66783656035467));
#51606=CARTESIAN_POINT('Ctrl Pts',(0.0275961191588265,0.380049155109377,
-1.64796938341153));
#51607=CARTESIAN_POINT('Ctrl Pts',(-0.304577413538642,0.228979268175285,
-1.62810220646839));
#51608=CARTESIAN_POINT('Ctrl Pts',(-0.357424154439649,-0.132086637912698,
-1.60823502952524));
#51609=CARTESIAN_POINT('Ctrl Pts',(-0.0824785577203104,-0.372016388897528,
-1.5883678525821));
#51610=CARTESIAN_POINT('Ctrl Pts',(0.268107811741657,-0.270771319336224,
-1.56850067563896));
#51611=CARTESIAN_POINT('Ctrl Pts',(0.372813523017964,0.0787971011326718,
-1.54863349869582));
#51612=CARTESIAN_POINT('Ctrl Pts',(0.135613365066933,0.35610099874502,-1.52876632175268));
#51613=CARTESIAN_POINT('Ctrl Pts',(-0.225957296096291,0.306826019810628,
-1.50889914480954));
#51614=CARTESIAN_POINT('Ctrl Pts',(-0.380303377247864,-0.023837939211441,
-1.4890319678664));
#51615=CARTESIAN_POINT('Ctrl Pts',(-0.185874672239764,-0.332640214513727,
-1.46916479092326));
#51616=CARTESIAN_POINT('Ctrl Pts',(0.179018990329492,-0.336379409585943,
-1.44929761398012));
#51617=CARTESIAN_POINT('Ctrl Pts',(0.379735015238712,-0.0316263227965929,
-1.42943043703697));
#51618=CARTESIAN_POINT('Ctrl Pts',(0.232197496633113,0.302131144785331,
-1.40956326009383));
#51619=CARTESIAN_POINT('Ctrl Pts',(-0.128287466249961,0.358805284374608,
-1.38969608315069));
#51620=CARTESIAN_POINT('Ctrl Pts',(-0.371120479965266,0.0864204573138163,
-1.36982890620755));
#51621=CARTESIAN_POINT('Ctrl Pts',(-0.273600307821276,-0.26522024366945,
-1.34996172926441));
#51622=CARTESIAN_POINT('Ctrl Pts',(0.0748376698498334,-0.373628464203982,
-1.33009455232127));
#51623=CARTESIAN_POINT('Ctrl Pts',(0.354642304090093,-0.139383436037601,
-1.31022737537813));
#51624=CARTESIAN_POINT('Ctrl Pts',(0.309205825124097,0.222689613141937,
-1.29036019843499));
#51625=CARTESIAN_POINT('Ctrl Pts',(-0.0198021443645707,0.380534861964767,
-1.27049302149184));
#51626=CARTESIAN_POINT('Ctrl Pts',(-0.330649642294355,0.189393030871235,
-1.2506258445487));
#51627=CARTESIAN_POINT('Ctrl Pts',(-0.33825960623342,-0.175440431151973,
-1.23075866760556));
#51628=CARTESIAN_POINT('Ctrl Pts',(-0.0356529670902981,-0.379378138576325,
-1.21089149066242));
#51629=CARTESIAN_POINT('Ctrl Pts',(0.299650873068665,-0.235389592720591,
-1.19102431371928));
#51630=CARTESIAN_POINT('Ctrl Pts',(0.360146033027642,0.124473856638375,
-1.17115713677614));
#51631=CARTESIAN_POINT('Ctrl Pts',(0.0903526308274595,0.37018280375314,
-1.151289959833));
#51632=CARTESIAN_POINT('Ctrl Pts',(-0.262302826724056,0.276398504309537,
-1.13142278288985));
#51633=CARTESIAN_POINT('Ctrl Pts',(-0.374401355852254,-0.0708698160571368,
-1.11155560594672));
#51634=CARTESIAN_POINT('Ctrl Pts',(-0.14313782027769,-0.353143696670534,
-1.09168842900357));
#51635=CARTESIAN_POINT('Ctrl Pts',(0.219396867869826,-0.311550831263358,
-1.07182125206043));
#51636=CARTESIAN_POINT('Ctrl Pts',(0.380723519872219,0.0157641209106834,
-1.05195407511729));
#51637=CARTESIAN_POINT('Ctrl Pts',(0.192890074506225,0.328621857533794,
-1.03208689817415));
#51638=CARTESIAN_POINT('Ctrl Pts',(-0.171842127255466,0.340101733886045,
-1.01221972123101));
#51639=CARTESIAN_POINT('Ctrl Pts',(-0.378978565286443,0.039675598866412,
-0.992352544287869));
#51640=CARTESIAN_POINT('Ctrl Pts',(-0.238555197187349,-0.297136877527654,
-0.972485367344726));
#51641=CARTESIAN_POINT('Ctrl Pts',(0.12064623827576,-0.361446249505908,
-0.952618190401585));
#51642=CARTESIAN_POINT('Ctrl Pts',(0.369203465790718,-0.0942746357198006,
-0.932751013458444));
#51643=CARTESIAN_POINT('Ctrl Pts',(0.279165593881561,0.259355889242436,
-0.912883836515302));
#51644=CARTESIAN_POINT('Ctrl Pts',(-0.0668939863116134,0.375132110978679,
-0.893016659572163));
#51645=CARTESIAN_POINT('Ctrl Pts',(-0.351605345145198,0.146876095254826,
-0.873149482629021));
#51646=CARTESIAN_POINT('Ctrl Pts',(-0.313860774312695,-0.216079430857763,
-0.85328230568588));
#51647=CARTESIAN_POINT('Ctrl Pts',(0.0117243233039672,-0.38086932973796,
-0.833415128742737));
#51648=CARTESIAN_POINT('Ctrl Pts',(0.326557088446483,-0.196365409574429,
-0.813547951799597));
#51649=CARTESIAN_POINT('Ctrl Pts',(0.341905585223924,0.168224483606484,
-0.793680774856455));
#51650=CARTESIAN_POINT('Ctrl Pts',(0.0436937654029756,0.378536340338528,
-0.773813597913315));
#51651=CARTESIAN_POINT('Ctrl Pts',(-0.294589441096693,0.241693953764487,
-0.753946420970174));
#51652=CARTESIAN_POINT('Ctrl Pts',(-0.362705787478237,-0.11680504193654,
-0.734079244027031));
#51653=CARTESIAN_POINT('Ctrl Pts',(-0.098186030593751,-0.368182576296315,
-0.714212067083892));
#51654=CARTESIAN_POINT('Ctrl Pts',(0.256379762883779,-0.281901265118838,
-0.694344890140749));
#51655=CARTESIAN_POINT('Ctrl Pts',(0.375820647341585,0.0629106280680267,
-0.674477713197609));
#51656=CARTESIAN_POINT('Ctrl Pts',(0.150597840249194,0.35002742264572,-0.654610536254467));
#51657=CARTESIAN_POINT('Ctrl Pts',(-0.212737675461616,0.316135394302848,
-0.634743359311326));
#51658=CARTESIAN_POINT('Ctrl Pts',(-0.38097227515361,-0.00768320619890207,
-0.614876182368184));
#51659=CARTESIAN_POINT('Ctrl Pts',(-0.199818644945625,-0.324455567408028,
-0.595009005425044));
#51660=CARTESIAN_POINT('Ctrl Pts',(0.164587907342214,-0.343670957237192,
-0.575141828481902));
#51661=CARTESIAN_POINT('Ctrl Pts',(0.378051513513506,-0.0477070144762039,
-0.555274651538762));
#51662=CARTESIAN_POINT('Ctrl Pts',(0.24480550918305,0.2920088504654,-0.535407474595619));
#51663=CARTESIAN_POINT('Ctrl Pts',(-0.112950699881881,0.363924505207545,
-0.515540297652479));
#51664=CARTESIAN_POINT('Ctrl Pts',(-0.367120250243846,0.102086375215724,
-0.495673120709337));
#51665=CARTESIAN_POINT('Ctrl Pts',(-0.284605209987079,-0.253374782533741,
-0.475805943766196));
#51666=CARTESIAN_POINT('Ctrl Pts',(0.0589201893379548,-0.376466887562887,
-0.455938766823054));
#51667=CARTESIAN_POINT('Ctrl Pts',(0.348410107313365,-0.154302636186626,
-0.436071589879914));
#51668=CARTESIAN_POINT('Ctrl Pts',(0.318374434175064,0.20937197736306,-0.416204412936773));
#51669=CARTESIAN_POINT('Ctrl Pts',(-0.0036412223595689,0.38103234532199,
-0.396337235993631));
#51670=CARTESIAN_POINT('Ctrl Pts',(-0.322317534834062,0.203249390469792,
-0.37647005905049));
#51671=CARTESIAN_POINT('Ctrl Pts',(-0.345397643772028,-0.160932804845182,
-0.356602882107349));
#51672=CARTESIAN_POINT('Ctrl Pts',(-0.0517149087271477,-0.377524144911485,
-0.336735705164208));
#51673=CARTESIAN_POINT('Ctrl Pts',(0.289395423456396,-0.247889502657562,
-0.316868528221066));
#51674=CARTESIAN_POINT('Ctrl Pts',(0.365102213085359,0.109083625599228,
-0.297001351277925));
#51675=CARTESIAN_POINT('Ctrl Pts',(0.105975331050231,0.366016646048953,
-0.277134174334784));
#51676=CARTESIAN_POINT('Ctrl Pts',(-0.250341478663234,0.287277049774642,
-0.257266997391643));
#51677=CARTESIAN_POINT('Ctrl Pts',(-0.377070390759466,-0.0549229767688766,
-0.237399820448501));
#51678=CARTESIAN_POINT('Ctrl Pts',(-0.157990771009751,-0.346753853915265,
-0.21753264350536));
#51679=CARTESIAN_POINT('Ctrl Pts',(0.205984064995685,-0.320577119714015,
-0.197665466562219));
#51680=CARTESIAN_POINT('Ctrl Pts',(0.381046949345406,-0.000402173207826333,
-0.177798289619077));
#51681=CARTESIAN_POINT('Ctrl Pts',(0.206662207836228,0.320145145822377,
-0.157931112675937));
#51682=CARTESIAN_POINT('Ctrl Pts',(-0.157269060983239,0.347081784885588,
-0.138063935732795));
#51683=CARTESIAN_POINT('Ctrl Pts',(-0.376936154545472,0.0557240156618553,
-0.118196758789654));
#51684=CARTESIAN_POINT('Ctrl Pts',(-0.250980323683099,-0.286762893367498,
-0.0983295818465129));
#51685=CARTESIAN_POINT('Ctrl Pts',(0.105270814003626,-0.366213039015092,
-0.0784624049033714));
#51686=CARTESIAN_POINT('Ctrl Pts',(0.364743993945667,-0.10990181424216,
-0.0585952279602307));
#51687=CARTESIAN_POINT('Ctrl Pts',(0.290165445887089,0.247375328262155,
-0.038728051017089));
#51688=CARTESIAN_POINT('Ctrl Pts',(-0.0514328106451888,0.377443120485191,
-0.0188608740739483));
#51689=CARTESIAN_POINT('Ctrl Pts',(-0.246322214574953,0.233869940566782,
-0.00561608944518735));
#51690=CARTESIAN_POINT('Ctrl Pts',(-0.291834801104466,0.136724630148766,
0.00100630286919312));
#51691=CARTESIAN_POINT('Origin',(0.,0.,-2.22));
#51692=CARTESIAN_POINT('Origin',(0.,0.,-0.04));
#51693=CARTESIAN_POINT('Origin',(0.,0.,-0.04));
#51694=CARTESIAN_POINT('',(-0.4333,5.30639458070548E-17,0.));
#51695=CARTESIAN_POINT('Origin',(-0.4333,-5.30639458070548E-17,-0.04));
#51696=CARTESIAN_POINT('Origin',(0.,0.,0.));
#51697=CARTESIAN_POINT('Origin',(0.61,0.,0.));
#51698=CARTESIAN_POINT('',(-0.61,-7.47034547479885E-17,1.04083408558608E-17));
#51699=CARTESIAN_POINT('Origin',(0.,0.,0.));
#51700=CARTESIAN_POINT('Origin',(0.,0.,0.31));
#51701=CARTESIAN_POINT('',(0.,0.,0.22));
#51702=CARTESIAN_POINT('',(-0.29999119987093,-3.67383262694308E-17,0.4));
#51703=CARTESIAN_POINT('',(-0.149995599935465,-1.83691631347154E-17,0.31));
#51704=CARTESIAN_POINT('Origin',(0.,0.,0.4));
#51705=CARTESIAN_POINT('Origin',(0.173205080756888,0.3,0.8));
#51706=CARTESIAN_POINT('',(0.173205080756888,0.3,0.8));
#51707=CARTESIAN_POINT('',(0.346410161513775,0.,0.8));
#51708=CARTESIAN_POINT('',(0.21650635094611,0.225,0.8));
#51709=CARTESIAN_POINT('',(0.173205080756888,0.3,0.4));
#51710=CARTESIAN_POINT('',(0.173205080756888,0.3,0.8));
#51711=CARTESIAN_POINT('',(0.346410161513775,0.,0.4));
#51712=CARTESIAN_POINT('',(0.346410161513775,0.,0.4));
#51713=CARTESIAN_POINT('',(0.346410161513775,0.,0.8));
#51714=CARTESIAN_POINT('Origin',(-0.173205080756888,0.3,0.8));
#51715=CARTESIAN_POINT('',(-0.173205080756888,0.3,0.8));
#51716=CARTESIAN_POINT('',(-0.0866025403784438,0.3,0.8));
#51717=CARTESIAN_POINT('',(-0.173205080756888,0.3,0.4));
#51718=CARTESIAN_POINT('',(-0.173205080756888,0.3,0.8));
#51719=CARTESIAN_POINT('',(0.173205080756888,0.3,0.4));
#51720=CARTESIAN_POINT('Origin',(-0.346410161513775,5.55111512312578E-17,
0.8));
#51721=CARTESIAN_POINT('',(-0.346410161513775,4.24230095489963E-17,0.8));
#51722=CARTESIAN_POINT('',(-0.303108891324554,0.0750000000000001,0.8));
#51723=CARTESIAN_POINT('',(-0.346410161513775,5.55111512312578E-17,0.4));
#51724=CARTESIAN_POINT('',(-0.346410161513775,4.24230095489963E-17,0.8));
#51725=CARTESIAN_POINT('',(-0.173205080756888,0.3,0.4));
#51726=CARTESIAN_POINT('Origin',(-0.173205080756888,-0.3,0.8));
#51727=CARTESIAN_POINT('',(-0.173205080756888,-0.3,0.8));
#51728=CARTESIAN_POINT('',(-0.21650635094611,-0.225,0.8));
#51729=CARTESIAN_POINT('',(-0.173205080756888,-0.3,0.4));
#51730=CARTESIAN_POINT('',(-0.173205080756888,-0.3,0.8));
#51731=CARTESIAN_POINT('',(-0.346410161513775,4.24230095489963E-17,0.4));
#51732=CARTESIAN_POINT('Origin',(0.173205080756888,-0.3,0.8));
#51733=CARTESIAN_POINT('',(0.173205080756888,-0.3,0.8));
#51734=CARTESIAN_POINT('',(0.0866025403784439,-0.3,0.8));
#51735=CARTESIAN_POINT('',(0.173205080756888,-0.3,0.4));
#51736=CARTESIAN_POINT('',(0.173205080756888,-0.3,0.8));
#51737=CARTESIAN_POINT('',(-0.173205080756888,-0.3,0.4));
#51738=CARTESIAN_POINT('Origin',(0.346410161513775,0.,0.8));
#51739=CARTESIAN_POINT('',(0.303108891324554,-0.075,0.8));
#51740=CARTESIAN_POINT('',(0.173205080756888,-0.3,0.4));
#51741=CARTESIAN_POINT('Origin',(0.,5.55111512312578E-17,0.4));
#51742=CARTESIAN_POINT('Origin',(0.635148348882184,-0.269604478657599,0.74));
#51743=CARTESIAN_POINT('',(0.605292169324788,-0.236899535149592,0.14));
#51744=CARTESIAN_POINT('',(0.605292169324788,-0.236899535149592,0.74));
#51745=CARTESIAN_POINT('',(0.605292169324788,-0.236899535149592,0.39));
#51746=CARTESIAN_POINT('',(0.582609424887263,-0.212052488861915,0.14));
#51747=CARTESIAN_POINT('',(0.635148348882184,-0.269604478657599,0.14));
#51748=CARTESIAN_POINT('',(0.582609424887263,-0.212052488861915,0.74));
#51749=CARTESIAN_POINT('',(0.582609424887263,-0.212052488861915,0.74));
#51750=CARTESIAN_POINT('',(0.635148348882184,-0.269604478657599,0.74));
#51751=CARTESIAN_POINT('Origin',(0.621229853250879,-0.235670477458144,0.74));
#51752=CARTESIAN_POINT('',(0.615956788709343,-0.207598734203447,0.74));
#51753=CARTESIAN_POINT('Origin',(0.,0.,0.74));
#51754=CARTESIAN_POINT('',(0.582609424887263,-0.212052488861915,0.74));
#51755=CARTESIAN_POINT('Origin',(0.582609424887263,-0.212052488861915,0.74));
#51756=CARTESIAN_POINT('',(0.615956788709343,-0.207598734203447,0.14));
#51757=CARTESIAN_POINT('',(0.615956788709343,-0.207598734203447,0.39));
#51758=CARTESIAN_POINT('',(0.582609424887263,-0.212052488861915,0.14));
#51759=CARTESIAN_POINT('Origin',(0.621229853250879,-0.235670477458144,0.14));
#51760=CARTESIAN_POINT('Origin',(0.,0.,0.14));
#51761=CARTESIAN_POINT('Origin',(0.504634054117228,-0.470578868443124,0.74));
#51762=CARTESIAN_POINT('',(0.48776417196835,-0.429634859554052,0.14));
#51763=CARTESIAN_POINT('',(0.48776417196835,-0.429634859554052,0.74));
#51764=CARTESIAN_POINT('',(0.48776417196835,-0.429634859554052,0.39));
#51765=CARTESIAN_POINT('',(0.474947554733766,-0.398528318005655,0.14));
#51766=CARTESIAN_POINT('',(0.504634054117228,-0.470578868443124,0.14));
#51767=CARTESIAN_POINT('',(0.474947554733766,-0.398528318005655,0.74));
#51768=CARTESIAN_POINT('',(0.474947554733766,-0.398528318005655,0.74));
#51769=CARTESIAN_POINT('',(0.504634054117228,-0.470578868443124,0.74));
#51770=CARTESIAN_POINT('Origin',(0.513003028333199,-0.434553593224389,0.74));
#51771=CARTESIAN_POINT('',(0.507807100246665,-0.405748627772263,0.74));
#51772=CARTESIAN_POINT('Origin',(0.,0.,0.74));
#51773=CARTESIAN_POINT('',(0.474947554733766,-0.398528318005655,0.74));
#51774=CARTESIAN_POINT('Origin',(0.474947554733766,-0.398528318005655,0.74));
#51775=CARTESIAN_POINT('',(0.507807100246665,-0.405748627772263,0.14));
#51776=CARTESIAN_POINT('',(0.507807100246665,-0.405748627772263,0.39));
#51777=CARTESIAN_POINT('',(0.474947554733766,-0.398528318005655,0.14));
#51778=CARTESIAN_POINT('Origin',(0.513003028333199,-0.434553593224389,0.14));
#51779=CARTESIAN_POINT('Origin',(0.,0.,0.14));
#51780=CARTESIAN_POINT('Origin',(0.313253444820287,-0.614794501689974,0.74));
#51781=CARTESIAN_POINT('',(0.311404616840027,-0.570549879161074,0.14));
#51782=CARTESIAN_POINT('',(0.311404616840027,-0.570549879161074,0.74));
#51783=CARTESIAN_POINT('',(0.311404616840027,-0.570549879161074,0.39));
#51784=CARTESIAN_POINT('',(0.31,-0.536935750346352,0.14));
#51785=CARTESIAN_POINT('',(0.313253444820287,-0.614794501689974,0.14));
#51786=CARTESIAN_POINT('',(0.31,-0.536935750346352,0.74));
#51787=CARTESIAN_POINT('',(0.31,-0.536935750346352,0.74));
#51788=CARTESIAN_POINT('',(0.313253444820287,-0.614794501689974,0.74));
#51789=CARTESIAN_POINT('Origin',(0.342900467080184,-0.575865126018163,0.74));
#51790=CARTESIAN_POINT('',(0.338408381059618,-0.55495924861976,0.74));
#51791=CARTESIAN_POINT('Origin',(0.,0.,0.74));
#51792=CARTESIAN_POINT('',(0.31,-0.536935750346352,0.74));
#51793=CARTESIAN_POINT('Origin',(0.31,-0.536935750346352,0.74));
#51794=CARTESIAN_POINT('',(0.338408381059618,-0.55495924861976,0.14));
#51795=CARTESIAN_POINT('',(0.338408381059618,-0.55495924861976,0.39));
#51796=CARTESIAN_POINT('',(0.31,-0.536935750346352,0.14));
#51797=CARTESIAN_POINT('Origin',(0.342900467080184,-0.575865126018163,0.14));
#51798=CARTESIAN_POINT('Origin',(0.,0.,0.14));
#51799=CARTESIAN_POINT('Origin',(0.0840898469495519,-0.684856844632512,
0.74));
#51800=CARTESIAN_POINT('',(0.097485069078123,-0.642648162921854,0.14));
#51801=CARTESIAN_POINT('',(0.097485069078123,-0.642648162921854,0.74));
#51802=CARTESIAN_POINT('',(0.097485069078123,-0.642648162921854,0.39));
#51803=CARTESIAN_POINT('',(0.107661870153497,-0.610580806867569,0.14));
#51804=CARTESIAN_POINT('',(0.0840898469495519,-0.684856844632512,0.14));
#51805=CARTESIAN_POINT('',(0.107661870153497,-0.610580806867569,0.74));
#51806=CARTESIAN_POINT('',(0.107661870153497,-0.610580806867569,0.74));
#51807=CARTESIAN_POINT('',(0.0840898469495519,-0.684856844632512,0.74));
#51808=CARTESIAN_POINT('Origin',(0.119653037223409,-0.647718825750041,0.74));
#51809=CARTESIAN_POINT('',(0.128192616740993,-0.637233593757499,0.74));
#51810=CARTESIAN_POINT('Origin',(0.,0.,0.74));
#51811=CARTESIAN_POINT('',(0.107661870153497,-0.610580806867569,0.74));
#51812=CARTESIAN_POINT('Origin',(0.107661870153497,-0.610580806867569,0.74));
#51813=CARTESIAN_POINT('',(0.128192616740993,-0.637233593757499,0.14));
#51814=CARTESIAN_POINT('',(0.128192616740993,-0.637233593757499,0.39));
#51815=CARTESIAN_POINT('',(0.107661870153497,-0.610580806867569,0.14));
#51816=CARTESIAN_POINT('Origin',(0.119653037223409,-0.647718825750041,0.14));
#51817=CARTESIAN_POINT('Origin',(0.,0.,0.14));
#51818=CARTESIAN_POINT('Origin',(-0.155216227497267,-0.672315344701812,
0.74));
#51819=CARTESIAN_POINT('',(-0.128192616740993,-0.637233593757499,0.14));
#51820=CARTESIAN_POINT('',(-0.128192616740993,-0.637233593757499,0.74));
#51821=CARTESIAN_POINT('',(-0.128192616740993,-0.637233593757499,0.39));
#51822=CARTESIAN_POINT('',(-0.107661870153497,-0.610580806867569,0.14));
#51823=CARTESIAN_POINT('',(-0.155216227497267,-0.672315344701812,0.14));
#51824=CARTESIAN_POINT('',(-0.107661870153497,-0.610580806867569,0.74));
#51825=CARTESIAN_POINT('',(-0.107661870153497,-0.610580806867569,0.74));
#51826=CARTESIAN_POINT('',(-0.155216227497267,-0.672315344701812,0.74));
#51827=CARTESIAN_POINT('Origin',(-0.119653037223409,-0.647718825750041,
0.74));
#51828=CARTESIAN_POINT('',(-0.097485069078123,-0.642648162921854,0.74));
#51829=CARTESIAN_POINT('Origin',(0.,0.,0.74));
#51830=CARTESIAN_POINT('',(-0.107661870153497,-0.610580806867569,0.74));
#51831=CARTESIAN_POINT('Origin',(-0.107661870153497,-0.610580806867569,
0.74));
#51832=CARTESIAN_POINT('',(-0.097485069078123,-0.642648162921854,0.14));
#51833=CARTESIAN_POINT('',(-0.097485069078123,-0.642648162921854,0.39));
#51834=CARTESIAN_POINT('',(-0.107661870153497,-0.610580806867569,0.14));
#51835=CARTESIAN_POINT('Origin',(-0.119653037223409,-0.647718825750041,
0.14));
#51836=CARTESIAN_POINT('Origin',(0.,0.,0.14));
#51837=CARTESIAN_POINT('Origin',(-0.375800934160369,-0.578682691882343,
0.74));
#51838=CARTESIAN_POINT('',(-0.338408381059618,-0.55495924861976,0.14));
#51839=CARTESIAN_POINT('',(-0.338408381059618,-0.55495924861976,0.74));
#51840=CARTESIAN_POINT('',(-0.338408381059618,-0.55495924861976,0.39));
#51841=CARTESIAN_POINT('',(-0.31,-0.536935750346352,0.14));
#51842=CARTESIAN_POINT('',(-0.375800934160369,-0.578682691882343,0.14));
#51843=CARTESIAN_POINT('',(-0.31,-0.536935750346352,0.74));
#51844=CARTESIAN_POINT('',(-0.31,-0.536935750346352,0.74));
#51845=CARTESIAN_POINT('',(-0.375800934160369,-0.578682691882343,0.74));
#51846=CARTESIAN_POINT('Origin',(-0.342900467080184,-0.575865126018163,
0.74));
#51847=CARTESIAN_POINT('',(-0.311404616840027,-0.570549879161074,0.74));
#51848=CARTESIAN_POINT('Origin',(0.,0.,0.74));
#51849=CARTESIAN_POINT('',(-0.31,-0.536935750346352,0.74));
#51850=CARTESIAN_POINT('Origin',(-0.31,-0.536935750346352,0.74));
#51851=CARTESIAN_POINT('',(-0.311404616840027,-0.570549879161074,0.14));
#51852=CARTESIAN_POINT('',(-0.311404616840027,-0.570549879161074,0.39));
#51853=CARTESIAN_POINT('',(-0.31,-0.536935750346352,0.14));
#51854=CARTESIAN_POINT('Origin',(-0.342900467080184,-0.575865126018163,
0.14));
#51855=CARTESIAN_POINT('Origin',(0.,0.,0.14));
#51856=CARTESIAN_POINT('Origin',(-0.551058501932632,-0.415252365974913,
0.74));
#51857=CARTESIAN_POINT('',(-0.507807100246665,-0.405748627772262,0.14));
#51858=CARTESIAN_POINT('',(-0.507807100246665,-0.405748627772262,0.74));
#51859=CARTESIAN_POINT('',(-0.507807100246665,-0.405748627772262,0.39));
#51860=CARTESIAN_POINT('',(-0.474947554733766,-0.398528318005654,0.14));
#51861=CARTESIAN_POINT('',(-0.551058501932632,-0.415252365974913,0.14));
#51862=CARTESIAN_POINT('',(-0.474947554733766,-0.398528318005654,0.74));
#51863=CARTESIAN_POINT('',(-0.474947554733766,-0.398528318005654,0.74));
#51864=CARTESIAN_POINT('',(-0.551058501932632,-0.415252365974913,0.74));
#51865=CARTESIAN_POINT('Origin',(-0.513003028333199,-0.434553593224389,
0.74));
#51866=CARTESIAN_POINT('',(-0.48776417196835,-0.429634859554052,0.74));
#51867=CARTESIAN_POINT('Origin',(0.,0.,0.74));
#51868=CARTESIAN_POINT('',(-0.474947554733766,-0.398528318005654,0.74));
#51869=CARTESIAN_POINT('Origin',(-0.474947554733766,-0.398528318005654,
0.74));
#51870=CARTESIAN_POINT('',(-0.48776417196835,-0.429634859554052,0.14));
#51871=CARTESIAN_POINT('',(-0.48776417196835,-0.429634859554052,0.39));
#51872=CARTESIAN_POINT('',(-0.474947554733766,-0.398528318005654,0.14));
#51873=CARTESIAN_POINT('Origin',(-0.513003028333199,-0.434553593224389,
0.14));
#51874=CARTESIAN_POINT('Origin',(0.,0.,0.14));
#51875=CARTESIAN_POINT('Origin',(-0.659850281614495,-0.201736476258688,
0.74));
#51876=CARTESIAN_POINT('',(-0.615956788709343,-0.207598734203447,0.14));
#51877=CARTESIAN_POINT('',(-0.615956788709343,-0.207598734203447,0.74));
#51878=CARTESIAN_POINT('',(-0.615956788709343,-0.207598734203447,0.39));
#51879=CARTESIAN_POINT('',(-0.582609424887263,-0.212052488861915,0.14));
#51880=CARTESIAN_POINT('',(-0.659850281614495,-0.201736476258688,0.14));
#51881=CARTESIAN_POINT('',(-0.582609424887263,-0.212052488861915,0.74));
#51882=CARTESIAN_POINT('',(-0.582609424887263,-0.212052488861915,0.74));
#51883=CARTESIAN_POINT('',(-0.659850281614495,-0.201736476258688,0.74));
#51884=CARTESIAN_POINT('Origin',(-0.621229853250879,-0.235670477458144,
0.74));
#51885=CARTESIAN_POINT('',(-0.605292169324788,-0.236899535149591,0.74));
#51886=CARTESIAN_POINT('Origin',(0.,0.,0.74));
#51887=CARTESIAN_POINT('',(-0.582609424887263,-0.212052488861915,0.74));
#51888=CARTESIAN_POINT('Origin',(-0.582609424887263,-0.212052488861915,
0.74));
#51889=CARTESIAN_POINT('',(-0.605292169324788,-0.236899535149591,0.14));
#51890=CARTESIAN_POINT('',(-0.605292169324788,-0.236899535149591,0.39));
#51891=CARTESIAN_POINT('',(-0.582609424887263,-0.212052488861915,0.14));
#51892=CARTESIAN_POINT('Origin',(-0.621229853250879,-0.235670477458144,
0.14));
#51893=CARTESIAN_POINT('Origin',(0.,0.,0.14));
#51894=CARTESIAN_POINT('Origin',(-0.689054378980656,0.0361118098076312,
0.74));
#51895=CARTESIAN_POINT('',(-0.649812997899645,0.0155906305413142,0.14));
#51896=CARTESIAN_POINT('',(-0.649812997899645,0.0155906305413142,0.74));
#51897=CARTESIAN_POINT('',(-0.649812997899645,0.0155906305413142,0.39));
#51898=CARTESIAN_POINT('',(-0.62,7.59281015471359E-17,0.14));
#51899=CARTESIAN_POINT('',(-0.689054378980656,0.0361118098076312,0.14));
#51900=CARTESIAN_POINT('',(-0.62,7.59281015471359E-17,0.74));
#51901=CARTESIAN_POINT('',(-0.62,7.59281015471359E-17,0.74));
#51902=CARTESIAN_POINT('',(-0.689054378980656,0.0361118098076312,0.74));
#51903=CARTESIAN_POINT('Origin',(-0.654527189490328,8.32667268468867E-17,
0.74));
#51904=CARTESIAN_POINT('',(-0.65,-7.9602041944578E-17,0.74));
#51905=CARTESIAN_POINT('Origin',(0.,0.,0.74));
#51906=CARTESIAN_POINT('',(-0.649812997899645,-0.015590630541314,0.74));
#51907=CARTESIAN_POINT('',(-0.62,7.59281015471359E-17,0.74));
#51908=CARTESIAN_POINT('Origin',(0.,0.,0.74));
#51909=CARTESIAN_POINT('Origin',(-0.62,7.59281015471359E-17,0.74));
#51910=CARTESIAN_POINT('',(-0.649812997899645,-0.015590630541314,0.14));
#51911=CARTESIAN_POINT('',(-0.649812997899645,-0.015590630541314,0.39));
#51912=CARTESIAN_POINT('',(-0.62,7.59281015471359E-17,0.14));
#51913=CARTESIAN_POINT('Origin',(-0.654527189490328,8.32667268468867E-17,
0.14));
#51914=CARTESIAN_POINT('',(-0.65,-7.9602041944578E-17,0.14));
#51915=CARTESIAN_POINT('Origin',(0.,0.,0.14));
#51916=CARTESIAN_POINT('Origin',(0.,0.,0.14));
#51917=CARTESIAN_POINT('Origin',(-0.672315344701812,0.155216227497267,0.74));
#51918=CARTESIAN_POINT('',(-0.637233593757499,0.128192616740993,0.14));
#51919=CARTESIAN_POINT('',(-0.637233593757499,0.128192616740993,0.74));
#51920=CARTESIAN_POINT('',(-0.637233593757499,0.128192616740993,0.39));
#51921=CARTESIAN_POINT('',(-0.610580806867569,0.107661870153497,0.14));
#51922=CARTESIAN_POINT('',(-0.672315344701812,0.155216227497267,0.14));
#51923=CARTESIAN_POINT('',(-0.610580806867569,0.107661870153497,0.74));
#51924=CARTESIAN_POINT('',(-0.610580806867569,0.107661870153497,0.74));
#51925=CARTESIAN_POINT('',(-0.672315344701812,0.155216227497267,0.74));
#51926=CARTESIAN_POINT('Origin',(-0.647718825750041,0.119653037223409,0.74));
#51927=CARTESIAN_POINT('',(-0.642648162921854,0.0974850690781231,0.74));
#51928=CARTESIAN_POINT('Origin',(0.,0.,0.74));
#51929=CARTESIAN_POINT('',(-0.610580806867569,0.107661870153497,0.74));
#51930=CARTESIAN_POINT('Origin',(-0.610580806867569,0.107661870153497,0.74));
#51931=CARTESIAN_POINT('',(-0.642648162921854,0.0974850690781231,0.14));
#51932=CARTESIAN_POINT('',(-0.642648162921854,0.0974850690781231,0.39));
#51933=CARTESIAN_POINT('',(-0.610580806867569,0.107661870153497,0.14));
#51934=CARTESIAN_POINT('Origin',(-0.647718825750041,0.119653037223409,0.14));
#51935=CARTESIAN_POINT('Origin',(0.,0.,0.14));
#51936=CARTESIAN_POINT('Origin',(-0.578682691882343,0.375800934160369,0.74));
#51937=CARTESIAN_POINT('',(-0.55495924861976,0.338408381059618,0.14));
#51938=CARTESIAN_POINT('',(-0.55495924861976,0.338408381059618,0.74));
#51939=CARTESIAN_POINT('',(-0.55495924861976,0.338408381059618,0.39));
#51940=CARTESIAN_POINT('',(-0.536935750346352,0.31,0.14));
#51941=CARTESIAN_POINT('',(-0.578682691882343,0.375800934160369,0.14));
#51942=CARTESIAN_POINT('',(-0.536935750346352,0.31,0.74));
#51943=CARTESIAN_POINT('',(-0.536935750346352,0.31,0.74));
#51944=CARTESIAN_POINT('',(-0.578682691882343,0.375800934160369,0.74));
#51945=CARTESIAN_POINT('Origin',(-0.575865126018163,0.342900467080184,0.74));
#51946=CARTESIAN_POINT('',(-0.570549879161074,0.311404616840027,0.74));
#51947=CARTESIAN_POINT('Origin',(0.,0.,0.74));
#51948=CARTESIAN_POINT('',(-0.536935750346352,0.31,0.74));
#51949=CARTESIAN_POINT('Origin',(-0.536935750346352,0.31,0.74));
#51950=CARTESIAN_POINT('',(-0.570549879161074,0.311404616840027,0.14));
#51951=CARTESIAN_POINT('',(-0.570549879161074,0.311404616840027,0.39));
#51952=CARTESIAN_POINT('',(-0.536935750346352,0.31,0.14));
#51953=CARTESIAN_POINT('Origin',(-0.575865126018163,0.342900467080184,0.14));
#51954=CARTESIAN_POINT('Origin',(0.,0.,0.14));
#51955=CARTESIAN_POINT('Origin',(-0.415252365974913,0.551058501932632,0.74));
#51956=CARTESIAN_POINT('',(-0.405748627772263,0.507807100246665,0.14));
#51957=CARTESIAN_POINT('',(-0.405748627772263,0.507807100246665,0.74));
#51958=CARTESIAN_POINT('',(-0.405748627772263,0.507807100246665,0.39));
#51959=CARTESIAN_POINT('',(-0.398528318005654,0.474947554733766,0.14));
#51960=CARTESIAN_POINT('',(-0.415252365974913,0.551058501932632,0.14));
#51961=CARTESIAN_POINT('',(-0.398528318005654,0.474947554733766,0.74));
#51962=CARTESIAN_POINT('',(-0.398528318005654,0.474947554733766,0.74));
#51963=CARTESIAN_POINT('',(-0.415252365974913,0.551058501932632,0.74));
#51964=CARTESIAN_POINT('Origin',(-0.434553593224389,0.513003028333199,0.74));
#51965=CARTESIAN_POINT('',(-0.429634859554052,0.48776417196835,0.74));
#51966=CARTESIAN_POINT('Origin',(0.,0.,0.74));
#51967=CARTESIAN_POINT('',(-0.398528318005654,0.474947554733766,0.74));
#51968=CARTESIAN_POINT('Origin',(-0.398528318005654,0.474947554733766,0.74));
#51969=CARTESIAN_POINT('',(-0.429634859554052,0.48776417196835,0.14));
#51970=CARTESIAN_POINT('',(-0.429634859554052,0.48776417196835,0.39));
#51971=CARTESIAN_POINT('',(-0.398528318005654,0.474947554733766,0.14));
#51972=CARTESIAN_POINT('Origin',(-0.434553593224389,0.513003028333199,0.14));
#51973=CARTESIAN_POINT('Origin',(0.,0.,0.14));
#51974=CARTESIAN_POINT('Origin',(-0.201736476258688,0.659850281614495,0.74));
#51975=CARTESIAN_POINT('',(-0.207598734203447,0.615956788709343,0.14));
#51976=CARTESIAN_POINT('',(-0.207598734203447,0.615956788709343,0.74));
#51977=CARTESIAN_POINT('',(-0.207598734203447,0.615956788709343,0.39));
#51978=CARTESIAN_POINT('',(-0.212052488861915,0.582609424887263,0.14));
#51979=CARTESIAN_POINT('',(-0.201736476258688,0.659850281614495,0.14));
#51980=CARTESIAN_POINT('',(-0.212052488861915,0.582609424887263,0.74));
#51981=CARTESIAN_POINT('',(-0.212052488861915,0.582609424887263,0.74));
#51982=CARTESIAN_POINT('',(-0.201736476258688,0.659850281614495,0.74));
#51983=CARTESIAN_POINT('Origin',(-0.235670477458144,0.621229853250879,0.74));
#51984=CARTESIAN_POINT('',(-0.236899535149591,0.605292169324788,0.74));
#51985=CARTESIAN_POINT('Origin',(0.,0.,0.74));
#51986=CARTESIAN_POINT('',(-0.212052488861915,0.582609424887263,0.74));
#51987=CARTESIAN_POINT('Origin',(-0.212052488861915,0.582609424887263,0.74));
#51988=CARTESIAN_POINT('',(-0.236899535149591,0.605292169324788,0.14));
#51989=CARTESIAN_POINT('',(-0.236899535149591,0.605292169324788,0.39));
#51990=CARTESIAN_POINT('',(-0.212052488861915,0.582609424887263,0.14));
#51991=CARTESIAN_POINT('Origin',(-0.235670477458144,0.621229853250879,0.14));
#51992=CARTESIAN_POINT('Origin',(0.,0.,0.14));
#51993=CARTESIAN_POINT('Origin',(0.0361118098076313,0.689054378980656,0.74));
#51994=CARTESIAN_POINT('',(0.0155906305413142,0.649812997899645,0.14));
#51995=CARTESIAN_POINT('',(0.0155906305413142,0.649812997899645,0.74));
#51996=CARTESIAN_POINT('',(0.0155906305413142,0.649812997899645,0.39));
#51997=CARTESIAN_POINT('',(3.7964050773568E-17,0.62,0.14));
#51998=CARTESIAN_POINT('',(0.0361118098076313,0.689054378980656,0.14));
#51999=CARTESIAN_POINT('',(3.7964050773568E-17,0.62,0.74));
#52000=CARTESIAN_POINT('',(3.7964050773568E-17,0.62,0.74));
#52001=CARTESIAN_POINT('',(0.0361118098076313,0.689054378980656,0.74));
#52002=CARTESIAN_POINT('Origin',(4.16333634234434E-17,0.654527189490328,
0.74));
#52003=CARTESIAN_POINT('',(-0.0155906305413141,0.649812997899645,0.74));
#52004=CARTESIAN_POINT('Origin',(0.,0.,0.74));
#52005=CARTESIAN_POINT('',(3.7964050773568E-17,0.62,0.74));
#52006=CARTESIAN_POINT('Origin',(3.7964050773568E-17,0.62,0.74));
#52007=CARTESIAN_POINT('',(-0.0155906305413141,0.649812997899645,0.14));
#52008=CARTESIAN_POINT('',(-0.0155906305413141,0.649812997899645,0.39));
#52009=CARTESIAN_POINT('',(3.7964050773568E-17,0.62,0.14));
#52010=CARTESIAN_POINT('Origin',(4.16333634234434E-17,0.654527189490328,
0.14));
#52011=CARTESIAN_POINT('Origin',(0.,0.,0.14));
#52012=CARTESIAN_POINT('Origin',(0.269604478657599,0.635148348882184,0.74));
#52013=CARTESIAN_POINT('',(0.236899535149591,0.605292169324788,0.14));
#52014=CARTESIAN_POINT('',(0.236899535149591,0.605292169324788,0.74));
#52015=CARTESIAN_POINT('',(0.236899535149591,0.605292169324788,0.39));
#52016=CARTESIAN_POINT('',(0.212052488861915,0.582609424887263,0.14));
#52017=CARTESIAN_POINT('',(0.269604478657599,0.635148348882184,0.14));
#52018=CARTESIAN_POINT('',(0.212052488861915,0.582609424887263,0.74));
#52019=CARTESIAN_POINT('',(0.212052488861915,0.582609424887263,0.74));
#52020=CARTESIAN_POINT('',(0.269604478657599,0.635148348882184,0.74));
#52021=CARTESIAN_POINT('Origin',(0.235670477458144,0.621229853250879,0.74));
#52022=CARTESIAN_POINT('',(0.207598734203447,0.615956788709343,0.74));
#52023=CARTESIAN_POINT('Origin',(0.,0.,0.74));
#52024=CARTESIAN_POINT('',(0.212052488861915,0.582609424887263,0.74));
#52025=CARTESIAN_POINT('Origin',(0.212052488861915,0.582609424887263,0.74));
#52026=CARTESIAN_POINT('',(0.207598734203447,0.615956788709343,0.14));
#52027=CARTESIAN_POINT('',(0.207598734203447,0.615956788709343,0.39));
#52028=CARTESIAN_POINT('',(0.212052488861915,0.582609424887263,0.14));
#52029=CARTESIAN_POINT('Origin',(0.235670477458144,0.621229853250879,0.14));
#52030=CARTESIAN_POINT('Origin',(0.,0.,0.14));
#52031=CARTESIAN_POINT('Origin',(0.470578868443124,0.504634054117228,0.74));
#52032=CARTESIAN_POINT('',(0.429634859554052,0.48776417196835,0.14));
#52033=CARTESIAN_POINT('',(0.429634859554052,0.48776417196835,0.74));
#52034=CARTESIAN_POINT('',(0.429634859554052,0.48776417196835,0.39));
#52035=CARTESIAN_POINT('',(0.398528318005654,0.474947554733766,0.14));
#52036=CARTESIAN_POINT('',(0.470578868443124,0.504634054117228,0.14));
#52037=CARTESIAN_POINT('',(0.398528318005654,0.474947554733766,0.74));
#52038=CARTESIAN_POINT('',(0.398528318005654,0.474947554733766,0.74));
#52039=CARTESIAN_POINT('',(0.470578868443124,0.504634054117228,0.74));
#52040=CARTESIAN_POINT('Origin',(0.434553593224389,0.513003028333199,0.74));
#52041=CARTESIAN_POINT('',(0.405748627772262,0.507807100246665,0.74));
#52042=CARTESIAN_POINT('Origin',(0.,0.,0.74));
#52043=CARTESIAN_POINT('',(0.398528318005654,0.474947554733766,0.74));
#52044=CARTESIAN_POINT('Origin',(0.398528318005654,0.474947554733766,0.74));
#52045=CARTESIAN_POINT('',(0.405748627772262,0.507807100246665,0.14));
#52046=CARTESIAN_POINT('',(0.405748627772262,0.507807100246665,0.39));
#52047=CARTESIAN_POINT('',(0.398528318005654,0.474947554733766,0.14));
#52048=CARTESIAN_POINT('Origin',(0.434553593224389,0.513003028333199,0.14));
#52049=CARTESIAN_POINT('Origin',(0.,0.,0.14));
#52050=CARTESIAN_POINT('Origin',(0.614794501689974,0.313253444820287,0.74));
#52051=CARTESIAN_POINT('',(0.570549879161074,0.311404616840027,0.14));
#52052=CARTESIAN_POINT('',(0.570549879161074,0.311404616840027,0.74));
#52053=CARTESIAN_POINT('',(0.570549879161074,0.311404616840027,0.39));
#52054=CARTESIAN_POINT('',(0.536935750346352,0.31,0.14));
#52055=CARTESIAN_POINT('',(0.614794501689974,0.313253444820287,0.14));
#52056=CARTESIAN_POINT('',(0.536935750346352,0.31,0.74));
#52057=CARTESIAN_POINT('',(0.536935750346352,0.31,0.74));
#52058=CARTESIAN_POINT('',(0.614794501689974,0.313253444820287,0.74));
#52059=CARTESIAN_POINT('Origin',(0.575865126018163,0.342900467080184,0.74));
#52060=CARTESIAN_POINT('',(0.55495924861976,0.338408381059618,0.74));
#52061=CARTESIAN_POINT('Origin',(0.,0.,0.74));
#52062=CARTESIAN_POINT('',(0.536935750346352,0.31,0.74));
#52063=CARTESIAN_POINT('Origin',(0.536935750346352,0.31,0.74));
#52064=CARTESIAN_POINT('',(0.55495924861976,0.338408381059618,0.14));
#52065=CARTESIAN_POINT('',(0.55495924861976,0.338408381059618,0.39));
#52066=CARTESIAN_POINT('',(0.536935750346352,0.31,0.14));
#52067=CARTESIAN_POINT('Origin',(0.575865126018163,0.342900467080184,0.14));
#52068=CARTESIAN_POINT('Origin',(0.,0.,0.14));
#52069=CARTESIAN_POINT('Origin',(0.684856844632512,0.0840898469495518,0.74));
#52070=CARTESIAN_POINT('',(0.642648162921854,0.0974850690781231,0.14));
#52071=CARTESIAN_POINT('',(0.642648162921854,0.0974850690781231,0.74));
#52072=CARTESIAN_POINT('',(0.642648162921854,0.0974850690781232,0.39));
#52073=CARTESIAN_POINT('',(0.610580806867569,0.107661870153497,0.14));
#52074=CARTESIAN_POINT('',(0.684856844632512,0.0840898469495518,0.14));
#52075=CARTESIAN_POINT('',(0.610580806867569,0.107661870153497,0.74));
#52076=CARTESIAN_POINT('',(0.610580806867569,0.107661870153497,0.74));
#52077=CARTESIAN_POINT('',(0.684856844632512,0.0840898469495518,0.74));
#52078=CARTESIAN_POINT('Origin',(0.647718825750041,0.119653037223409,0.74));
#52079=CARTESIAN_POINT('',(0.637233593757499,0.128192616740993,0.74));
#52080=CARTESIAN_POINT('Origin',(0.,0.,0.74));
#52081=CARTESIAN_POINT('',(0.610580806867569,0.107661870153497,0.74));
#52082=CARTESIAN_POINT('Origin',(0.610580806867569,0.107661870153497,0.74));
#52083=CARTESIAN_POINT('',(0.637233593757499,0.128192616740993,0.14));
#52084=CARTESIAN_POINT('',(0.637233593757499,0.128192616740993,0.39));
#52085=CARTESIAN_POINT('',(0.610580806867569,0.107661870153497,0.14));
#52086=CARTESIAN_POINT('Origin',(0.647718825750041,0.119653037223409,0.14));
#52087=CARTESIAN_POINT('Origin',(0.,0.,0.14));
#52088=CARTESIAN_POINT('Origin',(0.659850281614495,0.201736476258688,0.74));
#52089=CARTESIAN_POINT('',(0.615956788709343,0.207598734203447,0.14));
#52090=CARTESIAN_POINT('',(0.615956788709343,0.207598734203447,0.74));
#52091=CARTESIAN_POINT('',(0.615956788709343,0.207598734203447,0.39));
#52092=CARTESIAN_POINT('',(0.582609424887263,0.212052488861915,0.14));
#52093=CARTESIAN_POINT('',(0.659850281614495,0.201736476258688,0.14));
#52094=CARTESIAN_POINT('',(0.582609424887263,0.212052488861915,0.74));
#52095=CARTESIAN_POINT('',(0.582609424887263,0.212052488861915,0.74));
#52096=CARTESIAN_POINT('',(0.659850281614495,0.201736476258688,0.74));
#52097=CARTESIAN_POINT('Origin',(0.621229853250879,0.235670477458144,0.74));
#52098=CARTESIAN_POINT('',(0.605292169324788,0.236899535149591,0.74));
#52099=CARTESIAN_POINT('Origin',(0.,0.,0.74));
#52100=CARTESIAN_POINT('',(0.582609424887263,0.212052488861915,0.74));
#52101=CARTESIAN_POINT('Origin',(0.582609424887263,0.212052488861915,0.74));
#52102=CARTESIAN_POINT('',(0.605292169324788,0.236899535149591,0.14));
#52103=CARTESIAN_POINT('',(0.605292169324788,0.236899535149591,0.39));
#52104=CARTESIAN_POINT('',(0.582609424887263,0.212052488861915,0.14));
#52105=CARTESIAN_POINT('Origin',(0.621229853250879,0.235670477458144,0.14));
#52106=CARTESIAN_POINT('Origin',(0.,0.,0.14));
#52107=CARTESIAN_POINT('Origin',(0.551058501932632,0.415252365974913,0.74));
#52108=CARTESIAN_POINT('',(0.507807100246665,0.405748627772262,0.14));
#52109=CARTESIAN_POINT('',(0.507807100246665,0.405748627772262,0.74));
#52110=CARTESIAN_POINT('',(0.507807100246665,0.405748627772262,0.39));
#52111=CARTESIAN_POINT('',(0.474947554733766,0.398528318005654,0.14));
#52112=CARTESIAN_POINT('',(0.551058501932632,0.415252365974913,0.14));
#52113=CARTESIAN_POINT('',(0.474947554733766,0.398528318005654,0.74));
#52114=CARTESIAN_POINT('',(0.474947554733766,0.398528318005654,0.74));
#52115=CARTESIAN_POINT('',(0.551058501932632,0.415252365974913,0.74));
#52116=CARTESIAN_POINT('Origin',(0.513003028333199,0.434553593224389,0.74));
#52117=CARTESIAN_POINT('',(0.48776417196835,0.429634859554052,0.74));
#52118=CARTESIAN_POINT('Origin',(0.,0.,0.74));
#52119=CARTESIAN_POINT('',(0.474947554733766,0.398528318005654,0.74));
#52120=CARTESIAN_POINT('Origin',(0.474947554733766,0.398528318005654,0.74));
#52121=CARTESIAN_POINT('',(0.48776417196835,0.429634859554052,0.14));
#52122=CARTESIAN_POINT('',(0.48776417196835,0.429634859554052,0.39));
#52123=CARTESIAN_POINT('',(0.474947554733766,0.398528318005654,0.14));
#52124=CARTESIAN_POINT('Origin',(0.513003028333199,0.434553593224389,0.14));
#52125=CARTESIAN_POINT('Origin',(0.,0.,0.14));
#52126=CARTESIAN_POINT('Origin',(0.375800934160369,0.578682691882343,0.74));
#52127=CARTESIAN_POINT('',(0.338408381059618,0.55495924861976,0.14));
#52128=CARTESIAN_POINT('',(0.338408381059618,0.55495924861976,0.74));
#52129=CARTESIAN_POINT('',(0.338408381059618,0.55495924861976,0.39));
#52130=CARTESIAN_POINT('',(0.31,0.536935750346352,0.14));
#52131=CARTESIAN_POINT('',(0.375800934160369,0.578682691882343,0.14));
#52132=CARTESIAN_POINT('',(0.31,0.536935750346352,0.74));
#52133=CARTESIAN_POINT('',(0.31,0.536935750346352,0.74));
#52134=CARTESIAN_POINT('',(0.375800934160369,0.578682691882343,0.74));
#52135=CARTESIAN_POINT('Origin',(0.342900467080184,0.575865126018163,0.74));
#52136=CARTESIAN_POINT('',(0.311404616840027,0.570549879161074,0.74));
#52137=CARTESIAN_POINT('Origin',(0.,0.,0.74));
#52138=CARTESIAN_POINT('',(0.31,0.536935750346352,0.74));
#52139=CARTESIAN_POINT('Origin',(0.31,0.536935750346352,0.74));
#52140=CARTESIAN_POINT('',(0.311404616840027,0.570549879161074,0.14));
#52141=CARTESIAN_POINT('',(0.311404616840027,0.570549879161074,0.39));
#52142=CARTESIAN_POINT('',(0.31,0.536935750346352,0.14));
#52143=CARTESIAN_POINT('Origin',(0.342900467080184,0.575865126018163,0.14));
#52144=CARTESIAN_POINT('Origin',(0.,0.,0.14));
#52145=CARTESIAN_POINT('Origin',(0.155216227497267,0.672315344701812,0.74));
#52146=CARTESIAN_POINT('',(0.128192616740993,0.637233593757499,0.14));
#52147=CARTESIAN_POINT('',(0.128192616740993,0.637233593757499,0.74));
#52148=CARTESIAN_POINT('',(0.128192616740993,0.637233593757499,0.39));
#52149=CARTESIAN_POINT('',(0.107661870153497,0.610580806867569,0.14));
#52150=CARTESIAN_POINT('',(0.155216227497267,0.672315344701812,0.14));
#52151=CARTESIAN_POINT('',(0.107661870153497,0.610580806867569,0.74));
#52152=CARTESIAN_POINT('',(0.107661870153497,0.610580806867569,0.74));
#52153=CARTESIAN_POINT('',(0.155216227497267,0.672315344701812,0.74));
#52154=CARTESIAN_POINT('Origin',(0.119653037223409,0.647718825750041,0.74));
#52155=CARTESIAN_POINT('',(0.0974850690781232,0.642648162921854,0.74));
#52156=CARTESIAN_POINT('Origin',(0.,0.,0.74));
#52157=CARTESIAN_POINT('',(0.107661870153497,0.610580806867569,0.74));
#52158=CARTESIAN_POINT('Origin',(0.107661870153497,0.610580806867569,0.74));
#52159=CARTESIAN_POINT('',(0.0974850690781232,0.642648162921854,0.14));
#52160=CARTESIAN_POINT('',(0.0974850690781232,0.642648162921854,0.39));
#52161=CARTESIAN_POINT('',(0.107661870153497,0.610580806867569,0.14));
#52162=CARTESIAN_POINT('Origin',(0.119653037223409,0.647718825750041,0.14));
#52163=CARTESIAN_POINT('Origin',(0.,0.,0.14));
#52164=CARTESIAN_POINT('Origin',(-0.0840898469495517,0.684856844632512,
0.74));
#52165=CARTESIAN_POINT('',(-0.0974850690781231,0.642648162921854,0.14));
#52166=CARTESIAN_POINT('',(-0.0974850690781231,0.642648162921854,0.74));
#52167=CARTESIAN_POINT('',(-0.0974850690781231,0.642648162921854,0.39));
#52168=CARTESIAN_POINT('',(-0.107661870153497,0.610580806867569,0.14));
#52169=CARTESIAN_POINT('',(-0.0840898469495517,0.684856844632512,0.14));
#52170=CARTESIAN_POINT('',(-0.107661870153497,0.610580806867569,0.74));
#52171=CARTESIAN_POINT('',(-0.107661870153497,0.610580806867569,0.74));
#52172=CARTESIAN_POINT('',(-0.0840898469495517,0.684856844632512,0.74));
#52173=CARTESIAN_POINT('Origin',(-0.119653037223409,0.647718825750041,0.74));
#52174=CARTESIAN_POINT('',(-0.128192616740993,0.637233593757499,0.74));
#52175=CARTESIAN_POINT('Origin',(0.,0.,0.74));
#52176=CARTESIAN_POINT('',(-0.107661870153497,0.610580806867569,0.74));
#52177=CARTESIAN_POINT('Origin',(-0.107661870153497,0.610580806867569,0.74));
#52178=CARTESIAN_POINT('',(-0.128192616740993,0.637233593757499,0.14));
#52179=CARTESIAN_POINT('',(-0.128192616740993,0.637233593757499,0.39));
#52180=CARTESIAN_POINT('',(-0.107661870153497,0.610580806867569,0.14));
#52181=CARTESIAN_POINT('Origin',(-0.119653037223409,0.647718825750041,0.14));
#52182=CARTESIAN_POINT('Origin',(0.,0.,0.14));
#52183=CARTESIAN_POINT('Origin',(-0.313253444820287,0.614794501689974,0.74));
#52184=CARTESIAN_POINT('',(-0.311404616840027,0.570549879161074,0.14));
#52185=CARTESIAN_POINT('',(-0.311404616840027,0.570549879161074,0.74));
#52186=CARTESIAN_POINT('',(-0.311404616840027,0.570549879161074,0.39));
#52187=CARTESIAN_POINT('',(-0.31,0.536935750346352,0.14));
#52188=CARTESIAN_POINT('',(-0.313253444820287,0.614794501689974,0.14));
#52189=CARTESIAN_POINT('',(-0.31,0.536935750346352,0.74));
#52190=CARTESIAN_POINT('',(-0.31,0.536935750346352,0.74));
#52191=CARTESIAN_POINT('',(-0.313253444820287,0.614794501689974,0.74));
#52192=CARTESIAN_POINT('Origin',(-0.342900467080184,0.575865126018163,0.74));
#52193=CARTESIAN_POINT('',(-0.338408381059618,0.55495924861976,0.74));
#52194=CARTESIAN_POINT('Origin',(0.,0.,0.74));
#52195=CARTESIAN_POINT('',(-0.31,0.536935750346352,0.74));
#52196=CARTESIAN_POINT('Origin',(-0.31,0.536935750346352,0.74));
#52197=CARTESIAN_POINT('',(-0.338408381059618,0.55495924861976,0.14));
#52198=CARTESIAN_POINT('',(-0.338408381059618,0.55495924861976,0.39));
#52199=CARTESIAN_POINT('',(-0.31,0.536935750346352,0.14));
#52200=CARTESIAN_POINT('Origin',(-0.342900467080184,0.575865126018163,0.14));
#52201=CARTESIAN_POINT('Origin',(0.,0.,0.14));
#52202=CARTESIAN_POINT('Origin',(-0.504634054117228,0.470578868443124,0.74));
#52203=CARTESIAN_POINT('',(-0.48776417196835,0.429634859554052,0.14));
#52204=CARTESIAN_POINT('',(-0.48776417196835,0.429634859554052,0.74));
#52205=CARTESIAN_POINT('',(-0.48776417196835,0.429634859554052,0.39));
#52206=CARTESIAN_POINT('',(-0.474947554733766,0.398528318005654,0.14));
#52207=CARTESIAN_POINT('',(-0.504634054117228,0.470578868443124,0.14));
#52208=CARTESIAN_POINT('',(-0.474947554733766,0.398528318005654,0.74));
#52209=CARTESIAN_POINT('',(-0.474947554733766,0.398528318005654,0.74));
#52210=CARTESIAN_POINT('',(-0.504634054117228,0.470578868443124,0.74));
#52211=CARTESIAN_POINT('Origin',(-0.513003028333199,0.434553593224389,0.74));
#52212=CARTESIAN_POINT('',(-0.507807100246665,0.405748627772262,0.74));
#52213=CARTESIAN_POINT('Origin',(0.,0.,0.74));
#52214=CARTESIAN_POINT('',(-0.474947554733766,0.398528318005654,0.74));
#52215=CARTESIAN_POINT('Origin',(-0.474947554733766,0.398528318005654,0.74));
#52216=CARTESIAN_POINT('',(-0.507807100246665,0.405748627772262,0.14));
#52217=CARTESIAN_POINT('',(-0.507807100246665,0.405748627772262,0.39));
#52218=CARTESIAN_POINT('',(-0.474947554733766,0.398528318005654,0.14));
#52219=CARTESIAN_POINT('Origin',(-0.513003028333199,0.434553593224389,0.14));
#52220=CARTESIAN_POINT('Origin',(0.,0.,0.14));
#52221=CARTESIAN_POINT('Origin',(-0.635148348882184,0.269604478657599,0.74));
#52222=CARTESIAN_POINT('',(-0.605292169324788,0.236899535149591,0.14));
#52223=CARTESIAN_POINT('',(-0.605292169324788,0.236899535149591,0.74));
#52224=CARTESIAN_POINT('',(-0.605292169324788,0.236899535149591,0.39));
#52225=CARTESIAN_POINT('',(-0.582609424887263,0.212052488861915,0.14));
#52226=CARTESIAN_POINT('',(-0.635148348882184,0.269604478657599,0.14));
#52227=CARTESIAN_POINT('',(-0.582609424887263,0.212052488861915,0.74));
#52228=CARTESIAN_POINT('',(-0.582609424887263,0.212052488861915,0.74));
#52229=CARTESIAN_POINT('',(-0.635148348882184,0.269604478657599,0.74));
#52230=CARTESIAN_POINT('Origin',(-0.621229853250879,0.235670477458144,0.74));
#52231=CARTESIAN_POINT('',(-0.615956788709343,0.207598734203447,0.74));
#52232=CARTESIAN_POINT('Origin',(0.,0.,0.74));
#52233=CARTESIAN_POINT('',(-0.582609424887263,0.212052488861915,0.74));
#52234=CARTESIAN_POINT('Origin',(-0.582609424887263,0.212052488861915,0.74));
#52235=CARTESIAN_POINT('',(-0.615956788709343,0.207598734203447,0.14));
#52236=CARTESIAN_POINT('',(-0.615956788709343,0.207598734203447,0.39));
#52237=CARTESIAN_POINT('',(-0.582609424887263,0.212052488861915,0.14));
#52238=CARTESIAN_POINT('Origin',(-0.621229853250879,0.235670477458144,0.14));
#52239=CARTESIAN_POINT('Origin',(0.,0.,0.14));
#52240=CARTESIAN_POINT('Origin',(0.654527189490328,0.,0.74));
#52241=CARTESIAN_POINT('',(0.649812997899645,-0.0155906305413142,0.74));
#52242=CARTESIAN_POINT('',(0.649812997899645,0.0155906305413142,0.74));
#52243=CARTESIAN_POINT('Origin',(0.,0.,0.74));
#52244=CARTESIAN_POINT('',(0.62,0.,0.74));
#52245=CARTESIAN_POINT('',(0.689054378980656,-0.0361118098076312,0.74));
#52246=CARTESIAN_POINT('',(0.62,0.,0.74));
#52247=CARTESIAN_POINT('Origin',(0.689054378980656,-0.0361118098076312,
0.74));
#52248=CARTESIAN_POINT('',(0.649812997899645,-0.0155906305413142,0.14));
#52249=CARTESIAN_POINT('',(0.649812997899645,-0.0155906305413142,0.39));
#52250=CARTESIAN_POINT('',(0.62,0.,0.14));
#52251=CARTESIAN_POINT('',(0.689054378980656,-0.0361118098076312,0.14));
#52252=CARTESIAN_POINT('',(0.62,0.,0.74));
#52253=CARTESIAN_POINT('Origin',(0.62,0.,0.74));
#52254=CARTESIAN_POINT('',(0.649812997899645,0.0155906305413142,0.14));
#52255=CARTESIAN_POINT('',(0.649812997899645,0.0155906305413142,0.39));
#52256=CARTESIAN_POINT('',(0.62,0.,0.14));
#52257=CARTESIAN_POINT('Origin',(0.654527189490328,0.,0.14));
#52258=CARTESIAN_POINT('Origin',(0.,0.,0.14));
#52259=CARTESIAN_POINT('Origin',(-0.684856844632512,-0.0840898469495517,
0.74));
#52260=CARTESIAN_POINT('',(-0.642648162921854,-0.0974850690781232,0.14));
#52261=CARTESIAN_POINT('',(-0.642648162921854,-0.0974850690781232,0.74));
#52262=CARTESIAN_POINT('',(-0.642648162921854,-0.0974850690781232,0.39));
#52263=CARTESIAN_POINT('',(-0.610580806867569,-0.107661870153497,0.14));
#52264=CARTESIAN_POINT('',(-0.684856844632512,-0.0840898469495517,0.14));
#52265=CARTESIAN_POINT('',(-0.610580806867569,-0.107661870153497,0.74));
#52266=CARTESIAN_POINT('',(-0.610580806867569,-0.107661870153497,0.74));
#52267=CARTESIAN_POINT('',(-0.684856844632512,-0.0840898469495517,0.74));
#52268=CARTESIAN_POINT('Origin',(-0.647718825750041,-0.119653037223409,
0.74));
#52269=CARTESIAN_POINT('',(-0.637233593757499,-0.128192616740993,0.74));
#52270=CARTESIAN_POINT('Origin',(0.,0.,0.74));
#52271=CARTESIAN_POINT('',(-0.610580806867569,-0.107661870153497,0.74));
#52272=CARTESIAN_POINT('Origin',(-0.610580806867569,-0.107661870153497,
0.74));
#52273=CARTESIAN_POINT('',(-0.637233593757499,-0.128192616740993,0.14));
#52274=CARTESIAN_POINT('',(-0.637233593757499,-0.128192616740993,0.39));
#52275=CARTESIAN_POINT('',(-0.610580806867569,-0.107661870153497,0.14));
#52276=CARTESIAN_POINT('Origin',(-0.647718825750041,-0.119653037223409,
0.14));
#52277=CARTESIAN_POINT('Origin',(0.,0.,0.14));
#52278=CARTESIAN_POINT('Origin',(-0.614794501689974,-0.313253444820287,
0.74));
#52279=CARTESIAN_POINT('',(-0.570549879161074,-0.311404616840027,0.14));
#52280=CARTESIAN_POINT('',(-0.570549879161074,-0.311404616840027,0.74));
#52281=CARTESIAN_POINT('',(-0.570549879161074,-0.311404616840027,0.39));
#52282=CARTESIAN_POINT('',(-0.536935750346352,-0.31,0.14));
#52283=CARTESIAN_POINT('',(-0.614794501689974,-0.313253444820287,0.14));
#52284=CARTESIAN_POINT('',(-0.536935750346352,-0.31,0.74));
#52285=CARTESIAN_POINT('',(-0.536935750346352,-0.31,0.74));
#52286=CARTESIAN_POINT('',(-0.614794501689974,-0.313253444820287,0.74));
#52287=CARTESIAN_POINT('Origin',(-0.575865126018163,-0.342900467080184,
0.74));
#52288=CARTESIAN_POINT('',(-0.55495924861976,-0.338408381059618,0.74));
#52289=CARTESIAN_POINT('Origin',(0.,0.,0.74));
#52290=CARTESIAN_POINT('',(-0.536935750346352,-0.31,0.74));
#52291=CARTESIAN_POINT('Origin',(-0.536935750346352,-0.31,0.74));
#52292=CARTESIAN_POINT('',(-0.55495924861976,-0.338408381059618,0.14));
#52293=CARTESIAN_POINT('',(-0.55495924861976,-0.338408381059618,0.39));
#52294=CARTESIAN_POINT('',(-0.536935750346352,-0.31,0.14));
#52295=CARTESIAN_POINT('Origin',(-0.575865126018163,-0.342900467080184,
0.14));
#52296=CARTESIAN_POINT('Origin',(0.,0.,0.14));
#52297=CARTESIAN_POINT('Origin',(-0.470578868443124,-0.504634054117228,
0.74));
#52298=CARTESIAN_POINT('',(-0.429634859554052,-0.48776417196835,0.14));
#52299=CARTESIAN_POINT('',(-0.429634859554052,-0.48776417196835,0.74));
#52300=CARTESIAN_POINT('',(-0.429634859554052,-0.48776417196835,0.39));
#52301=CARTESIAN_POINT('',(-0.398528318005654,-0.474947554733766,0.14));
#52302=CARTESIAN_POINT('',(-0.470578868443124,-0.504634054117228,0.14));
#52303=CARTESIAN_POINT('',(-0.398528318005654,-0.474947554733766,0.74));
#52304=CARTESIAN_POINT('',(-0.398528318005654,-0.474947554733766,0.74));
#52305=CARTESIAN_POINT('',(-0.470578868443124,-0.504634054117228,0.74));
#52306=CARTESIAN_POINT('Origin',(-0.434553593224389,-0.513003028333199,
0.74));
#52307=CARTESIAN_POINT('',(-0.405748627772262,-0.507807100246665,0.74));
#52308=CARTESIAN_POINT('Origin',(0.,0.,0.74));
#52309=CARTESIAN_POINT('',(-0.398528318005654,-0.474947554733766,0.74));
#52310=CARTESIAN_POINT('Origin',(-0.398528318005654,-0.474947554733766,
0.74));
#52311=CARTESIAN_POINT('',(-0.405748627772262,-0.507807100246665,0.14));
#52312=CARTESIAN_POINT('',(-0.405748627772263,-0.507807100246665,0.39));
#52313=CARTESIAN_POINT('',(-0.398528318005654,-0.474947554733766,0.14));
#52314=CARTESIAN_POINT('Origin',(-0.434553593224389,-0.513003028333199,
0.14));
#52315=CARTESIAN_POINT('Origin',(0.,0.,0.14));
#52316=CARTESIAN_POINT('Origin',(-0.269604478657599,-0.635148348882184,
0.74));
#52317=CARTESIAN_POINT('',(-0.236899535149592,-0.605292169324788,0.14));
#52318=CARTESIAN_POINT('',(-0.236899535149592,-0.605292169324788,0.74));
#52319=CARTESIAN_POINT('',(-0.236899535149592,-0.605292169324788,0.39));
#52320=CARTESIAN_POINT('',(-0.212052488861914,-0.582609424887263,0.14));
#52321=CARTESIAN_POINT('',(-0.269604478657599,-0.635148348882184,0.14));
#52322=CARTESIAN_POINT('',(-0.212052488861914,-0.582609424887263,0.74));
#52323=CARTESIAN_POINT('',(-0.212052488861914,-0.582609424887263,0.74));
#52324=CARTESIAN_POINT('',(-0.269604478657599,-0.635148348882184,0.74));
#52325=CARTESIAN_POINT('Origin',(-0.235670477458144,-0.621229853250879,
0.74));
#52326=CARTESIAN_POINT('',(-0.207598734203447,-0.615956788709343,0.74));
#52327=CARTESIAN_POINT('Origin',(0.,0.,0.74));
#52328=CARTESIAN_POINT('',(-0.212052488861914,-0.582609424887263,0.74));
#52329=CARTESIAN_POINT('Origin',(-0.212052488861914,-0.582609424887263,
0.74));
#52330=CARTESIAN_POINT('',(-0.207598734203447,-0.615956788709343,0.14));
#52331=CARTESIAN_POINT('',(-0.207598734203447,-0.615956788709343,0.39));
#52332=CARTESIAN_POINT('',(-0.212052488861914,-0.582609424887263,0.14));
#52333=CARTESIAN_POINT('Origin',(-0.235670477458144,-0.621229853250879,
0.14));
#52334=CARTESIAN_POINT('Origin',(0.,0.,0.14));
#52335=CARTESIAN_POINT('Origin',(-0.0361118098076316,-0.689054378980656,
0.74));
#52336=CARTESIAN_POINT('',(-0.0155906305413143,-0.649812997899645,0.14));
#52337=CARTESIAN_POINT('',(-0.0155906305413143,-0.649812997899645,0.74));
#52338=CARTESIAN_POINT('',(-0.0155906305413143,-0.649812997899645,0.39));
#52339=CARTESIAN_POINT('',(-1.13892152320704E-16,-0.62,0.14));
#52340=CARTESIAN_POINT('',(-0.0361118098076316,-0.689054378980656,0.14));
#52341=CARTESIAN_POINT('',(-1.13892152320704E-16,-0.62,0.74));
#52342=CARTESIAN_POINT('',(-1.13892152320704E-16,-0.62,0.74));
#52343=CARTESIAN_POINT('',(-0.0361118098076316,-0.689054378980656,0.74));
#52344=CARTESIAN_POINT('Origin',(-1.2490009027033E-16,-0.654527189490328,
0.74));
#52345=CARTESIAN_POINT('',(0.0155906305413141,-0.649812997899645,0.74));
#52346=CARTESIAN_POINT('Origin',(0.,0.,0.74));
#52347=CARTESIAN_POINT('',(-1.13892152320704E-16,-0.62,0.74));
#52348=CARTESIAN_POINT('Origin',(-1.13892152320704E-16,-0.62,0.74));
#52349=CARTESIAN_POINT('',(0.0155906305413141,-0.649812997899645,0.14));
#52350=CARTESIAN_POINT('',(0.0155906305413141,-0.649812997899645,0.39));
#52351=CARTESIAN_POINT('',(-1.13892152320704E-16,-0.62,0.14));
#52352=CARTESIAN_POINT('Origin',(-1.2490009027033E-16,-0.654527189490328,
0.14));
#52353=CARTESIAN_POINT('Origin',(0.,0.,0.14));
#52354=CARTESIAN_POINT('Origin',(0.201736476258688,-0.659850281614495,0.74));
#52355=CARTESIAN_POINT('',(0.207598734203447,-0.615956788709343,0.14));
#52356=CARTESIAN_POINT('',(0.207598734203447,-0.615956788709343,0.74));
#52357=CARTESIAN_POINT('',(0.207598734203447,-0.615956788709343,0.39));
#52358=CARTESIAN_POINT('',(0.212052488861915,-0.582609424887263,0.14));
#52359=CARTESIAN_POINT('',(0.201736476258688,-0.659850281614495,0.14));
#52360=CARTESIAN_POINT('',(0.212052488861915,-0.582609424887263,0.74));
#52361=CARTESIAN_POINT('',(0.212052488861915,-0.582609424887263,0.74));
#52362=CARTESIAN_POINT('',(0.201736476258688,-0.659850281614495,0.74));
#52363=CARTESIAN_POINT('Origin',(0.235670477458144,-0.621229853250879,0.74));
#52364=CARTESIAN_POINT('',(0.236899535149591,-0.605292169324788,0.74));
#52365=CARTESIAN_POINT('Origin',(0.,0.,0.74));
#52366=CARTESIAN_POINT('',(0.212052488861915,-0.582609424887263,0.74));
#52367=CARTESIAN_POINT('Origin',(0.212052488861915,-0.582609424887263,0.74));
#52368=CARTESIAN_POINT('',(0.236899535149591,-0.605292169324788,0.14));
#52369=CARTESIAN_POINT('',(0.236899535149591,-0.605292169324788,0.39));
#52370=CARTESIAN_POINT('',(0.212052488861915,-0.582609424887263,0.14));
#52371=CARTESIAN_POINT('Origin',(0.235670477458144,-0.621229853250879,0.14));
#52372=CARTESIAN_POINT('Origin',(0.,0.,0.14));
#52373=CARTESIAN_POINT('Origin',(0.415252365974913,-0.551058501932632,0.74));
#52374=CARTESIAN_POINT('',(0.405748627772262,-0.507807100246665,0.14));
#52375=CARTESIAN_POINT('',(0.405748627772262,-0.507807100246665,0.74));
#52376=CARTESIAN_POINT('',(0.405748627772262,-0.507807100246665,0.39));
#52377=CARTESIAN_POINT('',(0.398528318005654,-0.474947554733766,0.14));
#52378=CARTESIAN_POINT('',(0.415252365974913,-0.551058501932632,0.14));
#52379=CARTESIAN_POINT('',(0.398528318005654,-0.474947554733766,0.74));
#52380=CARTESIAN_POINT('',(0.398528318005654,-0.474947554733766,0.74));
#52381=CARTESIAN_POINT('',(0.415252365974913,-0.551058501932632,0.74));
#52382=CARTESIAN_POINT('Origin',(0.434553593224389,-0.513003028333199,0.74));
#52383=CARTESIAN_POINT('',(0.429634859554052,-0.48776417196835,0.74));
#52384=CARTESIAN_POINT('Origin',(0.,0.,0.74));
#52385=CARTESIAN_POINT('',(0.398528318005654,-0.474947554733766,0.74));
#52386=CARTESIAN_POINT('Origin',(0.398528318005654,-0.474947554733766,0.74));
#52387=CARTESIAN_POINT('',(0.429634859554052,-0.48776417196835,0.14));
#52388=CARTESIAN_POINT('',(0.429634859554052,-0.48776417196835,0.39));
#52389=CARTESIAN_POINT('',(0.398528318005654,-0.474947554733766,0.14));
#52390=CARTESIAN_POINT('Origin',(0.434553593224389,-0.513003028333199,0.14));
#52391=CARTESIAN_POINT('Origin',(0.,0.,0.14));
#52392=CARTESIAN_POINT('Origin',(0.578682691882343,-0.375800934160369,0.74));
#52393=CARTESIAN_POINT('',(0.55495924861976,-0.338408381059618,0.14));
#52394=CARTESIAN_POINT('',(0.55495924861976,-0.338408381059618,0.74));
#52395=CARTESIAN_POINT('',(0.55495924861976,-0.338408381059618,0.39));
#52396=CARTESIAN_POINT('',(0.536935750346352,-0.31,0.14));
#52397=CARTESIAN_POINT('',(0.578682691882343,-0.375800934160369,0.14));
#52398=CARTESIAN_POINT('',(0.536935750346352,-0.31,0.74));
#52399=CARTESIAN_POINT('',(0.536935750346352,-0.31,0.74));
#52400=CARTESIAN_POINT('',(0.578682691882343,-0.375800934160369,0.74));
#52401=CARTESIAN_POINT('Origin',(0.575865126018163,-0.342900467080184,0.74));
#52402=CARTESIAN_POINT('',(0.570549879161074,-0.311404616840027,0.74));
#52403=CARTESIAN_POINT('Origin',(0.,0.,0.74));
#52404=CARTESIAN_POINT('',(0.536935750346352,-0.31,0.74));
#52405=CARTESIAN_POINT('Origin',(0.536935750346352,-0.31,0.74));
#52406=CARTESIAN_POINT('',(0.570549879161074,-0.311404616840027,0.14));
#52407=CARTESIAN_POINT('',(0.570549879161074,-0.311404616840027,0.39));
#52408=CARTESIAN_POINT('',(0.536935750346352,-0.31,0.14));
#52409=CARTESIAN_POINT('Origin',(0.575865126018163,-0.342900467080184,0.14));
#52410=CARTESIAN_POINT('Origin',(0.,0.,0.14));
#52411=CARTESIAN_POINT('Origin',(0.672315344701812,-0.155216227497267,0.74));
#52412=CARTESIAN_POINT('',(0.637233593757499,-0.128192616740993,0.14));
#52413=CARTESIAN_POINT('',(0.637233593757499,-0.128192616740993,0.74));
#52414=CARTESIAN_POINT('',(0.637233593757499,-0.128192616740993,0.39));
#52415=CARTESIAN_POINT('',(0.610580806867569,-0.107661870153497,0.14));
#52416=CARTESIAN_POINT('',(0.672315344701812,-0.155216227497267,0.14));
#52417=CARTESIAN_POINT('',(0.610580806867569,-0.107661870153497,0.74));
#52418=CARTESIAN_POINT('',(0.610580806867569,-0.107661870153497,0.74));
#52419=CARTESIAN_POINT('',(0.672315344701812,-0.155216227497267,0.74));
#52420=CARTESIAN_POINT('Origin',(0.647718825750041,-0.119653037223409,0.74));
#52421=CARTESIAN_POINT('',(0.642648162921854,-0.0974850690781231,0.74));
#52422=CARTESIAN_POINT('Origin',(0.,0.,0.74));
#52423=CARTESIAN_POINT('',(0.610580806867569,-0.107661870153497,0.74));
#52424=CARTESIAN_POINT('Origin',(0.610580806867569,-0.107661870153497,0.74));
#52425=CARTESIAN_POINT('',(0.642648162921854,-0.0974850690781231,0.14));
#52426=CARTESIAN_POINT('',(0.642648162921854,-0.0974850690781231,0.39));
#52427=CARTESIAN_POINT('',(0.610580806867569,-0.107661870153497,0.14));
#52428=CARTESIAN_POINT('Origin',(0.647718825750041,-0.119653037223409,0.14));
#52429=CARTESIAN_POINT('Origin',(0.,0.,0.14));
#52430=CARTESIAN_POINT('Origin',(0.34,0.,-4.5));
#52431=CARTESIAN_POINT('',(-0.34,-4.163799117101E-17,-4.5));
#52432=CARTESIAN_POINT('Origin',(0.,0.,-4.5));
#52433=CARTESIAN_POINT('Origin',(0.,0.,-4.47));
#52434=CARTESIAN_POINT('',(-0.37,-4.53119315684521E-17,-4.47));
#52435=CARTESIAN_POINT('Origin',(0.,0.,0.02));
#52436=CARTESIAN_POINT('',(-0.65,-7.9602041944578E-17,0.04));
#52437=CARTESIAN_POINT('Origin',(0.,0.,0.04));
#52438=CARTESIAN_POINT('',(-0.63,-7.71527483462833E-17,0.02));
#52439=CARTESIAN_POINT('Origin',(0.,0.,0.39));
#52440=CARTESIAN_POINT('Origin',(0.,0.,0.74));
#52441=CARTESIAN_POINT('Origin',(0.,0.,0.74));
#52442=CARTESIAN_POINT('Origin',(0.,0.,0.74));
#52443=CARTESIAN_POINT('Origin',(0.,0.,0.74));
#52444=CARTESIAN_POINT('Origin',(0.,0.,0.74));
#52445=CARTESIAN_POINT('Origin',(0.,0.,0.74));
#52446=CARTESIAN_POINT('Origin',(0.,0.,0.74));
#52447=CARTESIAN_POINT('Origin',(0.,0.,0.74));
#52448=CARTESIAN_POINT('Origin',(0.,0.,0.74));
#52449=CARTESIAN_POINT('Origin',(0.,0.,0.74));
#52450=CARTESIAN_POINT('Origin',(0.,0.,0.74));
#52451=CARTESIAN_POINT('Origin',(0.,0.,0.74));
#52452=CARTESIAN_POINT('Origin',(0.,0.,0.74));
#52453=CARTESIAN_POINT('Origin',(0.,0.,0.74));
#52454=CARTESIAN_POINT('Origin',(0.,0.,0.74));
#52455=CARTESIAN_POINT('Origin',(0.,0.,0.74));
#52456=CARTESIAN_POINT('',(-0.65,-7.9602041944578E-17,0.39));
#52457=CARTESIAN_POINT('Origin',(0.,0.,0.74));
#52458=CARTESIAN_POINT('Origin',(0.,0.,0.74));
#52459=CARTESIAN_POINT('Origin',(0.,0.,0.74));
#52460=CARTESIAN_POINT('Origin',(0.,0.,0.74));
#52461=CARTESIAN_POINT('Origin',(0.,0.,0.74));
#52462=CARTESIAN_POINT('Origin',(0.,0.,0.74));
#52463=CARTESIAN_POINT('Origin',(0.,0.,0.74));
#52464=CARTESIAN_POINT('Origin',(0.,0.,0.74));
#52465=CARTESIAN_POINT('Origin',(0.,0.,0.74));
#52466=CARTESIAN_POINT('Origin',(0.,0.,0.74));
#52467=CARTESIAN_POINT('Origin',(0.,0.,0.74));
#52468=CARTESIAN_POINT('Origin',(0.,0.,0.74));
#52469=CARTESIAN_POINT('Origin',(0.,0.,0.74));
#52470=CARTESIAN_POINT('Origin',(0.,0.,0.74));
#52471=CARTESIAN_POINT('Origin',(0.,0.,0.74));
#52472=CARTESIAN_POINT('Origin',(0.,0.,0.74));
#52473=CARTESIAN_POINT('Origin',(0.,0.,0.74));
#52474=CARTESIAN_POINT('Origin',(0.,0.,0.74));
#52475=CARTESIAN_POINT('Origin',(0.,0.,0.74));
#52476=CARTESIAN_POINT('Origin',(0.,0.,0.74));
#52477=CARTESIAN_POINT('Origin',(0.,0.,0.77));
#52478=CARTESIAN_POINT('',(-0.59,-7.22541611496939E-17,0.8));
#52479=CARTESIAN_POINT('Origin',(0.,0.,0.8));
#52480=CARTESIAN_POINT('',(-0.62,-7.59281015471359E-17,0.77));
#52481=CARTESIAN_POINT('Origin',(0.,0.,0.8));
#59180=UNCERTAINTY_MEASURE_WITH_UNIT(LENGTH_MEASURE(0.001),#59205,
'DISTANCE_ACCURACY_VALUE',
'Maximum model space distance between geometric entities at asserted c
onnectivities');
#59182=UNCERTAINTY_MEASURE_WITH_UNIT(LENGTH_MEASURE(0.001),#59205,
'DISTANCE_ACCURACY_VALUE',
'Maximum model space distance between geometric entities at asserted c
onnectivities');
#59202=(
GEOMETRIC_REPRESENTATION_CONTEXT(3)
GLOBAL_UNCERTAINTY_ASSIGNED_CONTEXT((#59180))
GLOBAL_UNIT_ASSIGNED_CONTEXT((#59205,#59207,#59208))
REPRESENTATION_CONTEXT('','3D')
);
#59204=(
GEOMETRIC_REPRESENTATION_CONTEXT(3)
GLOBAL_UNCERTAINTY_ASSIGNED_CONTEXT((#59182))
GLOBAL_UNIT_ASSIGNED_CONTEXT((#59205,#59207,#59208))
REPRESENTATION_CONTEXT('','3D')
);
#59205=(
LENGTH_UNIT()
NAMED_UNIT(*)
SI_UNIT(.CENTI.,.METRE.)
);
#59207=(
NAMED_UNIT(*)
PLANE_ANGLE_UNIT()
SI_UNIT($,.RADIAN.)
);
#59208=(
NAMED_UNIT(*)
SI_UNIT($,.STERADIAN.)
SOLID_ANGLE_UNIT()
);
#59228=SHAPE_DEFINITION_REPRESENTATION(#59249,#59315);
#59249=PRODUCT_DEFINITION_SHAPE('',$,#59337);
#59315=SHAPE_REPRESENTATION('',(#24661),#59202);
#59317=PRODUCT_DEFINITION_CONTEXT('part definition',#59382,'design');
#59337=PRODUCT_DEFINITION('2026-10-23-00-47-30-365',
'17_ISO_4762_M8x45-12.9_Socket_Head_Screw',#59358,#59317);
#59358=PRODUCT_DEFINITION_FORMATION('',$,#59403);
#59382=APPLICATION_CONTEXT(
'Core Data for Automotive Mechanical Design Process');
#59383=PRODUCT_CONTEXT('part definition',#59382,'mechanical');
#59403=PRODUCT('2026-10-23-00-47-30-365',
'17_ISO_4762_M8x45-12.9_Socket_Head_Screw',$,(#59383));
#59587=COLOUR_RGB('Black',0.12,0.14,0.17);
#59588=FILL_AREA_STYLE_COLOUR('',#59587);
#59589=FILL_AREA_STYLE('',(#59588));
#59590=SURFACE_STYLE_FILL_AREA(#59589);
#59591=SURFACE_SIDE_STYLE('',(#59590));
#59592=SURFACE_STYLE_USAGE(.BOTH.,#59591);
#59593=PRESENTATION_STYLE_ASSIGNMENT((#59592));
ENDSEC;
END-ISO-10303-21;
